ISO-10303-21;
HEADER;
FILE_DESCRIPTION (('STEP AP214'),
    '1' );
FILE_NAME ('spring holder_ISO - Spur gear 0.8M 60T 20PA 3FW ---S60A75H50L8.0N.step',
    '2026-10-08T12:30:53',
    ( '' ),
    ( '' ),
    'SwSTEP 2.0',
    'SolidWorks 2026',
    '' );
FILE_SCHEMA (( 'AUTOMOTIVE_DESIGN' ));
ENDSEC;

DATA;
#1=VECTOR ( 'NONE', #9436, 1000.000000000000000 ) ;
#2=CARTESIAN_POINT ( 'NONE',  ( 0.000000000000000000, 11.20082935824103565, -20.08719549084853284 ) ) ;
#3=CIRCLE ( 'NONE', #2554, 9.599999999999994316 ) ;
#4=ORIENTED_EDGE ( 'NONE', *, *, #1712, .F. ) ;
#6=CARTESIAN_POINT ( 'NONE',  ( 3.000000000000000888, -19.29833442572367375, 11.67026512804540950 ) ) ;
#7=CIRCLE ( 'NONE', #8025, 9.599999999999996092 ) ;
#8=DIRECTION ( 'NONE',  ( 0.000000000000000000, 0.000000000000000000, 1.000000000000000000 ) ) ;
#9=AXIS2_PLACEMENT_3D ( 'NONE', #2328, #5147, #7953 ) ;
#10=DIRECTION ( 'NONE',  ( 0.000000000000000000, 0.000000000000000000, 1.000000000000000000 ) ) ;
#13=DIRECTION ( 'NONE',  ( -1.000000000000000000, -0.000000000000000000, -0.000000000000000000 ) ) ;
#16=ORIENTED_EDGE ( 'NONE', *, *, #10840, .T. ) ;
#17=AXIS2_PLACEMENT_3D ( 'NONE', #6287, #975, #11260 ) ;
#20=AXIS2_PLACEMENT_3D ( 'NONE', #2237, #8791, #3220 ) ;
#22=ORIENTED_EDGE ( 'NONE', *, *, #6904, .T. ) ;
#23=CIRCLE ( 'NONE', #4524, 9.599999999999997868 ) ;
#24=ADVANCED_FACE ( 'NONE', ( #5969 ), #4246, .T. ) ;
#27=DIRECTION ( 'NONE',  ( -1.000000000000000000, 0.000000000000000000, -0.000000000000000000 ) ) ;
#28=DIRECTION ( 'NONE',  ( -1.000000000000000000, 0.000000000000000000, 0.000000000000000000 ) ) ;
#29=CARTESIAN_POINT ( 'NONE',  ( 3.000000000000000888, 21.14796121233209192, -9.039786367038628256 ) ) ;
#30=CIRCLE ( 'NONE', #1023, 22.99899999999999878 ) ;
#32=EDGE_CURVE ( 'NONE', #9019, #7573, #5110, .T. ) ;
#33=DIRECTION ( 'NONE',  ( 0.000000000000000000, 0.3090169943749479509, -0.9510565162951534202 ) ) ;
#34=DIRECTION ( 'NONE',  ( 0.000000000000000000, -1.000000000000000000, -1.048062100069321163E-14 ) ) ;
#35=VERTEX_POINT ( 'NONE', #7865 ) ;
#36=ORIENTED_EDGE ( 'NONE', *, *, #9803, .F. ) ;
#37=ORIENTED_EDGE ( 'NONE', *, *, #3148, .F. ) ;
#38=VECTOR ( 'NONE', #7219, 1000.000000000000000 ) ;
#39=ORIENTED_EDGE ( 'NONE', *, *, #3079, .T. ) ;
#40=DIRECTION ( 'NONE',  ( -1.000000000000000000, 0.000000000000000000, 0.000000000000000000 ) ) ;
#41=AXIS2_PLACEMENT_3D ( 'NONE', #9489, #9312, #7403 ) ;
#42=DIRECTION ( 'NONE',  ( 0.000000000000000000, 0.000000000000000000, 1.000000000000000000 ) ) ;
#43=DIRECTION ( 'NONE',  ( -1.000000000000000000, 0.000000000000000000, 0.000000000000000000 ) ) ;
#44=LINE ( 'NONE', #10212, #8176 ) ;
#45=CARTESIAN_POINT ( 'NONE',  ( 3.000000000000000888, 0.000000000000000000, 0.000000000000000000 ) ) ;
#47=DIRECTION ( 'NONE',  ( 0.000000000000000000, 0.000000000000000000, 1.000000000000000000 ) ) ;
#48=AXIS2_PLACEMENT_3D ( 'NONE', #10892, #6417, #1590 ) ;
#49=CARTESIAN_POINT ( 'NONE',  ( 0.000000000000000000, -6.168200451485582825, -24.02068490260619171 ) ) ;
#50=ORIENTED_EDGE ( 'NONE', *, *, #1342, .T. ) ;
#51=ORIENTED_EDGE ( 'NONE', *, *, #6988, .T. ) ;
#52=VECTOR ( 'NONE', #9630, 1000.000000000000000 ) ;
#53=DIRECTION ( 'NONE',  ( -1.000000000000000000, 0.000000000000000000, 0.000000000000000000 ) ) ;
#54=ORIENTED_EDGE ( 'NONE', *, *, #10768, .T. ) ;
#55=DIRECTION ( 'NONE',  ( 0.000000000000000000, -0.8090169943749407899, -0.5877852522924822409 ) ) ;
#56=AXIS2_PLACEMENT_3D ( 'NONE', #9179, #2517, #5398 ) ;
#57=FACE_OUTER_BOUND ( 'NONE', #11142, .T. ) ;
#58=EDGE_LOOP ( 'NONE', ( #4252, #3617, #2595, #8061 ) ) ;
#59=VECTOR ( 'NONE', #9290, 1000.000000000000000 ) ;
#60=CARTESIAN_POINT ( 'NONE',  ( 0.000000000000000000, 23.05871956130134492, -9.128825345752797915 ) ) ;
#61=VECTOR ( 'NONE', #2880, 1000.000000000000000 ) ;
#62=CARTESIAN_POINT ( 'NONE',  ( 1.500000000000000444, 13.72351598154924979, -20.65684170206477788 ) ) ;
#64=DIRECTION ( 'NONE',  ( -1.000000000000000000, 0.000000000000000000, 0.000000000000000000 ) ) ;
#65=DIRECTION ( 'NONE',  ( -1.000000000000000000, 0.000000000000000000, 0.000000000000000000 ) ) ;
#66=AXIS2_PLACEMENT_3D ( 'NONE', #9964, #4339, #1589 ) ;
#67=VERTEX_POINT ( 'NONE', #3096 ) ;
#68=DIRECTION ( 'NONE',  ( 0.000000000000000000, 0.3090169943749479509, -0.9510565162951534202 ) ) ;
#69=ADVANCED_FACE ( 'NONE', ( #8905 ), #11651, .T. ) ;
#70=EDGE_LOOP ( 'NONE', ( #8780, #11207, #4314, #267 ) ) ;
#71=EDGE_CURVE ( 'NONE', #10823, #3496, #9699, .T. ) ;
#72=EDGE_CURVE ( 'NONE', #67, #4226, #10582, .T. ) ;
#74=DIRECTION ( 'NONE',  ( -1.000000000000000000, 0.000000000000000000, 0.000000000000000000 ) ) ;
#75=CIRCLE ( 'NONE', #9465, 9.599999999999996092 ) ;
#76=CARTESIAN_POINT ( 'NONE',  ( 3.000000000000000888, 4.445336973060856955, 22.56530478845650123 ) ) ;
#77=CARTESIAN_POINT ( 'NONE',  ( 0.000000000000000000, 0.000000000000000000, 0.000000000000000000 ) ) ;
#80=CYLINDRICAL_SURFACE ( 'NONE', #11012, 24.80000000000000071 ) ;
#81=EDGE_CURVE ( 'NONE', #3630, #9406, #2177, .T. ) ;
#82=CARTESIAN_POINT ( 'NONE',  ( 0.000000000000000000, -9.128825345752877851, -23.05871956130131650 ) ) ;
#83=EDGE_LOOP ( 'NONE', ( #9902, #9745, #3116, #9830 ) ) ;
#85=CIRCLE ( 'NONE', #8890, 9.599999999999996092 ) ;
#89=FACE_OUTER_BOUND ( 'NONE', #5570, .T. ) ;
#90=EDGE_CURVE ( 'NONE', #11050, #6456, #8224, .T. ) ;
#92=DIRECTION ( 'NONE',  ( -1.000000000000000000, 0.000000000000000000, -0.000000000000000000 ) ) ;
#93=ADVANCED_FACE ( 'NONE', ( #4372 ), #1729, .T. ) ;
#94=CYLINDRICAL_SURFACE ( 'NONE', #1594, 9.600000000000001421 ) ;
#95=EDGE_LOOP ( 'NONE', ( #11816, #4327, #9723, #6573 ) ) ;
#97=EDGE_LOOP ( 'NONE', ( #3670, #7839, #7441, #7336 ) ) ;
#99=AXIS2_PLACEMENT_3D ( 'NONE', #9136, #8103, #9261 ) ;
#100=CYLINDRICAL_SURFACE ( 'NONE', #2958, 9.599999999999997868 ) ;
#101=EDGE_CURVE ( 'NONE', #2317, #5920, #9198, .T. ) ;
#102=CARTESIAN_POINT ( 'NONE',  ( 1.500000000000000444, -17.71842311621541555, 17.35216073792434699 ) ) ;
#103=CARTESIAN_POINT ( 'NONE',  ( 3.000000000000000888, 0.000000000000000000, 0.000000000000000000 ) ) ;
#104=DIRECTION ( 'NONE',  ( 0.000000000000000000, 0.000000000000000000, 1.000000000000000000 ) ) ;
#106=ADVANCED_FACE ( 'NONE', ( #7353 ), #11098, .T. ) ;
#107=CIRCLE ( 'NONE', #4811, 9.599999999999997868 ) ;
#108=DIRECTION ( 'NONE',  ( 0.000000000000000000, 0.9135454576425990902, 0.4067366430758040385 ) ) ;
#110=VERTEX_POINT ( 'NONE', #8057 ) ;
#112=ORIENTED_EDGE ( 'NONE', *, *, #7114, .T. ) ;
#113=LINE ( 'NONE', #9365, #1823 ) ;
#114=EDGE_CURVE ( 'NONE', #4536, #8735, #5706, .T. ) ;
#115=CARTESIAN_POINT ( 'NONE',  ( 3.000000000000000888, -13.79477846460783574, -18.40266524480602683 ) ) ;
#116=VECTOR ( 'NONE', #1337, 1000.000000000000000 ) ;
#117=VERTEX_POINT ( 'NONE', #8324 ) ;
#118=DIRECTION ( 'NONE',  ( -1.000000000000000000, 0.000000000000000000, 0.000000000000000000 ) ) ;
#119=DIRECTION ( 'NONE',  ( 0.000000000000000000, 0.000000000000000000, 1.000000000000000000 ) ) ;
#121=CARTESIAN_POINT ( 'NONE',  ( 1.500000000000000444, -19.10918332567968037, 15.80756504416684649 ) ) ;
#122=LINE ( 'NONE', #10596, #2752 ) ;
#123=EDGE_LOOP ( 'NONE', ( #5719, #2257, #1328, #877 ) ) ;
#124=ORIENTED_EDGE ( 'NONE', *, *, #10581, .T. ) ;
#125=CYLINDRICAL_SURFACE ( 'NONE', #591, 24.80000000000000071 ) ;
#126=ORIENTED_EDGE ( 'NONE', *, *, #101, .T. ) ;
#128=DIRECTION ( 'NONE',  ( -1.000000000000000000, -0.000000000000000000, 0.000000000000000000 ) ) ;
#129=DIRECTION ( 'NONE',  ( -1.000000000000000000, -0.000000000000000000, -0.000000000000000000 ) ) ;
#130=DIRECTION ( 'NONE',  ( -1.000000000000000000, -0.000000000000000000, -0.000000000000000000 ) ) ;
#132=CARTESIAN_POINT ( 'NONE',  ( 3.000000000000000888, -20.08719549084857192, -11.20082935824096459 ) ) ;
#133=DIRECTION ( 'NONE',  ( 0.000000000000000000, 0.000000000000000000, 1.000000000000000000 ) ) ;
#134=EDGE_CURVE ( 'NONE', #11556, #1082, #8831, .T. ) ;
#135=CARTESIAN_POINT ( 'NONE',  ( 0.000000000000000000, 23.88662356770124262, -6.668524164681382871 ) ) ;
#136=EDGE_LOOP ( 'NONE', ( #8153, #10755, #690, #2326 ) ) ;
#137=CARTESIAN_POINT ( 'NONE',  ( 3.000000000000000888, 23.05871956130122769, 9.128825345753107001 ) ) ;
#138=ADVANCED_FACE ( 'NONE', ( #8260 ), #9330, .T. ) ;
#139=VERTEX_POINT ( 'NONE', #6556 ) ;
#140=AXIS2_PLACEMENT_3D ( 'NONE', #1311, #3213, #4191 ) ;
#141=DIRECTION ( 'NONE',  ( -1.000000000000000000, 0.000000000000000000, 0.000000000000000000 ) ) ;
#143=EDGE_CURVE ( 'NONE', #264, #10120, #7532, .T. ) ;
#144=CARTESIAN_POINT ( 'NONE',  ( 3.000000000000000888, -19.75591328264893676, 10.87771529938155268 ) ) ;
#145=EDGE_CURVE ( 'NONE', #6788, #7710, #2973, .T. ) ;
#148=EDGE_CURVE ( 'NONE', #2827, #622, #1200, .T. ) ;
#149=LINE ( 'NONE', #3894, #4131 ) ;
#150=ORIENTED_EDGE ( 'NONE', *, *, #11407, .F. ) ;
#151=ORIENTED_EDGE ( 'NONE', *, *, #1050, .T. ) ;
#152=CARTESIAN_POINT ( 'NONE',  ( 0.000000000000000000, -20.65684170206500170, 13.72351598154890873 ) ) ;
#153=DIRECTION ( 'NONE',  ( -1.000000000000000000, -0.000000000000000000, -0.000000000000000000 ) ) ;
#154=ORIENTED_EDGE ( 'NONE', *, *, #10715, .T. ) ;
#155=CIRCLE ( 'NONE', #8572, 24.80000000000000071 ) ;
#156=DIRECTION ( 'NONE',  ( 0.000000000000000000, 0.000000000000000000, -1.000000000000000000 ) ) ;
#157=DIRECTION ( 'NONE',  ( 0.000000000000000000, 0.000000000000000000, 1.000000000000000000 ) ) ;
#158=AXIS2_PLACEMENT_3D ( 'NONE', #8860, #4204, #7932 ) ;
#159=DIRECTION ( 'NONE',  ( -1.000000000000000000, 0.000000000000000000, 0.000000000000000000 ) ) ;
#163=CIRCLE ( 'NONE', #7193, 9.599999999999996092 ) ;
#164=ORIENTED_EDGE ( 'NONE', *, *, #9086, .T. ) ;
#165=ORIENTED_EDGE ( 'NONE', *, *, #3483, .F. ) ;
#168=ORIENTED_EDGE ( 'NONE', *, *, #4197, .F. ) ;
#169=CARTESIAN_POINT ( 'NONE',  ( 3.000000000000000888, 11.79560690673872259, 19.74380051311544193 ) ) ;
#170=EDGE_CURVE ( 'NONE', #8421, #7675, #12083, .T. ) ;
#171=CARTESIAN_POINT ( 'NONE',  ( 3.000000000000000888, 0.000000000000000000, 0.000000000000000000 ) ) ;
#172=ORIENTED_EDGE ( 'NONE', *, *, #10346, .T. ) ;
#173=CIRCLE ( 'NONE', #10738, 9.599999999999997868 ) ;
#174=DIRECTION ( 'NONE',  ( 0.000000000000000000, 0.000000000000000000, -1.000000000000000000 ) ) ;
#175=AXIS2_PLACEMENT_3D ( 'NONE', #4264, #7991, #7881 ) ;
#176=DIRECTION ( 'NONE',  ( 0.000000000000000000, 0.000000000000000000, 1.000000000000000000 ) ) ;
#178=DIRECTION ( 'NONE',  ( 0.000000000000000000, 0.000000000000000000, 1.000000000000000000 ) ) ;
#179=EDGE_CURVE ( 'NONE', #5993, #10077, #7445, .T. ) ;
#180=FACE_BOUND ( 'NONE', #4104, .T. ) ;
#182=EDGE_LOOP ( 'NONE', ( #7159, #6754, #6114, #7604 ) ) ;
#183=DIRECTION ( 'NONE',  ( -1.000000000000000000, -0.000000000000000000, 0.000000000000000000 ) ) ;
#184=ORIENTED_EDGE ( 'NONE', *, *, #4970, .F. ) ;
#187=DIRECTION ( 'NONE',  ( 0.000000000000000000, -0.2079116908177466305, -0.9781476007338082423 ) ) ;
#189=CARTESIAN_POINT ( 'NONE',  ( 3.000000000000000888, -11.67026512804560134, 19.29833442572355651 ) ) ;
#190=DIRECTION ( 'NONE',  ( -1.000000000000000000, 0.000000000000000000, 0.000000000000000000 ) ) ;
#192=DIRECTION ( 'NONE',  ( -1.000000000000000000, -0.000000000000000000, -0.000000000000000000 ) ) ;
#193=CARTESIAN_POINT ( 'NONE',  ( 3.000000000000000888, 0.000000000000000000, 0.000000000000000000 ) ) ;
#194=VECTOR ( 'NONE', #12063, 1000.000000000000000 ) ;
#195=CARTESIAN_POINT ( 'NONE',  ( 0.000000000000000000, 22.90635393027946165, 2.062268319295641472 ) ) ;
#196=ORIENTED_EDGE ( 'NONE', *, *, #179, .F. ) ;
#198=CARTESIAN_POINT ( 'NONE',  ( 0.000000000000000000, 8.753070780933159156, 20.78471918669863427 ) ) ;
#199=ORIENTED_EDGE ( 'NONE', *, *, #8228, .F. ) ;
#200=EDGE_LOOP ( 'NONE', ( #985, #7534, #923, #1511 ) ) ;
#201=FACE_OUTER_BOUND ( 'NONE', #6676, .T. ) ;
#203=AXIS2_PLACEMENT_3D ( 'NONE', #4845, #183, #3931 ) ;
#204=AXIS2_PLACEMENT_3D ( 'NONE', #2867, #1942, #9708 ) ;
#205=CARTESIAN_POINT ( 'NONE',  ( 3.000000000000000888, 3.623565124517108771, 24.53384959170459112 ) ) ;
#207=EDGE_CURVE ( 'NONE', #11877, #10975, #1592, .T. ) ;
#209=CARTESIAN_POINT ( 'NONE',  ( 3.000000000000000888, -18.80635025205178579, 13.23915371906949012 ) ) ;
#210=AXIS2_PLACEMENT_3D ( 'NONE', #11002, #1452, #711 ) ;
#211=ORIENTED_EDGE ( 'NONE', *, *, #11236, .T. ) ;
#214=EDGE_CURVE ( 'NONE', #11471, #12032, #3698, .T. ) ;
#215=VERTEX_POINT ( 'NONE', #5899 ) ;
#216=DIRECTION ( 'NONE',  ( 0.000000000000000000, 0.000000000000000000, 1.000000000000000000 ) ) ;
#217=DIRECTION ( 'NONE',  ( 1.000000000000000000, 0.000000000000000000, 0.000000000000000000 ) ) ;
#218=EDGE_CURVE ( 'NONE', #5509, #9694, #2903, .T. ) ;
#219=VERTEX_POINT ( 'NONE', #319 ) ;
#221=DIRECTION ( 'NONE',  ( -1.000000000000000000, -0.000000000000000000, -0.000000000000000000 ) ) ;
#222=CARTESIAN_POINT ( 'NONE',  ( -10.00000000000000000, 0.000000000000000000, 0.000000000000000000 ) ) ;
#223=VECTOR ( 'NONE', #5078, 1000.000000000000000 ) ;
#224=LINE ( 'NONE', #3968, #11226 ) ;
#226=AXIS2_PLACEMENT_3D ( 'NONE', #2459, #9011, #4118 ) ;
#227=EDGE_CURVE ( 'NONE', #9479, #5646, #2572, .T. ) ;
#228=DIRECTION ( 'NONE',  ( 0.000000000000000000, 0.000000000000000000, 1.000000000000000000 ) ) ;
#229=ORIENTED_EDGE ( 'NONE', *, *, #9164, .T. ) ;
#230=VECTOR ( 'NONE', #10343, 1000.000000000000000 ) ;
#234=AXIS2_PLACEMENT_3D ( 'NONE', #3106, #10445, #9650 ) ;
#235=ORIENTED_EDGE ( 'NONE', *, *, #11407, .T. ) ;
#236=CARTESIAN_POINT ( 'NONE',  ( 3.000000000000000888, -8.753070780933295936, 20.78471918669858098 ) ) ;
#237=DIRECTION ( 'NONE',  ( 0.000000000000000000, 0.4067366430757948237, 0.9135454576426034201 ) ) ;
#238=LINE ( 'NONE', #7709, #6766 ) ;
#240=AXIS2_PLACEMENT_3D ( 'NONE', #2683, #723, #8075 ) ;
#241=DIRECTION ( 'NONE',  ( -1.000000000000000000, 0.000000000000000000, 0.000000000000000000 ) ) ;
#242=EDGE_CURVE ( 'NONE', #1657, #5674, #9219, .T. ) ;
#243=DIRECTION ( 'NONE',  ( -1.000000000000000000, 0.000000000000000000, 0.000000000000000000 ) ) ;
#245=DIRECTION ( 'NONE',  ( -1.000000000000000000, 0.000000000000000000, 0.000000000000000000 ) ) ;
#246=VERTEX_POINT ( 'NONE', #5725 ) ;
#247=ADVANCED_FACE ( 'NONE', ( #4057 ), #3140, .T. ) ;
#248=DIRECTION ( 'NONE',  ( -1.000000000000000000, -0.000000000000000000, -0.000000000000000000 ) ) ;
#249=CARTESIAN_POINT ( 'NONE',  ( -10.00000000000000000, 0.000000000000000000, 0.000000000000000000 ) ) ;
#251=CIRCLE ( 'NONE', #649, 9.599999999999997868 ) ;
#254=AXIS2_PLACEMENT_3D ( 'NONE', #9306, #8459, #3858 ) ;
#255=FACE_OUTER_BOUND ( 'NONE', #5644, .T. ) ;
#256=EDGE_CURVE ( 'NONE', #3896, #6837, #11173, .T. ) ;
#257=FACE_OUTER_BOUND ( 'NONE', #4671, .T. ) ;
#258=DIRECTION ( 'NONE',  ( 0.000000000000000000, 0.000000000000000000, 1.000000000000000000 ) ) ;
#260=VECTOR ( 'NONE', #5503, 1000.000000000000000 ) ;
#261=DIRECTION ( 'NONE',  ( -1.000000000000000000, -0.000000000000000000, -0.000000000000000000 ) ) ;
#263=CYLINDRICAL_SURFACE ( 'NONE', #5092, 24.80000000000000071 ) ;
#264=VERTEX_POINT ( 'NONE', #6627 ) ;
#265=DIRECTION ( 'NONE',  ( 0.000000000000000000, 0.000000000000000000, 1.000000000000000000 ) ) ;
#266=ORIENTED_EDGE ( 'NONE', *, *, #9243, .T. ) ;
#267=ORIENTED_EDGE ( 'NONE', *, *, #11375, .T. ) ;
#268=CIRCLE ( 'NONE', #3992, 24.80000000000000071 ) ;
#269=CARTESIAN_POINT ( 'NONE',  ( 0.000000000000000000, -22.54798042742718422, 0.4575788569251160731 ) ) ;
#271=CARTESIAN_POINT ( 'NONE',  ( 1.500000000000000444, -23.88662356770119644, 6.668524164681547184 ) ) ;
#274=CYLINDRICAL_SURFACE ( 'NONE', #9026, 22.99899999999999878 ) ;
#275=AXIS2_PLACEMENT_3D ( 'NONE', #77, #3821, #7541 ) ;
#276=DIRECTION ( 'NONE',  ( -1.000000000000000000, 0.000000000000000000, 0.000000000000000000 ) ) ;
#277=VERTEX_POINT ( 'NONE', #10360 ) ;
#278=ORIENTED_EDGE ( 'NONE', *, *, #3169, .T. ) ;
#279=DIRECTION ( 'NONE',  ( 0.000000000000000000, 0.000000000000000000, 1.000000000000000000 ) ) ;
#280=CARTESIAN_POINT ( 'NONE',  ( 0.000000000000000000, 0.000000000000000000, 0.000000000000000000 ) ) ;
#282=CIRCLE ( 'NONE', #3035, 22.99899999999999878 ) ;
#283=DIRECTION ( 'NONE',  ( 0.000000000000000000, -0.8090169943749526693, 0.5877852522924661427 ) ) ;
#284=CARTESIAN_POINT ( 'NONE',  ( 0.000000000000000000, -13.23915371906942440, -18.80635025205183197 ) ) ;
#285=ADVANCED_FACE ( 'NONE', ( #2160 ), #1983, .T. ) ;
#287=ADVANCED_FACE ( 'NONE', ( #3086 ), #4921, .T. ) ;
#288=EDGE_CURVE ( 'NONE', #7265, #6939, #10196, .T. ) ;
#289=CARTESIAN_POINT ( 'NONE',  ( 3.000000000000000888, 0.000000000000000000, 0.000000000000000000 ) ) ;
#290=ORIENTED_EDGE ( 'NONE', *, *, #3419, .T. ) ;
#291=ORIENTED_EDGE ( 'NONE', *, *, #1715, .T. ) ;
#294=ORIENTED_EDGE ( 'NONE', *, *, #2175, .F. ) ;
#295=DIRECTION ( 'NONE',  ( -1.000000000000000000, 0.000000000000000000, -0.000000000000000000 ) ) ;
#296=CARTESIAN_POINT ( 'NONE',  ( 0.000000000000000000, -17.31945870441157354, 15.13242714128113775 ) ) ;
#297=LINE ( 'NONE', #4096, #116 ) ;
#298=ORIENTED_EDGE ( 'NONE', *, *, #7745, .F. ) ;
#299=EDGE_CURVE ( 'NONE', #7150, #10349, #8718, .T. ) ;
#300=DIRECTION ( 'NONE',  ( 0.000000000000000000, 0.000000000000000000, 1.000000000000000000 ) ) ;
#301=AXIS2_PLACEMENT_3D ( 'NONE', #4366, #4615, #5408 ) ;
#302=MANIFOLD_SOLID_BREP ( 'Extrude-Thin1', #3949 ) ;
#303=EDGE_CURVE ( 'NONE', #9360, #3895, #826, .T. ) ;
#304=CARTESIAN_POINT ( 'NONE',  ( 3.000000000000000888, 20.41249101028211754, 9.589108953447965433 ) ) ;
#306=ORIENTED_EDGE ( 'NONE', *, *, #3487, .F. ) ;
#307=FACE_OUTER_BOUND ( 'NONE', #8234, .T. ) ;
#308=VERTEX_POINT ( 'NONE', #2045 ) ;
#309=CARTESIAN_POINT ( 'NONE',  ( 3.000000000000000888, 4.135161237383916166, -24.45282072769596482 ) ) ;
#310=ORIENTED_EDGE ( 'NONE', *, *, #6297, .T. ) ;
#311=AXIS2_PLACEMENT_3D ( 'NONE', #3561, #11026, #9176 ) ;
#315=CARTESIAN_POINT ( 'NONE',  ( 3.000000000000000888, 23.24434456306336827, -8.645255683528764834 ) ) ;
#316=FACE_OUTER_BOUND ( 'NONE', #11315, .T. ) ;
#318=CIRCLE ( 'NONE', #8142, 9.599999999999997868 ) ;
#319=CARTESIAN_POINT ( 'NONE',  ( 3.000000000000000888, 13.23915371906980276, -18.80635025205156552 ) ) ;
#320=DIRECTION ( 'NONE',  ( -1.000000000000000000, 0.000000000000000000, 0.000000000000000000 ) ) ;
#322=CARTESIAN_POINT ( 'NONE',  ( 3.000000000000000888, 5.117118920208799437, -22.42251312757874260 ) ) ;
#323=ADVANCED_BREP_SHAPE_REPRESENTATION ( '', ( #302, #8474 ), #6316 ) ;
#324=ORIENTED_EDGE ( 'NONE', *, *, #7929, .F. ) ;
#325=PRODUCT_DEFINITION_SHAPE ( 'NONE', 'NONE',  #10691 ) ;
#326=ORIENTED_EDGE ( 'NONE', *, *, #7918, .T. ) ;
#327=ORIENTED_EDGE ( 'NONE', *, *, #10763, .F. ) ;
#328=CARTESIAN_POINT ( 'NONE',  ( 0.000000000000000000, 21.97702544527757951, 6.779701584702809924 ) ) ;
#330=EDGE_CURVE ( 'NONE', #10333, #8749, #6479, .T. ) ;
#332=DIRECTION ( 'NONE',  ( 0.000000000000000000, 0.2079116908177532086, 0.9781476007338069101 ) ) ;
#335=CARTESIAN_POINT ( 'NONE',  ( 3.000000000000000888, 1.901833551798254973, 22.47229024614977888 ) ) ;
#336=AXIS2_PLACEMENT_3D ( 'NONE', #2470, #6710, #4945 ) ;
#337=ORIENTED_EDGE ( 'NONE', *, *, #10319, .T. ) ;
#338=EDGE_CURVE ( 'NONE', #6397, #4410, #2384, .T. ) ;
#340=ORIENTED_EDGE ( 'NONE', *, *, #11523, .F. ) ;
#341=CARTESIAN_POINT ( 'NONE',  ( 1.499999999999999556, 6.668524164681631561, 23.88662356770117512 ) ) ;
#343=CARTESIAN_POINT ( 'NONE',  ( 3.000000000000000888, -21.30300407174357957, -7.402892494506506438 ) ) ;
#344=VECTOR ( 'NONE', #10356, 1000.000000000000000 ) ;
#346=CARTESIAN_POINT ( 'NONE',  ( -10.00000000000000000, 0.000000000000000000, 0.000000000000000000 ) ) ;
#347=ORIENTED_EDGE ( 'NONE', *, *, #481, .T. ) ;
#348=VERTEX_POINT ( 'NONE', #6979 ) ;
#350=ORIENTED_EDGE ( 'NONE', *, *, #2639, .T. ) ;
#351=VECTOR ( 'NONE', #11431, 1000.000000000000000 ) ;
#353=CARTESIAN_POINT ( 'NONE',  ( 0.000000000000000000, 1.556492618230641556, 24.75110766671652485 ) ) ;
#354=FACE_OUTER_BOUND ( 'NONE', #7228, .T. ) ;
#355=CARTESIAN_POINT ( 'NONE',  ( 0.000000000000000000, -24.45282072769603587, 4.135161237383499611 ) ) ;
#356=ORIENTED_EDGE ( 'NONE', *, *, #1238, .T. ) ;
#357=DIRECTION ( 'NONE',  ( 0.000000000000000000, 0.000000000000000000, 1.000000000000000000 ) ) ;
#358=CARTESIAN_POINT ( 'NONE',  ( 0.000000000000000000, 0.000000000000000000, 0.000000000000000000 ) ) ;
#360=AXIS2_PLACEMENT_3D ( 'NONE', #8241, #708, #9894 ) ;
#362=VECTOR ( 'NONE', #11355, 1000.000000000000000 ) ;
#364=CARTESIAN_POINT ( 'NONE',  ( 0.000000000000000000, 11.02759168516775112, -22.21333432029552668 ) ) ;
#366=DIRECTION ( 'NONE',  ( 0.000000000000000000, 0.000000000000000000, 1.000000000000000000 ) ) ;
#367=ORIENTED_EDGE ( 'NONE', *, *, #6608, .F. ) ;
#368=EDGE_CURVE ( 'NONE', #8212, #1454, #10724, .T. ) ;
#370=EDGE_CURVE ( 'NONE', #4413, #11133, #1604, .T. ) ;
#371=AXIS2_PLACEMENT_3D ( 'NONE', #4586, #7316, #10140 ) ;
#372=CARTESIAN_POINT ( 'NONE',  ( 0.000000000000000000, 4.135161237383582211, 24.45282072769602166 ) ) ;
#373=ADVANCED_FACE ( 'NONE', ( #8027 ), #499, .T. ) ;
#376=DIRECTION ( 'NONE',  ( -1.000000000000000000, 0.000000000000000000, -0.000000000000000000 ) ) ;
#378=DIRECTION ( 'NONE',  ( 0.000000000000000000, 0.8090169943749446757, 0.5877852522924770229 ) ) ;
#380=CIRCLE ( 'NONE', #7211, 9.599999999999997868 ) ;
#381=CARTESIAN_POINT ( 'NONE',  ( 3.000000000000000888, -19.29833442572351743, -11.67026512804567062 ) ) ;
#382=ORIENTED_EDGE ( 'NONE', *, *, #1494, .F. ) ;
#383=DIRECTION ( 'NONE',  ( -1.000000000000000000, 0.000000000000000000, -0.000000000000000000 ) ) ;
#384=VERTEX_POINT ( 'NONE', #4238 ) ;
#385=ORIENTED_EDGE ( 'NONE', *, *, #2810, .T. ) ;
#386=CYLINDRICAL_SURFACE ( 'NONE', #2254, 24.80000000000000071 ) ;
#387=AXIS2_PLACEMENT_3D ( 'NONE', #6705, #11603, #6819 ) ;
#388=CARTESIAN_POINT ( 'NONE',  ( 3.000000000000000888, 13.23915371906980276, -18.80635025205156552 ) ) ;
#390=DIRECTION ( 'NONE',  ( 0.000000000000000000, 0.000000000000000000, 1.000000000000000000 ) ) ;
#392=EDGE_CURVE ( 'NONE', #2895, #2526, #5317, .T. ) ;
#394=DIRECTION ( 'NONE',  ( 0.000000000000000000, 0.000000000000000000, 1.000000000000000000 ) ) ;
#395=FACE_OUTER_BOUND ( 'NONE', #5803, .T. ) ;
#396=EDGE_LOOP ( 'NONE', ( #8402, #10334, #7110, #9558 ) ) ;
#397=ADVANCED_FACE ( 'NONE', ( #6257 ), #7100, .T. ) ;
#398=EDGE_LOOP ( 'NONE', ( #9542, #6481, #3860, #9440 ) ) ;
#399=AXIS2_PLACEMENT_3D ( 'NONE', #1152, #3055, #3114 ) ;
#400=VECTOR ( 'NONE', #4611, 1000.000000000000000 ) ;
#401=VERTEX_POINT ( 'NONE', #1423 ) ;
#402=CARTESIAN_POINT ( 'NONE',  ( 3.000000000000000888, 0.000000000000000000, 0.000000000000000000 ) ) ;
#404=LINE ( 'NONE', #8798, #9929 ) ;
#405=ADVANCED_FACE ( 'NONE', ( #11588 ), #2280, .T. ) ;
#406=AXIS2_PLACEMENT_3D ( 'NONE', #10470, #10347, #9556 ) ;
#407=VECTOR ( 'NONE', #6673, 1000.000000000000000 ) ;
#409=CARTESIAN_POINT ( 'NONE',  ( 0.000000000000000000, 21.30300407174352983, 7.402892494506653875 ) ) ;
#410=ORIENTED_EDGE ( 'NONE', *, *, #9951, .F. ) ;
#411=VERTEX_POINT ( 'NONE', #3260 ) ;
#414=AXIS2_PLACEMENT_3D ( 'NONE', #1180, #192, #2968 ) ;
#415=ORIENTED_EDGE ( 'NONE', *, *, #705, .F. ) ;
#416=AXIS2_PLACEMENT_3D ( 'NONE', #3272, #11655, #4436 ) ;
#417=DIRECTION ( 'NONE',  ( 0.000000000000000000, 0.6691306063588544628, 0.7431448254773976858 ) ) ;
#418=CARTESIAN_POINT ( 'NONE',  ( 1.500000000000000444, -15.80756504416678432, -19.10918332567973721 ) ) ;
#420=CARTESIAN_POINT ( 'NONE',  ( 3.000000000000000888, 18.51065745848395849, -12.88318129270159673 ) ) ;
#421=EDGE_LOOP ( 'NONE', ( #1532, #5869, #9678, #9526 ) ) ;
#422=FACE_OUTER_BOUND ( 'NONE', #7887, .T. ) ;
#423=CYLINDRICAL_SURFACE ( 'NONE', #5915, 9.599999999999997868 ) ;
#425=CIRCLE ( 'NONE', #7256, 9.599999999999997868 ) ;
#427=DIRECTION ( 'NONE',  ( 1.000000000000000000, 0.000000000000000000, 0.000000000000000000 ) ) ;
#428=DIRECTION ( 'NONE',  ( -1.000000000000000000, 0.000000000000000000, 0.000000000000000000 ) ) ;
#429=VERTEX_POINT ( 'NONE', #7852 ) ;
#431=( GEOMETRIC_REPRESENTATION_CONTEXT ( 3 ) GLOBAL_UNCERTAINTY_ASSIGNED_CONTEXT ( ( #7196 ) ) GLOBAL_UNIT_ASSIGNED_CONTEXT ( ( #3634, #3937, #4674 ) ) REPRESENTATION_CONTEXT ( 'NONE', 'WORKASPACE' ) );
#432=ORIENTED_EDGE ( 'NONE', *, *, #9829, .T. ) ;
#433=DIRECTION ( 'NONE',  ( 0.000000000000000000, -0.5877852522924633671, -0.8090169943749546677 ) ) ;
#435=ORIENTED_EDGE ( 'NONE', *, *, #4714, .F. ) ;
#436=AXIS2_PLACEMENT_3D ( 'NONE', #4702, #11192, #1883 ) ;
#437=FACE_OUTER_BOUND ( 'NONE', #11878, .T. ) ;
#438=CARTESIAN_POINT ( 'NONE',  ( 3.000000000000000888, 22.90635393027946165, 2.062268319295641472 ) ) ;
#440=DIRECTION ( 'NONE',  ( -1.000000000000000000, 0.000000000000000000, 0.000000000000000000 ) ) ;
#441=DIRECTION ( 'NONE',  ( 0.000000000000000000, 0.000000000000000000, 1.000000000000000000 ) ) ;
#442=EDGE_CURVE ( 'NONE', #12032, #9479, #5517, .T. ) ;
#443=DIRECTION ( 'NONE',  ( 0.000000000000000000, -0.9135454576425964257, -0.4067366430758104223 ) ) ;
#444=EDGE_CURVE ( 'NONE', #5746, #5082, #6868, .T. ) ;
#445=ADVANCED_FACE ( 'NONE', ( #6142 ), #5277, .T. ) ;
#446=DIRECTION ( 'NONE',  ( 0.000000000000000000, 0.000000000000000000, 1.000000000000000000 ) ) ;
#447=ORIENTED_EDGE ( 'NONE', *, *, #11363, .T. ) ;
#448=AXIS2_PLACEMENT_3D ( 'NONE', #5250, #7314, #11062 ) ;
#449=CIRCLE ( 'NONE', #2608, 24.80000000000000071 ) ;
#450=FACE_OUTER_BOUND ( 'NONE', #3951, .T. ) ;
#453=CARTESIAN_POINT ( 'NONE',  ( 3.000000000000000888, -21.96011696265487600, -5.135568396240250522 ) ) ;
#455=EDGE_CURVE ( 'NONE', #11607, #3718, #7156, .T. ) ;
#457=DIRECTION ( 'NONE',  ( 0.000000000000000000, 0.9945218953682729568, 0.1045284632676570929 ) ) ;
#458=ORIENTED_EDGE ( 'NONE', *, *, #10391, .F. ) ;
#459=ORIENTED_EDGE ( 'NONE', *, *, #4936, .T. ) ;
#460=AXIS2_PLACEMENT_3D ( 'NONE', #4853, #130, #7598 ) ;
#461=ORIENTED_EDGE ( 'NONE', *, *, #10996, .F. ) ;
#463=DIRECTION ( 'NONE',  ( 0.000000000000000000, 0.000000000000000000, -1.000000000000000000 ) ) ;
#464=CARTESIAN_POINT ( 'NONE',  ( 3.000000000000000888, 0.000000000000000000, 0.000000000000000000 ) ) ;
#465=DIRECTION ( 'NONE',  ( 1.000000000000000000, 0.000000000000000000, 0.000000000000000000 ) ) ;
#466=EDGE_CURVE ( 'NONE', #3254, #10253, #9814, .T. ) ;
#467=AXIS2_PLACEMENT_3D ( 'NONE', #3579, #2656, #5467 ) ;
#469=CYLINDRICAL_SURFACE ( 'NONE', #4322, 9.599999999999997868 ) ;
#470=DIRECTION ( 'NONE',  ( 0.000000000000000000, 0.000000000000000000, 1.000000000000000000 ) ) ;
#472=EDGE_LOOP ( 'NONE', ( #11221, #8128, #9957, #11135 ) ) ;
#474=VERTEX_POINT ( 'NONE', #9742 ) ;
#475=AXIS2_PLACEMENT_3D ( 'NONE', #3137, #5034, #6011 ) ;
#476=DIRECTION ( 'NONE',  ( -1.000000000000000000, 0.000000000000000000, -0.000000000000000000 ) ) ;
#477=DIRECTION ( 'NONE',  ( 0.000000000000000000, 0.000000000000000000, -1.000000000000000000 ) ) ;
#480=EDGE_LOOP ( 'NONE', ( #9305, #6355, #6678, #2511 ) ) ;
#481=EDGE_CURVE ( 'NONE', #7424, #4541, #1360, .T. ) ;
#482=DIRECTION ( 'NONE',  ( 0.000000000000000000, 0.000000000000000000, 1.000000000000000000 ) ) ;
#486=LINE ( 'NONE', #7085, #10595 ) ;
#487=ORIENTED_EDGE ( 'NONE', *, *, #7990, .F. ) ;
#488=FACE_OUTER_BOUND ( 'NONE', #6997, .T. ) ;
#489=ADVANCED_FACE ( 'NONE', ( #686 ), #1482, .F. ) ;
#490=VERTEX_POINT ( 'NONE', #11216 ) ;
#492=ORIENTED_EDGE ( 'NONE', *, *, #5461, .F. ) ;
#493=DIRECTION ( 'NONE',  ( 0.000000000000000000, 0.000000000000000000, 1.000000000000000000 ) ) ;
#494=CIRCLE ( 'NONE', #6752, 9.599999999999997868 ) ;
#495=ORIENTED_EDGE ( 'NONE', *, *, #6230, .F. ) ;
#496=DIRECTION ( 'NONE',  ( -1.000000000000000000, -0.000000000000000000, -0.000000000000000000 ) ) ;
#497=DIRECTION ( 'NONE',  ( 0.000000000000000000, 0.000000000000000000, 1.000000000000000000 ) ) ;
#499=CYLINDRICAL_SURFACE ( 'NONE', #3358, 9.599999999999997868 ) ;
#501=DIRECTION ( 'NONE',  ( 0.000000000000000000, 0.000000000000000000, -1.000000000000000000 ) ) ;
#502=AXIS2_PLACEMENT_3D ( 'NONE', #6, #11283, #6621 ) ;
#503=ORIENTED_EDGE ( 'NONE', *, *, #2058, .T. ) ;
#504=CYLINDRICAL_SURFACE ( 'NONE', #8992, 9.599999999999997868 ) ;
#505=VERTEX_POINT ( 'NONE', #1848 ) ;
#507=ORIENTED_EDGE ( 'NONE', *, *, #11003, .T. ) ;
#508=LINE ( 'NONE', #10676, #10897 ) ;
#509=CIRCLE ( 'NONE', #3249, 9.599999999999996092 ) ;
#510=EDGE_CURVE ( 'NONE', #9078, #5271, #30, .T. ) ;
#511=DIRECTION ( 'NONE',  ( -1.000000000000000000, -0.000000000000000000, 0.000000000000000000 ) ) ;
#512=DIRECTION ( 'NONE',  ( -1.000000000000000000, 0.000000000000000000, 0.000000000000000000 ) ) ;
#515=CARTESIAN_POINT ( 'NONE',  ( 0.000000000000000000, 0.000000000000000000, 0.000000000000000000 ) ) ;
#516=CARTESIAN_POINT ( 'NONE',  ( 3.000000000000000888, 0.000000000000000000, 0.000000000000000000 ) ) ;
#517=ADVANCED_FACE ( 'NONE', ( #7468 ), #9254, .T. ) ;
#518=VERTEX_POINT ( 'NONE', #10288 ) ;
#520=ORIENTED_EDGE ( 'NONE', *, *, #9304, .T. ) ;
#521=ADVANCED_FACE ( 'NONE', ( #8150 ), #5453, .T. ) ;
#523=EDGE_CURVE ( 'NONE', #2005, #11061, #9418, .T. ) ;
#524=EDGE_LOOP ( 'NONE', ( #7250, #3552, #2179, #11969 ) ) ;
#525=CARTESIAN_POINT ( 'NONE',  ( 3.000000000000000888, 0.000000000000000000, 0.000000000000000000 ) ) ;
#526=FACE_OUTER_BOUND ( 'NONE', #10762, .T. ) ;
#527=ADVANCED_FACE ( 'NONE', ( #5522 ), #9076, .T. ) ;
#529=DIRECTION ( 'NONE',  ( -1.000000000000000000, 0.000000000000000000, -0.000000000000000000 ) ) ;
#530=CARTESIAN_POINT ( 'NONE',  ( 0.000000000000000000, 22.15038895030654942, -4.240409074143872914 ) ) ;
#531=VERTEX_POINT ( 'NONE', #10047 ) ;
#532=VERTEX_POINT ( 'NONE', #3683 ) ;
#534=ORIENTED_EDGE ( 'NONE', *, *, #6875, .F. ) ;
#535=DIRECTION ( 'NONE',  ( 0.000000000000000000, 0.000000000000000000, 1.000000000000000000 ) ) ;
#536=DIRECTION ( 'NONE',  ( 0.000000000000000000, 0.000000000000000000, 1.000000000000000000 ) ) ;
#537=CARTESIAN_POINT ( 'NONE',  ( 3.000000000000000888, 0.000000000000000000, 0.000000000000000000 ) ) ;
#538=AXIS2_PLACEMENT_3D ( 'NONE', #5653, #6744, #4617 ) ;
#539=FACE_OUTER_BOUND ( 'NONE', #10644, .T. ) ;
#540=ORIENTED_EDGE ( 'NONE', *, *, #9508, .F. ) ;
#544=LINE ( 'NONE', #3302, #6484 ) ;
#545=VECTOR ( 'NONE', #8559, 1000.000000000000000 ) ;
#547=DIRECTION ( 'NONE',  ( -1.000000000000000000, -0.000000000000000000, 0.000000000000000000 ) ) ;
#548=ORIENTED_EDGE ( 'NONE', *, *, #8419, .F. ) ;
#549=EDGE_CURVE ( 'NONE', #5532, #11993, #8278, .T. ) ;
#551=ORIENTED_EDGE ( 'NONE', *, *, #5552, .T. ) ;
#552=FACE_OUTER_BOUND ( 'NONE', #933, .T. ) ;
#554=CARTESIAN_POINT ( 'NONE',  ( 0.000000000000000000, 0.000000000000000000, 0.000000000000000000 ) ) ;
#555=AXIS2_PLACEMENT_3D ( 'NONE', #7557, #6758, #3777 ) ;
#556=EDGE_CURVE ( 'NONE', #5532, #8486, #6878, .T. ) ;
#557=LINE ( 'NONE', #4291, #10055 ) ;
#559=CARTESIAN_POINT ( 'NONE',  ( -10.00000000000000000, 0.000000000000000000, 0.000000000000000000 ) ) ;
#561=DIRECTION ( 'NONE',  ( 0.000000000000000000, 0.000000000000000000, -1.000000000000000000 ) ) ;
#562=ORIENTED_EDGE ( 'NONE', *, *, #3448, .F. ) ;
#563=DIRECTION ( 'NONE',  ( -1.000000000000000000, 0.000000000000000000, 0.000000000000000000 ) ) ;
#564=ORIENTED_EDGE ( 'NONE', *, *, #3143, .T. ) ;
#565=AXIS2_PLACEMENT_3D ( 'NONE', #9349, #4232, #9292 ) ;
#566=CYLINDRICAL_SURFACE ( 'NONE', #2787, 9.599999999999997868 ) ;
#567=CARTESIAN_POINT ( 'NONE',  ( 0.000000000000000000, 9.039786367038837867, 21.14796121233199599 ) ) ;
#568=( NAMED_UNIT ( * ) PLANE_ANGLE_UNIT ( ) SI_UNIT ( $, .RADIAN. ) );
#569=ORIENTED_EDGE ( 'NONE', *, *, #2522, .T. ) ;
#572=CARTESIAN_POINT ( 'NONE',  ( 1.499999999999999556, -23.05871956130116018, -9.128825345753256215 ) ) ;
#573=VECTOR ( 'NONE', #3606, 1000.000000000000000 ) ;
#574=CIRCLE ( 'NONE', #2139, 9.599999999999996092 ) ;
#576=DIRECTION ( 'NONE',  ( 0.000000000000000000, 0.000000000000000000, -1.000000000000000000 ) ) ;
#577=CIRCLE ( 'NONE', #7215, 24.80000000000000071 ) ;
#578=CYLINDRICAL_SURFACE ( 'NONE', #1563, 22.99899999999999878 ) ;
#580=ORIENTED_EDGE ( 'NONE', *, *, #3066, .F. ) ;
#581=ORIENTED_EDGE ( 'NONE', *, *, #7048, .T. ) ;
#583=AXIS2_PLACEMENT_3D ( 'NONE', #10430, #10546, #7858 ) ;
#584=DIRECTION ( 'NONE',  ( 1.000000000000000000, 0.000000000000000000, 0.000000000000000000 ) ) ;
#586=VECTOR ( 'NONE', #10792, 1000.000000000000000 ) ;
#587=EDGE_CURVE ( 'NONE', #8746, #9071, #10601, .T. ) ;
#588=DIRECTION ( 'NONE',  ( -1.000000000000000000, 0.000000000000000000, 0.000000000000000000 ) ) ;
#589=AXIS2_PLACEMENT_3D ( 'NONE', #5331, #1593, #11683 ) ;
#590=EDGE_CURVE ( 'NONE', #10713, #4077, #5327, .T. ) ;
#591=AXIS2_PLACEMENT_3D ( 'NONE', #249, #11578, #11511 ) ;
#592=DIRECTION ( 'NONE',  ( 0.000000000000000000, 0.000000000000000000, 1.000000000000000000 ) ) ;
#593=ORIENTED_EDGE ( 'NONE', *, *, #3174, .F. ) ;
#594=ORIENTED_EDGE ( 'NONE', *, *, #7522, .F. ) ;
#596=EDGE_CURVE ( 'NONE', #6304, #1233, #11190, .T. ) ;
#597=ORIENTED_EDGE ( 'NONE', *, *, #549, .T. ) ;
#598=CARTESIAN_POINT ( 'NONE',  ( 3.000000000000000888, -13.62355943574006645, -17.97274125076088680 ) ) ;
#599=CARTESIAN_POINT ( 'NONE',  ( 0.000000000000000000, 0.000000000000000000, 0.000000000000000000 ) ) ;
#600=CARTESIAN_POINT ( 'NONE',  ( 0.000000000000000000, -6.532525787311115550, 21.58580335785674365 ) ) ;
#601=CIRCLE ( 'NONE', #7436, 9.599999999999997868 ) ;
#602=AXIS2_PLACEMENT_3D ( 'NONE', #7128, #11848, #6169 ) ;
#603=CYLINDRICAL_SURFACE ( 'NONE', #6413, 22.99899999999999878 ) ;
#604=EDGE_LOOP ( 'NONE', ( #8602, #11394, #3338, #9831 ) ) ;
#605=AXIS2_PLACEMENT_3D ( 'NONE', #6063, #1471, #11807 ) ;
#606=DIRECTION ( 'NONE',  ( 1.000000000000000000, 0.000000000000000000, 0.000000000000000000 ) ) ;
#607=CARTESIAN_POINT ( 'NONE',  ( 3.000000000000000888, -24.02068490260608868, -6.168200451486002045 ) ) ;
#609=EDGE_CURVE ( 'NONE', #8357, #2308, #4475, .T. ) ;
#610=DIRECTION ( 'NONE',  ( -1.000000000000000000, 0.000000000000000000, 0.000000000000000000 ) ) ;
#611=AXIS2_PLACEMENT_3D ( 'NONE', #8367, #8434, #12090 ) ;
#612=EDGE_LOOP ( 'NONE', ( #7954, #10758, #1154, #8872 ) ) ;
#613=DIRECTION ( 'NONE',  ( -1.000000000000000000, 0.000000000000000000, 0.000000000000000000 ) ) ;
#614=CIRCLE ( 'NONE', #3942, 9.599999999999996092 ) ;
#615=ORIENTED_EDGE ( 'NONE', *, *, #11895, .F. ) ;
#616=ORIENTED_EDGE ( 'NONE', *, *, #5832, .T. ) ;
#618=ORIENTED_EDGE ( 'NONE', *, *, #5367, .T. ) ;
#620=CARTESIAN_POINT ( 'NONE',  ( -10.00000000000000000, 0.000000000000000000, 0.000000000000000000 ) ) ;
#622=VERTEX_POINT ( 'NONE', #7936 ) ;
#623=DIRECTION ( 'NONE',  ( -1.000000000000000000, -0.000000000000000000, 0.000000000000000000 ) ) ;
#624=DIRECTION ( 'NONE',  ( 1.000000000000000000, -0.000000000000000000, -0.000000000000000000 ) ) ;
#626=EDGE_CURVE ( 'NONE', #8343, #518, #3071, .T. ) ;
#627=DIRECTION ( 'NONE',  ( -1.000000000000000000, 0.000000000000000000, -0.000000000000000000 ) ) ;
#629=CARTESIAN_POINT ( 'NONE',  ( 3.000000000000000888, 13.79477846460820700, -18.40266524480574972 ) ) ;
#630=DIRECTION ( 'NONE',  ( -1.000000000000000000, -0.000000000000000000, -0.000000000000000000 ) ) ;
#631=AXIS2_PLACEMENT_3D ( 'NONE', #10969, #3625, #3568 ) ;
#632=EDGE_LOOP ( 'NONE', ( #7025, #6641, #7576, #734 ) ) ;
#633=EDGE_CURVE ( 'NONE', #1751, #5065, #1965, .T. ) ;
#634=LINE ( 'NONE', #10859, #8056 ) ;
#635=DIRECTION ( 'NONE',  ( 0.000000000000000000, 0.000000000000000000, 1.000000000000000000 ) ) ;
#636=EDGE_LOOP ( 'NONE', ( #11452, #11857, #7283, #1512 ) ) ;
#637=CARTESIAN_POINT ( 'NONE',  ( 3.000000000000000888, 11.79560690673872259, 19.74380051311544193 ) ) ;
#638=CARTESIAN_POINT ( 'NONE',  ( 0.000000000000000000, -5.135568396239877487, -21.96011696265496838 ) ) ;
#639=LINE ( 'NONE', #9139, #6527 ) ;
#644=AXIS2_PLACEMENT_3D ( 'NONE', #7358, #6569, #7420 ) ;
#645=EDGE_LOOP ( 'NONE', ( #4129, #6737, #551, #9664 ) ) ;
#646=ORIENTED_EDGE ( 'NONE', *, *, #6981, .F. ) ;
#648=ORIENTED_EDGE ( 'NONE', *, *, #11063, .T. ) ;
#649=AXIS2_PLACEMENT_3D ( 'NONE', #4290, #10847, #1716 ) ;
#651=AXIS2_PLACEMENT_3D ( 'NONE', #598, #6300, #8928 ) ;
#652=DIRECTION ( 'NONE',  ( 0.000000000000000000, 0.000000000000000000, 1.000000000000000000 ) ) ;
#653=CIRCLE ( 'NONE', #10623, 22.99899999999999878 ) ;
#656=CIRCLE ( 'NONE', #2616, 9.599999999999997868 ) ;
#657=CARTESIAN_POINT ( 'NONE',  ( 0.000000000000000000, -15.40502424595158359, 19.43515443678397503 ) ) ;
#658=DIRECTION ( 'NONE',  ( -1.000000000000000000, 0.000000000000000000, 0.000000000000000000 ) ) ;
#660=ORIENTED_EDGE ( 'NONE', *, *, #392, .F. ) ;
#662=VERTEX_POINT ( 'NONE', #2144 ) ;
#664=DIRECTION ( 'NONE',  ( -1.000000000000000000, 0.000000000000000000, 0.000000000000000000 ) ) ;
#665=CIRCLE ( 'NONE', #8686, 22.99900000000000233 ) ;
#666=DIRECTION ( 'NONE',  ( -1.000000000000000000, 0.000000000000000000, 0.000000000000000000 ) ) ;
#667=ORIENTED_EDGE ( 'NONE', *, *, #4953, .F. ) ;
#669=EDGE_CURVE ( 'NONE', #11061, #8500, #8522, .T. ) ;
#670=DIRECTION ( 'NONE',  ( -1.000000000000000000, 0.000000000000000000, 0.000000000000000000 ) ) ;
#672=DIRECTION ( 'NONE',  ( -1.000000000000000000, -0.000000000000000000, 0.000000000000000000 ) ) ;
#673=AXIS2_PLACEMENT_3D ( 'NONE', #11695, #4235, #4054 ) ;
#674=CARTESIAN_POINT ( 'NONE',  ( 3.000000000000000888, -2.811977935937933104, 22.37663021667342989 ) ) ;
#675=ORIENTED_EDGE ( 'NONE', *, *, #143, .F. ) ;
#676=ORIENTED_EDGE ( 'NONE', *, *, #5843, .F. ) ;
#678=ADVANCED_FACE ( 'NONE', ( #5823 ), #3283, .T. ) ;
#679=VERTEX_POINT ( 'NONE', #5641 ) ;
#680=CARTESIAN_POINT ( 'NONE',  ( 0.000000000000000000, 3.623565124517105218, 24.53384959170458757 ) ) ;
#681=ORIENTED_EDGE ( 'NONE', *, *, #9202, .T. ) ;
#683=DIRECTION ( 'NONE',  ( 1.000000000000000000, 0.000000000000000000, 0.000000000000000000 ) ) ;
#684=DIRECTION ( 'NONE',  ( 0.000000000000000000, 0.000000000000000000, 1.000000000000000000 ) ) ;
#686=FACE_OUTER_BOUND ( 'NONE', #5474, .T. ) ;
#687=DIRECTION ( 'NONE',  ( -1.000000000000000000, 0.000000000000000000, -0.000000000000000000 ) ) ;
#688=ORIENTED_EDGE ( 'NONE', *, *, #6545, .T. ) ;
#689=DIRECTION ( 'NONE',  ( 0.000000000000000000, 0.000000000000000000, -1.000000000000000000 ) ) ;
#690=ORIENTED_EDGE ( 'NONE', *, *, #8658, .T. ) ;
#691=CIRCLE ( 'NONE', #11447, 9.599999999999997868 ) ;
#693=DIRECTION ( 'NONE',  ( -1.000000000000000000, -0.000000000000000000, -0.000000000000000000 ) ) ;
#695=ORIENTED_EDGE ( 'NONE', *, *, #11382, .T. ) ;
#696=CARTESIAN_POINT ( 'NONE',  ( 3.000000000000000888, 14.74749645580034496, -17.06259499759930165 ) ) ;
#697=DIRECTION ( 'NONE',  ( -1.000000000000000000, -0.000000000000000000, 0.000000000000000000 ) ) ;
#700=CARTESIAN_POINT ( 'NONE',  ( 0.000000000000000000, 5.117118920208487687, 22.42251312757881365 ) ) ;
#701=CARTESIAN_POINT ( 'NONE',  ( 3.000000000000000888, -9.667200211209685534, -20.86861857134744014 ) ) ;
#702=ORIENTED_EDGE ( 'NONE', *, *, #8462, .F. ) ;
#703=ORIENTED_EDGE ( 'NONE', *, *, #7091, .F. ) ;
#705=EDGE_CURVE ( 'NONE', #1245, #3019, #4343, .T. ) ;
#707=CARTESIAN_POINT ( 'NONE',  ( 3.000000000000000888, -20.86861857134728027, -9.667200211210033700 ) ) ;
#708=DIRECTION ( 'NONE',  ( -1.000000000000000000, 0.000000000000000000, 0.000000000000000000 ) ) ;
#709=EDGE_CURVE ( 'NONE', #4686, #9990, #8581, .T. ) ;
#711=DIRECTION ( 'NONE',  ( 0.000000000000000000, 0.000000000000000000, 1.000000000000000000 ) ) ;
#712=VERTEX_POINT ( 'NONE', #11451 ) ;
#714=DIRECTION ( 'NONE',  ( -1.000000000000000000, 0.000000000000000000, 0.000000000000000000 ) ) ;
#715=EDGE_LOOP ( 'NONE', ( #1395, #7130, #2723, #8615 ) ) ;
#716=ORIENTED_EDGE ( 'NONE', *, *, #455, .T. ) ;
#717=ORIENTED_EDGE ( 'NONE', *, *, #10247, .F. ) ;
#718=DIRECTION ( 'NONE',  ( -1.000000000000000000, 0.000000000000000000, 0.000000000000000000 ) ) ;
#719=DIRECTION ( 'NONE',  ( -1.000000000000000000, -0.000000000000000000, -0.000000000000000000 ) ) ;
#721=CARTESIAN_POINT ( 'NONE',  ( 3.000000000000000888, 10.87771529938162196, 19.75591328264889768 ) ) ;
#722=DIRECTION ( 'NONE',  ( 1.000000000000000000, 0.000000000000000000, 0.000000000000000000 ) ) ;
#723=DIRECTION ( 'NONE',  ( -1.000000000000000000, 0.000000000000000000, 0.000000000000000000 ) ) ;
#725=CARTESIAN_POINT ( 'NONE',  ( 0.000000000000000000, -14.74749645579999857, -17.06259499759959297 ) ) ;
#726=AXIS2_PLACEMENT_3D ( 'NONE', #5849, #9637, #2109 ) ;
#727=CARTESIAN_POINT ( 'NONE',  ( 3.000000000000000888, 0.000000000000000000, 0.000000000000000000 ) ) ;
#728=ORIENTED_EDGE ( 'NONE', *, *, #4002, .F. ) ;
#729=AXIS2_PLACEMENT_3D ( 'NONE', #1436, #9880, #8848 ) ;
#730=VERTEX_POINT ( 'NONE', #7530 ) ;
#732=ORIENTED_EDGE ( 'NONE', *, *, #5614, .F. ) ;
#733=CARTESIAN_POINT ( 'NONE',  ( 3.000000000000000888, 17.06259499759944021, 14.74749645580017088 ) ) ;
#734=ORIENTED_EDGE ( 'NONE', *, *, #1836, .T. ) ;
#735=ADVANCED_FACE ( 'NONE', ( #8866 ), #469, .T. ) ;
#736=CYLINDRICAL_SURFACE ( 'NONE', #9441, 9.599999999999997868 ) ;
#738=DIRECTION ( 'NONE',  ( 0.000000000000000000, 0.000000000000000000, 1.000000000000000000 ) ) ;
#740=CIRCLE ( 'NONE', #10111, 9.599999999999996092 ) ;
#741=DIRECTION ( 'NONE',  ( 0.000000000000000000, 0.5877852522924690293, 0.8090169943749504489 ) ) ;
#743=LINE ( 'NONE', #3570, #11739 ) ;
#744=ORIENTED_EDGE ( 'NONE', *, *, #10443, .F. ) ;
#745=DIRECTION ( 'NONE',  ( -1.000000000000000000, -0.000000000000000000, -0.000000000000000000 ) ) ;
#747=ORIENTED_EDGE ( 'NONE', *, *, #11296, .F. ) ;
#748=EDGE_CURVE ( 'NONE', #3296, #4404, #2888, .T. ) ;
#751=CARTESIAN_POINT ( 'NONE',  ( 0.000000000000000000, 8.753070780933430939, -20.78471918669851703 ) ) ;
#753=ORIENTED_EDGE ( 'NONE', *, *, #3793, .T. ) ;
#754=DIRECTION ( 'NONE',  ( -1.000000000000000000, -0.000000000000000000, 0.000000000000000000 ) ) ;
#755=DIRECTION ( 'NONE',  ( 1.000000000000000000, -0.000000000000000000, -0.000000000000000000 ) ) ;
#758=DIRECTION ( 'NONE',  ( 0.000000000000000000, 0.000000000000000000, 1.000000000000000000 ) ) ;
#759=CIRCLE ( 'NONE', #7793, 22.99900000000000233 ) ;
#760=CARTESIAN_POINT ( 'NONE',  ( 3.000000000000000888, 19.74380051311556628, -11.79560690673851475 ) ) ;
#764=AXIS2_PLACEMENT_3D ( 'NONE', #9528, #11253, #7566 ) ;
#765=CIRCLE ( 'NONE', #11129, 9.599999999999996092 ) ;
#767=EDGE_CURVE ( 'NONE', #7710, #10871, #9435, .T. ) ;
#768=DIRECTION ( 'NONE',  ( 0.000000000000000000, 0.000000000000000000, 1.000000000000000000 ) ) ;
#769=CIRCLE ( 'NONE', #6825, 24.80000000000000071 ) ;
#771=EDGE_CURVE ( 'NONE', #4202, #11830, #11175, .T. ) ;
#772=LINE ( 'NONE', #3352, #10188 ) ;
#774=CARTESIAN_POINT ( 'NONE',  ( 3.000000000000000888, -5.135568396239877487, -21.96011696265496838 ) ) ;
#775=ORIENTED_EDGE ( 'NONE', *, *, #5689, .F. ) ;
#776=AXIS2_PLACEMENT_3D ( 'NONE', #9692, #4925, #7791 ) ;
#777=ORIENTED_EDGE ( 'NONE', *, *, #11884, .F. ) ;
#778=CARTESIAN_POINT ( 'NONE',  ( 3.000000000000000888, 17.71842311621530541, 17.35216073792446778 ) ) ;
#779=CARTESIAN_POINT ( 'NONE',  ( 3.000000000000000888, 9.128825345753341480, -23.05871956130113176 ) ) ;
#780=ADVANCED_FACE ( 'NONE', ( #10410 ), #2028, .T. ) ;
#782=CIRCLE ( 'NONE', #7616, 9.599999999999997868 ) ;
#784=CARTESIAN_POINT ( 'NONE',  ( 3.000000000000000888, -22.90635393027947941, 2.062268319295487817 ) ) ;
#785=DIRECTION ( 'NONE',  ( 0.000000000000000000, 0.8090169943749486725, -0.5877852522924714718 ) ) ;
#788=ORIENTED_EDGE ( 'NONE', *, *, #8191, .F. ) ;
#789=DIRECTION ( 'NONE',  ( -1.000000000000000000, 0.000000000000000000, 0.000000000000000000 ) ) ;
#790=VECTOR ( 'NONE', #5279, 1000.000000000000000 ) ;
#791=ORIENTED_EDGE ( 'NONE', *, *, #8074, .F. ) ;
#792=ORIENTED_EDGE ( 'NONE', *, *, #8917, .F. ) ;
#793=VECTOR ( 'NONE', #10087, 1000.000000000000000 ) ;
#795=VECTOR ( 'NONE', #10033, 1000.000000000000000 ) ;
#796=CIRCLE ( 'NONE', #4317, 22.99900000000000233 ) ;
#797=ORIENTED_EDGE ( 'NONE', *, *, #242, .T. ) ;
#798=CARTESIAN_POINT ( 'NONE',  ( 3.000000000000000888, -6.779701584702886308, 21.97702544527755109 ) ) ;
#800=ORIENTED_EDGE ( 'NONE', *, *, #8832, .F. ) ;
#801=CARTESIAN_POINT ( 'NONE',  ( 3.000000000000000888, -11.79560690673858403, -19.74380051311552364 ) ) ;
#802=FACE_OUTER_BOUND ( 'NONE', #2919, .T. ) ;
#804=AXIS2_PLACEMENT_3D ( 'NONE', #10853, #7966, #443 ) ;
#805=DIRECTION ( 'NONE',  ( -1.000000000000000000, 0.000000000000000000, 0.000000000000000000 ) ) ;
#806=CIRCLE ( 'NONE', #2015, 9.599999999999997868 ) ;
#807=AXIS2_PLACEMENT_3D ( 'NONE', #10687, #5057, #2244 ) ;
#808=CYLINDRICAL_SURFACE ( 'NONE', #8433, 24.80000000000000071 ) ;
#810=ORIENTED_EDGE ( 'NONE', *, *, #4224, .T. ) ;
#811=DIRECTION ( 'NONE',  ( 0.000000000000000000, 0.000000000000000000, 1.000000000000000000 ) ) ;
#812=ORIENTED_EDGE ( 'NONE', *, *, #4126, .T. ) ;
#815=FACE_OUTER_BOUND ( 'NONE', #4398, .T. ) ;
#816=FILL_AREA_STYLE_COLOUR ( '', #8664 ) ;
#817=AXIS2_PLACEMENT_3D ( 'NONE', #515, #10063, #9091 ) ;
#818=CARTESIAN_POINT ( 'NONE',  ( 0.000000000000000000, 13.28910708463157420, -20.93895013827567553 ) ) ;
#819=EDGE_CURVE ( 'NONE', #11808, #6397, #9010, .T. ) ;
#821=FACE_OUTER_BOUND ( 'NONE', #6585, .T. ) ;
#823=EDGE_CURVE ( 'NONE', #916, #8820, #10378, .T. ) ;
#824=CARTESIAN_POINT ( 'NONE',  ( 3.000000000000000888, 0.000000000000000000, 0.000000000000000000 ) ) ;
#826=CIRCLE ( 'NONE', #5120, 9.599999999999997868 ) ;
#827=DIRECTION ( 'NONE',  ( 0.000000000000000000, -0.8660254037844328234, -0.5000000000000101030 ) ) ;
#828=CIRCLE ( 'NONE', #8846, 22.99899999999999523 ) ;
#829=ORIENTED_EDGE ( 'NONE', *, *, #10768, .F. ) ;
#830=ORIENTED_EDGE ( 'NONE', *, *, #1712, .T. ) ;
#835=CARTESIAN_POINT ( 'NONE',  ( 0.000000000000000000, 23.88662356770115380, 6.668524164681710609 ) ) ;
#836=DIRECTION ( 'NONE',  ( -1.000000000000000000, 0.000000000000000000, 0.000000000000000000 ) ) ;
#837=EDGE_CURVE ( 'NONE', #5148, #6438, #9793, .T. ) ;
#839=DIRECTION ( 'NONE',  ( -1.000000000000000000, 0.000000000000000000, 0.000000000000000000 ) ) ;
#840=FACE_OUTER_BOUND ( 'NONE', #7883, .T. ) ;
#841=ORIENTED_EDGE ( 'NONE', *, *, #3703, .F. ) ;
#842=SHAPE_REPRESENTATION ( 'spring holder_ISO - Spur gear 0.8M 60T 20PA 3FW ---S60A75H50L8.0N', ( #8474 ), #6316 ) ;
#844=AXIS2_PLACEMENT_3D ( 'NONE', #3010, #8755, #300 ) ;
#845=VERTEX_POINT ( 'NONE', #7187 ) ;
#846=EDGE_CURVE ( 'NONE', #474, #5072, #8122, .T. ) ;
#847=ORIENTED_EDGE ( 'NONE', *, *, #4792, .T. ) ;
#848=FACE_OUTER_BOUND ( 'NONE', #10159, .T. ) ;
#849=CARTESIAN_POINT ( 'NONE',  ( 3.000000000000000888, 19.10918332567957734, 15.80756504416697084 ) ) ;
#850=CARTESIAN_POINT ( 'NONE',  ( 3.000000000000000888, -22.47229024614978599, 1.901833551798177036 ) ) ;
#851=EDGE_CURVE ( 'NONE', #5379, #4686, #8435, .T. ) ;
#853=DIRECTION ( 'NONE',  ( 0.000000000000000000, 0.000000000000000000, -1.000000000000000000 ) ) ;
#854=AXIS2_PLACEMENT_3D ( 'NONE', #4707, #8379, #12098 ) ;
#855=CYLINDRICAL_SURFACE ( 'NONE', #10629, 22.99899999999999878 ) ;
#858=CARTESIAN_POINT ( 'NONE',  ( 0.000000000000000000, 0.000000000000000000, 0.000000000000000000 ) ) ;
#859=ORIENTED_EDGE ( 'NONE', *, *, #1247, .T. ) ;
#860=ORIENTED_EDGE ( 'NONE', *, *, #3665, .T. ) ;
#861=DIRECTION ( 'NONE',  ( 0.000000000000000000, 0.000000000000000000, 1.000000000000000000 ) ) ;
#862=VERTEX_POINT ( 'NONE', #11792 ) ;
#863=AXIS2_PLACEMENT_3D ( 'NONE', #11432, #2290, #6026 ) ;
#864=ORIENTED_EDGE ( 'NONE', *, *, #8239, .F. ) ;
#866=EDGE_CURVE ( 'NONE', #12050, #1364, #7044, .T. ) ;
#867=ORIENTED_EDGE ( 'NONE', *, *, #7879, .F. ) ;
#868=DIRECTION ( 'NONE',  ( -1.000000000000000000, -0.000000000000000000, -0.000000000000000000 ) ) ;
#869=ORIENTED_EDGE ( 'NONE', *, *, #875, .F. ) ;
#871=CARTESIAN_POINT ( 'NONE',  ( 3.000000000000000888, 6.779701584703024864, -21.97702544527750845 ) ) ;
#873=CIRCLE ( 'NONE', #10645, 9.599999999999999645 ) ;
#874=CARTESIAN_POINT ( 'NONE',  ( 0.000000000000000000, 19.29833442572359559, 11.67026512804553562 ) ) ;
#875=EDGE_CURVE ( 'NONE', #9575, #2975, #1571, .T. ) ;
#877=ORIENTED_EDGE ( 'NONE', *, *, #6147, .F. ) ;
#878=DIRECTION ( 'NONE',  ( 0.000000000000000000, 0.000000000000000000, 1.000000000000000000 ) ) ;
#879=ORIENTED_EDGE ( 'NONE', *, *, #1369, .T. ) ;
#881=VECTOR ( 'NONE', #10966, 1000.000000000000000 ) ;
#882=CARTESIAN_POINT ( 'NONE',  ( 0.000000000000000000, 0.000000000000000000, 0.000000000000000000 ) ) ;
#883=CARTESIAN_POINT ( 'NONE',  ( 0.000000000000000000, -13.72351598154883412, -20.65684170206505499 ) ) ;
#884=DIRECTION ( 'NONE',  ( -1.000000000000000000, 0.000000000000000000, 0.000000000000000000 ) ) ;
#887=DIRECTION ( 'NONE',  ( 0.000000000000000000, 0.000000000000000000, 1.000000000000000000 ) ) ;
#888=CYLINDRICAL_SURFACE ( 'NONE', #5681, 9.599999999999997868 ) ;
#889=ORIENTED_EDGE ( 'NONE', *, *, #4726, .F. ) ;
#891=DIRECTION ( 'NONE',  ( 0.000000000000000000, 0.000000000000000000, 1.000000000000000000 ) ) ;
#893=EDGE_CURVE ( 'NONE', #3541, #5364, #1781, .T. ) ;
#895=DIRECTION ( 'NONE',  ( -1.000000000000000000, 0.000000000000000000, -0.000000000000000000 ) ) ;
#896=AXIS2_PLACEMENT_3D ( 'NONE', #8956, #11648, #6204 ) ;
#898=LINE ( 'NONE', #3781, #9632 ) ;
#899=DIRECTION ( 'NONE',  ( -1.000000000000000000, -0.000000000000000000, -0.000000000000000000 ) ) ;
#900=VERTEX_POINT ( 'NONE', #657 ) ;
#901=EDGE_CURVE ( 'NONE', #8749, #1851, #10773, .T. ) ;
#902=ORIENTED_EDGE ( 'NONE', *, *, #11966, .T. ) ;
#903=AXIS2_PLACEMENT_3D ( 'NONE', #9864, #10603, #1475 ) ;
#904=EDGE_CURVE ( 'NONE', #12019, #9943, #4262, .T. ) ;
#905=ORIENTED_EDGE ( 'NONE', *, *, #7737, .T. ) ;
#906=CARTESIAN_POINT ( 'NONE',  ( 0.000000000000000000, 11.48910920600683738, 21.97817939804043874 ) ) ;
#907=ADVANCED_FACE ( 'NONE', ( #6291 ), #9842, .T. ) ;
#908=CARTESIAN_POINT ( 'NONE',  ( 0.000000000000000000, -22.15038895030651744, 4.240409074144028345 ) ) ;
#909=FACE_OUTER_BOUND ( 'NONE', #10096, .T. ) ;
#911=DIRECTION ( 'NONE',  ( 0.000000000000000000, 0.000000000000000000, 1.000000000000000000 ) ) ;
#912=CIRCLE ( 'NONE', #11650, 22.99899999999999878 ) ;
#915=DIRECTION ( 'NONE',  ( 0.000000000000000000, -0.2079116908177665313, 0.9781476007338041345 ) ) ;
#916=VERTEX_POINT ( 'NONE', #8921 ) ;
#918=LINE ( 'NONE', #3732, #2567 ) ;
#919=ORIENTED_EDGE ( 'NONE', *, *, #6762, .T. ) ;
#920=ORIENTED_EDGE ( 'NONE', *, *, #8530, .T. ) ;
#921=DIRECTION ( 'NONE',  ( 1.000000000000000000, -0.000000000000000000, -0.000000000000000000 ) ) ;
#922=LINE ( 'NONE', #115, #11269 ) ;
#923=ORIENTED_EDGE ( 'NONE', *, *, #3474, .T. ) ;
#924=CARTESIAN_POINT ( 'NONE',  ( 3.000000000000000888, -17.31945870441136748, -15.13242714128137401 ) ) ;
#925=CARTESIAN_POINT ( 'NONE',  ( 3.000000000000000888, 22.99643626497956816, 0.3433949777332492848 ) ) ;
#928=ADVANCED_FACE ( 'NONE', ( #1638 ), #7989, .T. ) ;
#929=DIRECTION ( 'NONE',  ( 0.000000000000000000, 0.000000000000000000, 1.000000000000000000 ) ) ;
#930=AXIS2_PLACEMENT_3D ( 'NONE', #696, #10058, #4429 ) ;
#931=DIRECTION ( 'NONE',  ( 0.000000000000000000, 0.000000000000000000, 1.000000000000000000 ) ) ;
#932=ORIENTED_EDGE ( 'NONE', *, *, #5174, .F. ) ;
#933=EDGE_LOOP ( 'NONE', ( #6969, #1544, #1044, #3210 ) ) ;
#934=DIRECTION ( 'NONE',  ( -1.000000000000000000, 0.000000000000000000, -0.000000000000000000 ) ) ;
#935=ORIENTED_EDGE ( 'NONE', *, *, #4758, .F. ) ;
#938=EDGE_CURVE ( 'NONE', #3221, #10872, #2617, .T. ) ;
#939=VECTOR ( 'NONE', #11932, 1000.000000000000000 ) ;
#940=DIRECTION ( 'NONE',  ( 0.000000000000000000, -0.9781476007338079093, 0.2079116908177492118 ) ) ;
#941=CARTESIAN_POINT ( 'NONE',  ( 0.000000000000000000, -24.75110766671651064, -1.556492618230893132 ) ) ;
#944=DIRECTION ( 'NONE',  ( -1.000000000000000000, 0.000000000000000000, 0.000000000000000000 ) ) ;
#946=ORIENTED_EDGE ( 'NONE', *, *, #10281, .F. ) ;
#947=ORIENTED_EDGE ( 'NONE', *, *, #9579, .T. ) ;
#948=VECTOR ( 'NONE', #3473, 1000.000000000000000 ) ;
#950=DIRECTION ( 'NONE',  ( -1.000000000000000000, -0.000000000000000000, -0.000000000000000000 ) ) ;
#952=CARTESIAN_POINT ( 'NONE',  ( 3.000000000000000888, 0.000000000000000000, 0.000000000000000000 ) ) ;
#953=DIRECTION ( 'NONE',  ( -1.000000000000000000, -0.000000000000000000, -0.000000000000000000 ) ) ;
#954=DIRECTION ( 'NONE',  ( 1.000000000000000000, -0.000000000000000000, -0.000000000000000000 ) ) ;
#956=VECTOR ( 'NONE', #8634, 1000.000000000000000 ) ;
#957=CIRCLE ( 'NONE', #12088, 9.599999999999997868 ) ;
#958=DIRECTION ( 'NONE',  ( -1.000000000000000000, 0.000000000000000000, 0.000000000000000000 ) ) ;
#959=DIRECTION ( 'NONE',  ( 0.000000000000000000, 0.000000000000000000, 1.000000000000000000 ) ) ;
#960=ORIENTED_EDGE ( 'NONE', *, *, #11369, .T. ) ;
#961=ORIENTED_EDGE ( 'NONE', *, *, #8693, .T. ) ;
#962=VERTEX_POINT ( 'NONE', #4446 ) ;
#963=CYLINDRICAL_SURFACE ( 'NONE', #7869, 22.99899999999999878 ) ;
#964=CIRCLE ( 'NONE', #9169, 9.599999999999999645 ) ;
#965=DIRECTION ( 'NONE',  ( 0.000000000000000000, 0.000000000000000000, -1.000000000000000000 ) ) ;
#966=CARTESIAN_POINT ( 'NONE',  ( 0.000000000000000000, 0.000000000000000000, 0.000000000000000000 ) ) ;
#968=DIRECTION ( 'NONE',  ( -1.000000000000000000, 0.000000000000000000, -0.000000000000000000 ) ) ;
#969=EDGE_CURVE ( 'NONE', #10167, #9669, #6852, .T. ) ;
#973=EDGE_CURVE ( 'NONE', #6153, #9363, #772, .T. ) ;
#974=AXIS2_PLACEMENT_3D ( 'NONE', #409, #2251, #3422 ) ;
#975=DIRECTION ( 'NONE',  ( -1.000000000000000000, 0.000000000000000000, 0.000000000000000000 ) ) ;
#976=DIRECTION ( 'NONE',  ( -1.000000000000000000, 0.000000000000000000, 0.000000000000000000 ) ) ;
#977=ORIENTED_EDGE ( 'NONE', *, *, #8799, .T. ) ;
#978=ORIENTED_EDGE ( 'NONE', *, *, #5853, .F. ) ;
#979=CARTESIAN_POINT ( 'NONE',  ( 3.000000000000000888, -15.80756504416703656, 19.10918332567952760 ) ) ;
#980=ORIENTED_EDGE ( 'NONE', *, *, #11817, .F. ) ;
#981=ORIENTED_EDGE ( 'NONE', *, *, #6687, .F. ) ;
#982=CYLINDRICAL_SURFACE ( 'NONE', #5934, 22.99899999999999878 ) ;
#983=AXIS2_PLACEMENT_3D ( 'NONE', #8047, #5176, #8111 ) ;
#984=DIRECTION ( 'NONE',  ( 0.000000000000000000, 0.9781476007338062439, -0.2079116908177564282 ) ) ;
#985=ORIENTED_EDGE ( 'NONE', *, *, #2427, .T. ) ;
#986=ADVANCED_FACE ( 'NONE', ( #10821 ), #2430, .T. ) ;
#988=FACE_OUTER_BOUND ( 'NONE', #10135, .T. ) ;
#991=CARTESIAN_POINT ( 'NONE',  ( -10.00000000000000000, 0.000000000000000000, 0.000000000000000000 ) ) ;
#992=VERTEX_POINT ( 'NONE', #8059 ) ;
#994=VERTEX_POINT ( 'NONE', #10262 ) ;
#995=DIRECTION ( 'NONE',  ( 0.000000000000000000, 0.000000000000000000, 1.000000000000000000 ) ) ;
#996=AXIS2_PLACEMENT_3D ( 'NONE', #9018, #2467, #4298 ) ;
#997=ORIENTED_EDGE ( 'NONE', *, *, #4678, .F. ) ;
#998=EDGE_CURVE ( 'NONE', #11794, #6550, #10968, .T. ) ;
#1000=FACE_OUTER_BOUND ( 'NONE', #6266, .T. ) ;
#1002=VECTOR ( 'NONE', #4734, 1000.000000000000000 ) ;
#1003=EDGE_CURVE ( 'NONE', #9081, #662, #11301, .T. ) ;
#1004=CARTESIAN_POINT ( 'NONE',  ( 3.000000000000000888, -11.79560690673858403, -19.74380051311552364 ) ) ;
#1005=CIRCLE ( 'NONE', #7838, 9.599999999999997868 ) ;
#1006=CIRCLE ( 'NONE', #5301, 22.99900000000000233 ) ;
#1007=CYLINDRICAL_SURFACE ( 'NONE', #11040, 24.80000000000000071 ) ;
#1010=DIRECTION ( 'NONE',  ( 0.000000000000000000, 0.5000000000000011102, -0.8660254037844381525 ) ) ;
#1011=DIRECTION ( 'NONE',  ( 0.000000000000000000, 0.000000000000000000, 1.000000000000000000 ) ) ;
#1012=DIRECTION ( 'NONE',  ( 0.000000000000000000, 0.4067366430757948237, 0.9135454576426034201 ) ) ;
#1013=VERTEX_POINT ( 'NONE', #10377 ) ;
#1014=ADVANCED_FACE ( 'NONE', ( #840 ), #8307, .T. ) ;
#1015=DIRECTION ( 'NONE',  ( 0.000000000000000000, 0.000000000000000000, 1.000000000000000000 ) ) ;
#1017=VECTOR ( 'NONE', #3468, 1000.000000000000000 ) ;
#1018=AXIS2_PLACEMENT_3D ( 'NONE', #3797, #10330, #10625 ) ;
#1019=ORIENTED_EDGE ( 'NONE', *, *, #938, .T. ) ;
#1022=DIRECTION ( 'NONE',  ( -1.000000000000000000, 0.000000000000000000, -0.000000000000000000 ) ) ;
#1023=AXIS2_PLACEMENT_3D ( 'NONE', #1782, #9182, #1666 ) ;
#1025=AXIS2_PLACEMENT_3D ( 'NONE', #7648, #7528, #5820 ) ;
#1026=AXIS2_PLACEMENT_3D ( 'NONE', #1109, #4841, #5145 ) ;
#1028=DIRECTION ( 'NONE',  ( 0.000000000000000000, 0.000000000000000000, 1.000000000000000000 ) ) ;
#1029=ORIENTED_EDGE ( 'NONE', *, *, #8017, .F. ) ;
#1030=EDGE_CURVE ( 'NONE', #5818, #5746, #4634, .T. ) ;
#1032=ORIENTED_EDGE ( 'NONE', *, *, #5642, .T. ) ;
#1033=ORIENTED_EDGE ( 'NONE', *, *, #3594, .T. ) ;
#1035=VECTOR ( 'NONE', #9113, 1000.000000000000000 ) ;
#1036=CARTESIAN_POINT ( 'NONE',  ( 0.000000000000000000, 0.000000000000000000, 0.000000000000000000 ) ) ;
#1037=DIRECTION ( 'NONE',  ( 0.000000000000000000, 0.000000000000000000, -1.000000000000000000 ) ) ;
#1038=CYLINDRICAL_SURFACE ( 'NONE', #7585, 22.99899999999999878 ) ;
#1039=DIRECTION ( 'NONE',  ( -1.000000000000000000, -0.000000000000000000, -0.000000000000000000 ) ) ;
#1043=EDGE_LOOP ( 'NONE', ( #5356, #3147, #11496, #8649 ) ) ;
#1044=ORIENTED_EDGE ( 'NONE', *, *, #11340, .T. ) ;
#1046=ORIENTED_EDGE ( 'NONE', *, *, #8832, .T. ) ;
#1048=DIRECTION ( 'NONE',  ( 1.000000000000000000, 0.000000000000000000, -0.000000000000000000 ) ) ;
#1049=VERTEX_POINT ( 'NONE', #11186 ) ;
#1050=EDGE_CURVE ( 'NONE', #1721, #9359, #9285, .T. ) ;
#1051=CARTESIAN_POINT ( 'NONE',  ( 3.000000000000000888, -11.79560690673886292, 19.74380051311536022 ) ) ;
#1052=DIRECTION ( 'NONE',  ( -1.000000000000000000, 0.000000000000000000, -0.000000000000000000 ) ) ;
#1054=EDGE_CURVE ( 'NONE', #1140, #308, #5697, .T. ) ;
#1055=CARTESIAN_POINT ( 'NONE',  ( 3.000000000000000888, 0.4575788569251889593, 22.54798042742718067 ) ) ;
#1056=DIRECTION ( 'NONE',  ( -1.000000000000000000, -0.000000000000000000, -0.000000000000000000 ) ) ;
#1057=AXIS2_PLACEMENT_3D ( 'NONE', #10270, #1887, #8448 ) ;
#1058=ORIENTED_EDGE ( 'NONE', *, *, #1054, .T. ) ;
#1059=CARTESIAN_POINT ( 'NONE',  ( 3.000000000000000888, -22.54798042742717357, 9.142421143074578538 ) ) ;
#1060=ORIENTED_EDGE ( 'NONE', *, *, #3456, .F. ) ;
#1063=EDGE_CURVE ( 'NONE', #264, #11972, #2764, .T. ) ;
#1064=DIRECTION ( 'NONE',  ( 1.000000000000000000, 0.000000000000000000, 0.000000000000000000 ) ) ;
#1066=AXIS2_PLACEMENT_3D ( 'NONE', #10300, #6685, #3028 ) ;
#1067=CARTESIAN_POINT ( 'NONE',  ( 3.000000000000000888, 0.000000000000000000, 0.000000000000000000 ) ) ;
#1068=CARTESIAN_POINT ( 'NONE',  ( 0.000000000000000000, 15.42759117534407309, -16.45023496161649845 ) ) ;
#1070=DIRECTION ( 'NONE',  ( -1.000000000000000000, 0.000000000000000000, 0.000000000000000000 ) ) ;
#1072=ORIENTED_EDGE ( 'NONE', *, *, #7174, .T. ) ;
#1073=DIRECTION ( 'NONE',  ( 0.000000000000000000, 0.000000000000000000, 1.000000000000000000 ) ) ;
#1074=VECTOR ( 'NONE', #6072, 1000.000000000000000 ) ;
#1075=ORIENTED_EDGE ( 'NONE', *, *, #7340, .F. ) ;
#1076=DIRECTION ( 'NONE',  ( -1.000000000000000000, 0.000000000000000000, -0.000000000000000000 ) ) ;
#1081=CARTESIAN_POINT ( 'NONE',  ( 3.000000000000000888, 13.28910708463157775, -20.93895013827567908 ) ) ;
#1082=VERTEX_POINT ( 'NONE', #2736 ) ;
#1083=ADVANCED_FACE ( 'NONE', ( #1998 ), #6464, .T. ) ;
#1084=VERTEX_POINT ( 'NONE', #6638 ) ;
#1085=ORIENTED_EDGE ( 'NONE', *, *, #6750, .T. ) ;
#1086=CARTESIAN_POINT ( 'NONE',  ( 0.000000000000000000, 1.901833551798570721, -22.47229024614975401 ) ) ;
#1087=AXIS2_PLACEMENT_3D ( 'NONE', #11829, #1792, #10912 ) ;
#1089=ORIENTED_EDGE ( 'NONE', *, *, #3366, .T. ) ;
#1090=DIRECTION ( 'NONE',  ( 0.000000000000000000, 0.000000000000000000, 1.000000000000000000 ) ) ;
#1091=CYLINDRICAL_SURFACE ( 'NONE', #11684, 9.599999999999997868 ) ;
#1092=EDGE_CURVE ( 'NONE', #8486, #2895, #9605, .T. ) ;
#1093=DIRECTION ( 'NONE',  ( -1.000000000000000000, -0.000000000000000000, 0.000000000000000000 ) ) ;
#1095=AXIS2_PLACEMENT_3D ( 'NONE', #2095, #5833, #9563 ) ;
#1096=CARTESIAN_POINT ( 'NONE',  ( 0.000000000000000000, -20.78471918669854901, -8.753070780933368766 ) ) ;
#1097=ORIENTED_EDGE ( 'NONE', *, *, #8084, .F. ) ;
#1098=VERTEX_POINT ( 'NONE', #9466 ) ;
#1100=CARTESIAN_POINT ( 'NONE',  ( 0.000000000000000000, 1.901833551798254973, 22.47229024614977888 ) ) ;
#1101=VERTEX_POINT ( 'NONE', #1081 ) ;
#1102=LINE ( 'NONE', #169, #5352 ) ;
#1103=CARTESIAN_POINT ( 'NONE',  ( 0.000000000000000000, 20.93895013827581408, 13.28910708463135215 ) ) ;
#1104=ORIENTED_EDGE ( 'NONE', *, *, #7024, .T. ) ;
#1105=CARTESIAN_POINT ( 'NONE',  ( 0.000000000000000000, 0.000000000000000000, 0.000000000000000000 ) ) ;
#1106=CARTESIAN_POINT ( 'NONE',  ( 3.000000000000000888, 13.23915371906955052, 18.80635025205174671 ) ) ;
#1108=CARTESIAN_POINT ( 'NONE',  ( 50.00005079999999680, 0.000000000000000000, 4.000000000000000000 ) ) ;
#1109=CARTESIAN_POINT ( 'NONE',  ( -10.00000000000000000, 0.000000000000000000, 0.000000000000000000 ) ) ;
#1110=ORIENTED_EDGE ( 'NONE', *, *, #8556, .F. ) ;
#1111=ORIENTED_EDGE ( 'NONE', *, *, #709, .T. ) ;
#1112=CYLINDRICAL_SURFACE ( 'NONE', #203, 9.599999999999997868 ) ;
#1113=EDGE_LOOP ( 'NONE', ( #6486, #11813, #10521, #6467 ) ) ;
#1115=EDGE_CURVE ( 'NONE', #11364, #9575, #1005, .T. ) ;
#1116=DIRECTION ( 'NONE',  ( 0.000000000000000000, 0.8660254037844398178, -0.4999999999999979461 ) ) ;
#1118=DIRECTION ( 'NONE',  ( 0.000000000000000000, 0.2079116908177597312, -0.9781476007338056888 ) ) ;
#1119=CARTESIAN_POINT ( 'NONE',  ( 3.000000000000000888, 5.135568396240338451, -21.96011696265485824 ) ) ;
#1120=DIRECTION ( 'NONE',  ( -1.000000000000000000, 0.000000000000000000, 0.000000000000000000 ) ) ;
#1122=CARTESIAN_POINT ( 'NONE',  ( 3.000000000000000888, 0.000000000000000000, 0.000000000000000000 ) ) ;
#1124=EDGE_CURVE ( 'NONE', #9845, #5068, #6583, .T. ) ;
#1125=DIRECTION ( 'NONE',  ( 0.000000000000000000, 0.000000000000000000, 1.000000000000000000 ) ) ;
#1126=ORIENTED_EDGE ( 'NONE', *, *, #3442, .F. ) ;
#1127=EDGE_CURVE ( 'NONE', #11577, #2393, #10315, .T. ) ;
#1128=CARTESIAN_POINT ( 'NONE',  ( 3.000000000000000888, -20.93895013827591001, 13.28910708463121360 ) ) ;
#1129=ORIENTED_EDGE ( 'NONE', *, *, #6007, .F. ) ;
#1130=ORIENTED_EDGE ( 'NONE', *, *, #4758, .T. ) ;
#1131=AXIS2_PLACEMENT_3D ( 'NONE', #3999, #2397, #7847 ) ;
#1132=DIRECTION ( 'NONE',  ( 0.000000000000000000, 0.000000000000000000, 1.000000000000000000 ) ) ;
#1134=CARTESIAN_POINT ( 'NONE',  ( -10.00000000000000000, 0.000000000000000000, 0.000000000000000000 ) ) ;
#1136=ADVANCED_FACE ( 'NONE', ( #2672 ), #94, .T. ) ;
#1139=CARTESIAN_POINT ( 'NONE',  ( 0.000000000000000000, 15.64281154287620446, -16.85990652506883691 ) ) ;
#1140=VERTEX_POINT ( 'NONE', #4759 ) ;
#1141=ORIENTED_EDGE ( 'NONE', *, *, #3972, .F. ) ;
#1142=CARTESIAN_POINT ( 'NONE',  ( 3.000000000000000888, 0.000000000000000000, 0.000000000000000000 ) ) ;
#1143=EDGE_CURVE ( 'NONE', #2754, #8927, #149, .T. ) ;
#1144=DIRECTION ( 'NONE',  ( 1.000000000000000000, 0.000000000000000000, 0.000000000000000000 ) ) ;
#1145=VERTEX_POINT ( 'NONE', #6937 ) ;
#1146=VECTOR ( 'NONE', #1635, 1000.000000000000000 ) ;
#1147=DIRECTION ( 'NONE',  ( 0.000000000000000000, 0.000000000000000000, 1.000000000000000000 ) ) ;
#1148=DIRECTION ( 'NONE',  ( 0.000000000000000000, 0.000000000000000000, -1.000000000000000000 ) ) ;
#1149=EDGE_CURVE ( 'NONE', #7092, #11368, #11944, .T. ) ;
#1150=CARTESIAN_POINT ( 'NONE',  ( 3.000000000000000888, -22.83456483164690809, 2.745295967525920311 ) ) ;
#1152=CARTESIAN_POINT ( 'NONE',  ( 0.000000000000000000, -7.402892494506437160, 21.30300407174360444 ) ) ;
#1153=AXIS2_PLACEMENT_3D ( 'NONE', #8000, #950, #10759 ) ;
#1154=ORIENTED_EDGE ( 'NONE', *, *, #3077, .F. ) ;
#1155=ORIENTED_EDGE ( 'NONE', *, *, #9457, .T. ) ;
#1157=EDGE_CURVE ( 'NONE', #505, #6372, #11914, .T. ) ;
#1158=ORIENTED_EDGE ( 'NONE', *, *, #8658, .F. ) ;
#1159=CARTESIAN_POINT ( 'NONE',  ( 0.000000000000000000, -4.445336973061012387, 22.56530478845647636 ) ) ;
#1160=CARTESIAN_POINT ( 'NONE',  ( 3.000000000000000888, -21.76479567747246691, 7.432877647175128999 ) ) ;
#1161=DIRECTION ( 'NONE',  ( -1.000000000000000000, 0.000000000000000000, 0.000000000000000000 ) ) ;
#1162=ORIENTED_EDGE ( 'NONE', *, *, #7713, .T. ) ;
#1164=DIRECTION ( 'NONE',  ( -1.000000000000000000, 0.000000000000000000, -0.000000000000000000 ) ) ;
#1167=VERTEX_POINT ( 'NONE', #10498 ) ;
#1168=EDGE_CURVE ( 'NONE', #7859, #6466, #3553, .T. ) ;
#1169=CARTESIAN_POINT ( 'NONE',  ( 0.000000000000000000, 0.000000000000000000, 0.000000000000000000 ) ) ;
#1171=LINE ( 'NONE', #2090, #4306 ) ;
#1172=ORIENTED_EDGE ( 'NONE', *, *, #9523, .T. ) ;
#1174=CARTESIAN_POINT ( 'NONE',  ( 0.000000000000000000, 0.000000000000000000, 0.000000000000000000 ) ) ;
#1176=CARTESIAN_POINT ( 'NONE',  ( 1.500000000000000444, 20.65684170206491999, 13.72351598154904195 ) ) ;
#1177=CARTESIAN_POINT ( 'NONE',  ( 3.000000000000000888, 0.000000000000000000, 0.000000000000000000 ) ) ;
#1180=CARTESIAN_POINT ( 'NONE',  ( 0.000000000000000000, 0.000000000000000000, 0.000000000000000000 ) ) ;
#1182=CIRCLE ( 'NONE', #7240, 9.599999999999997868 ) ;
#1183=CARTESIAN_POINT ( 'NONE',  ( 0.000000000000000000, -1.901833551798098876, -22.47229024614979309 ) ) ;
#1184=ORIENTED_EDGE ( 'NONE', *, *, #11809, .F. ) ;
#1186=DIRECTION ( 'NONE',  ( -1.000000000000000000, -0.000000000000000000, -0.000000000000000000 ) ) ;
#1187=ORIENTED_EDGE ( 'NONE', *, *, #8155, .T. ) ;
#1188=ORIENTED_EDGE ( 'NONE', *, *, #2810, .F. ) ;
#1189=CIRCLE ( 'NONE', #5695, 24.80000000000000071 ) ;
#1192=ADVANCED_FACE ( 'NONE', ( #395 ), #7805, .T. ) ;
#1193=AXIS2_PLACEMENT_3D ( 'NONE', #9116, #12108, #861 ) ;
#1194=DIRECTION ( 'NONE',  ( 1.000000000000000000, -0.000000000000000000, -0.000000000000000000 ) ) ;
#1195=EDGE_CURVE ( 'NONE', #11174, #8071, #3958, .T. ) ;
#1196=ADVANCED_FACE ( 'NONE', ( #9645 ), #5855, .T. ) ;
#1199=DIRECTION ( 'NONE',  ( -1.000000000000000000, -0.000000000000000000, 0.000000000000000000 ) ) ;
#1200=CIRCLE ( 'NONE', #7650, 24.80000000000000071 ) ;
#1201=CYLINDRICAL_SURFACE ( 'NONE', #7816, 9.599999999999997868 ) ;
#1203=ORIENTED_EDGE ( 'NONE', *, *, #10173, .F. ) ;
#1204=CIRCLE ( 'NONE', #2974, 24.80000000000000071 ) ;
#1205=VECTOR ( 'NONE', #9593, 1000.000000000000000 ) ;
#1206=ORIENTED_EDGE ( 'NONE', *, *, #5264, .F. ) ;
#1207=EDGE_CURVE ( 'NONE', #1082, #8820, #9702, .T. ) ;
#1208=DIRECTION ( 'NONE',  ( 0.000000000000000000, 0.000000000000000000, 1.000000000000000000 ) ) ;
#1209=CARTESIAN_POINT ( 'NONE',  ( -10.00000000000000000, 0.000000000000000000, 0.000000000000000000 ) ) ;
#1212=CYLINDRICAL_SURFACE ( 'NONE', #2729, 24.80000000000000071 ) ;
#1213=DIRECTION ( 'NONE',  ( -1.000000000000000000, -0.000000000000000000, 0.000000000000000000 ) ) ;
#1214=CIRCLE ( 'NONE', #589, 24.80000000000000071 ) ;
#1216=AXIS2_PLACEMENT_3D ( 'NONE', #4607, #6379, #4547 ) ;
#1217=CARTESIAN_POINT ( 'NONE',  ( 3.000000000000000888, -22.42251312757882786, 5.117118920208413968 ) ) ;
#1218=ORIENTED_EDGE ( 'NONE', *, *, #1030, .F. ) ;
#1219=ORIENTED_EDGE ( 'NONE', *, *, #8065, .T. ) ;
#1222=ORIENTED_EDGE ( 'NONE', *, *, #10564, .F. ) ;
#1223=EDGE_CURVE ( 'NONE', #215, #12050, #9586, .T. ) ;
#1224=DIRECTION ( 'NONE',  ( 0.000000000000000000, 0.000000000000000000, -1.000000000000000000 ) ) ;
#1225=DIRECTION ( 'NONE',  ( 1.000000000000000000, 0.000000000000000000, -0.000000000000000000 ) ) ;
#1226=DIRECTION ( 'NONE',  ( -1.000000000000000000, -0.000000000000000000, -0.000000000000000000 ) ) ;
#1227=ORIENTED_EDGE ( 'NONE', *, *, #2172, .T. ) ;
#1228=AXIS2_PLACEMENT_3D ( 'NONE', #11918, #11017, #4400 ) ;
#1229=CARTESIAN_POINT ( 'NONE',  ( 0.000000000000000000, -22.54798042742717357, -0.4575788569254196636 ) ) ;
#1230=DIRECTION ( 'NONE',  ( 0.000000000000000000, 0.000000000000000000, 1.000000000000000000 ) ) ;
#1233=VERTEX_POINT ( 'NONE', #209 ) ;
#1234=DIRECTION ( 'NONE',  ( 0.000000000000000000, 0.000000000000000000, 1.000000000000000000 ) ) ;
#1235=ORIENTED_EDGE ( 'NONE', *, *, #11621, .T. ) ;
#1236=LINE ( 'NONE', #5888, #9771 ) ;
#1237=ORIENTED_EDGE ( 'NONE', *, *, #4685, .T. ) ;
#1238=EDGE_CURVE ( 'NONE', #5236, #2346, #4017, .T. ) ;
#1239=AXIS2_PLACEMENT_3D ( 'NONE', #2203, #10651, #7712 ) ;
#1241=VECTOR ( 'NONE', #2002, 1000.000000000000000 ) ;
#1242=AXIS2_PLACEMENT_3D ( 'NONE', #4961, #5070, #10585 ) ;
#1245=VERTEX_POINT ( 'NONE', #6029 ) ;
#1247=EDGE_CURVE ( 'NONE', #10823, #6189, #4140, .T. ) ;
#1248=CARTESIAN_POINT ( 'NONE',  ( 3.000000000000000888, 22.54798042742718067, -0.4575788569252652871 ) ) ;
#1250=CIRCLE ( 'NONE', #11408, 24.80000000000000071 ) ;
#1251=DIRECTION ( 'NONE',  ( 0.000000000000000000, 0.000000000000000000, 1.000000000000000000 ) ) ;
#1253=DIRECTION ( 'NONE',  ( -1.000000000000000000, -0.000000000000000000, -0.000000000000000000 ) ) ;
#1254=DIRECTION ( 'NONE',  ( 0.000000000000000000, 0.000000000000000000, 1.000000000000000000 ) ) ;
#1255=ORIENTED_EDGE ( 'NONE', *, *, #3978, .F. ) ;
#1256=VERTEX_POINT ( 'NONE', #1139 ) ;
#1257=AXIS2_PLACEMENT_3D ( 'NONE', #9265, #10059, #1678 ) ;
#1258=DIRECTION ( 'NONE',  ( -1.000000000000000000, -0.000000000000000000, -0.000000000000000000 ) ) ;
#1260=CARTESIAN_POINT ( 'NONE',  ( 0.000000000000000000, -2.745295967526151237, 22.83456483164687967 ) ) ;
#1265=ORIENTED_EDGE ( 'NONE', *, *, #1432, .F. ) ;
#1266=ORIENTED_EDGE ( 'NONE', *, *, #3544, .F. ) ;
#1267=DIRECTION ( 'NONE',  ( -1.000000000000000000, 0.000000000000000000, 0.000000000000000000 ) ) ;
#1268=DIRECTION ( 'NONE',  ( 0.000000000000000000, 0.000000000000000000, -1.000000000000000000 ) ) ;
#1270=DIRECTION ( 'NONE',  ( -1.000000000000000000, -0.000000000000000000, -0.000000000000000000 ) ) ;
#1272=EDGE_CURVE ( 'NONE', #4610, #9844, #3527, .T. ) ;
#1273=EDGE_CURVE ( 'NONE', #11632, #10794, #11562, .T. ) ;
#1274=DIRECTION ( 'NONE',  ( -1.000000000000000000, 0.000000000000000000, 0.000000000000000000 ) ) ;
#1275=ORIENTED_EDGE ( 'NONE', *, *, #5497, .T. ) ;
#1276=ORIENTED_EDGE ( 'NONE', *, *, #2766, .T. ) ;
#1277=ADVANCED_FACE ( 'NONE', ( #10558 ), #1201, .T. ) ;
#1280=EDGE_LOOP ( 'NONE', ( #8265, #6299, #703, #8310 ) ) ;
#1281=CYLINDRICAL_SURFACE ( 'NONE', #8779, 9.599999999999997868 ) ;
#1282=CARTESIAN_POINT ( 'NONE',  ( 3.000000000000000888, 0.000000000000000000, 0.000000000000000000 ) ) ;
#1283=DIRECTION ( 'NONE',  ( -1.000000000000000000, -0.000000000000000000, 0.000000000000000000 ) ) ;
#1284=ORIENTED_EDGE ( 'NONE', *, *, #1273, .F. ) ;
#1285=DIRECTION ( 'NONE',  ( 0.000000000000000000, 0.000000000000000000, 1.000000000000000000 ) ) ;
#1286=CIRCLE ( 'NONE', #8126, 9.599999999999996092 ) ;
#1287=DIRECTION ( 'NONE',  ( -1.000000000000000000, 0.000000000000000000, -0.000000000000000000 ) ) ;
#1289=ORIENTED_EDGE ( 'NONE', *, *, #6750, .F. ) ;
#1290=DIRECTION ( 'NONE',  ( 0.000000000000000000, 0.000000000000000000, 1.000000000000000000 ) ) ;
#1291=ORIENTED_EDGE ( 'NONE', *, *, #148, .F. ) ;
#1292=LINE ( 'NONE', #11398, #10752 ) ;
#1293=ORIENTED_EDGE ( 'NONE', *, *, #3442, .T. ) ;
#1296=ADVANCED_FACE ( 'NONE', ( #8612 ), #11359, .T. ) ;
#1302=AXIS2_PLACEMENT_3D ( 'NONE', #4835, #10338, #11387 ) ;
#1303=LINE ( 'NONE', #2161, #52 ) ;
#1304=CARTESIAN_POINT ( 'NONE',  ( 0.000000000000000000, -9.039786367038701087, -21.14796121233205284 ) ) ;
#1305=DIRECTION ( 'NONE',  ( 1.000000000000000000, 0.000000000000000000, 0.000000000000000000 ) ) ;
#1306=ORIENTED_EDGE ( 'NONE', *, *, #10319, .F. ) ;
#1307=VERTEX_POINT ( 'NONE', #11838 ) ;
#1308=ADVANCED_FACE ( 'NONE', ( #1500 ), #7924, .T. ) ;
#1309=VERTEX_POINT ( 'NONE', #701 ) ;
#1310=CARTESIAN_POINT ( 'NONE',  ( 3.000000000000000888, 5.135568396240030253, 21.96011696265493285 ) ) ;
#1311=CARTESIAN_POINT ( 'NONE',  ( 3.000000000000000888, 21.58580335785676496, 6.532525787311040943 ) ) ;
#1314=DIRECTION ( 'NONE',  ( -1.000000000000000000, 0.000000000000000000, 0.000000000000000000 ) ) ;
#1316=ORIENTED_EDGE ( 'NONE', *, *, #32, .T. ) ;
#1317=AXIS2_PLACEMENT_3D ( 'NONE', #9087, #7352, #7170 ) ;
#1318=ORIENTED_EDGE ( 'NONE', *, *, #11892, .F. ) ;
#1319=ORIENTED_EDGE ( 'NONE', *, *, #5767, .F. ) ;
#1320=DIRECTION ( 'NONE',  ( 1.000000000000000000, -0.000000000000000000, -0.000000000000000000 ) ) ;
#1321=CARTESIAN_POINT ( 'NONE',  ( 3.000000000000000888, -19.75591328264893676, 10.87771529938155268 ) ) ;
#1322=CARTESIAN_POINT ( 'NONE',  ( 3.000000000000000888, 22.37663021667344054, 6.788022064062137595 ) ) ;
#1323=CARTESIAN_POINT ( 'NONE',  ( 1.500000000000000444, 24.77821629063821973, 1.039229259764577140 ) ) ;
#1324=AXIS2_PLACEMENT_3D ( 'NONE', #7096, #1479, #9126 ) ;
#1327=DIRECTION ( 'NONE',  ( 0.000000000000000000, 0.000000000000000000, 1.000000000000000000 ) ) ;
#1328=ORIENTED_EDGE ( 'NONE', *, *, #3223, .T. ) ;
#1329=VERTEX_POINT ( 'NONE', #6994 ) ;
#1332=ORIENTED_EDGE ( 'NONE', *, *, #11096, .T. ) ;
#1333=AXIS2_PLACEMENT_3D ( 'NONE', #4205, #465, #10569 ) ;
#1334=CARTESIAN_POINT ( 'NONE',  ( 3.000000000000000888, 21.97702544527757951, 6.779701584702809924 ) ) ;
#1335=DIRECTION ( 'NONE',  ( -1.000000000000000000, -0.000000000000000000, -0.000000000000000000 ) ) ;
#1337=DIRECTION ( 'NONE',  ( -1.000000000000000000, 0.000000000000000000, 0.000000000000000000 ) ) ;
#1338=ORIENTED_EDGE ( 'NONE', *, *, #11596, .F. ) ;
#1339=ADVANCED_FACE ( 'NONE', ( #3337 ), #9092, .T. ) ;
#1340=CARTESIAN_POINT ( 'NONE',  ( 0.000000000000000000, -17.71842311621541555, 17.35216073792434699 ) ) ;
#1341=EDGE_CURVE ( 'NONE', #10120, #5082, #7246, .T. ) ;
#1342=EDGE_CURVE ( 'NONE', #11577, #1307, #3132, .T. ) ;
#1343=FACE_OUTER_BOUND ( 'NONE', #7607, .T. ) ;
#1345=AXIS2_PLACEMENT_3D ( 'NONE', #8106, #6337, #1553 ) ;
#1346=EDGE_LOOP ( 'NONE', ( #829, #800, #7562, #3730 ) ) ;
#1347=CARTESIAN_POINT ( 'NONE',  ( 3.000000000000000888, 19.29833442572359559, 11.67026512804553562 ) ) ;
#1349=LINE ( 'NONE', #11686, #10573 ) ;
#1350=EDGE_LOOP ( 'NONE', ( #7731, #8140, #8311, #7645 ) ) ;
#1352=EDGE_CURVE ( 'NONE', #9137, #10458, #1628, .T. ) ;
#1353=VECTOR ( 'NONE', #9531, 1000.000000000000000 ) ;
#1354=LINE ( 'NONE', #10716, #5395 ) ;
#1356=AXIS2_PLACEMENT_3D ( 'NONE', #6773, #4026, #228 ) ;
#1357=DIRECTION ( 'NONE',  ( 0.000000000000000000, 0.000000000000000000, 1.000000000000000000 ) ) ;
#1358=CARTESIAN_POINT ( 'NONE',  ( 3.000000000000000888, 8.645255683529006419, 23.24434456306327590 ) ) ;
#1360=LINE ( 'NONE', #6075, #11377 ) ;
#1362=CARTESIAN_POINT ( 'NONE',  ( 0.000000000000000000, 15.80756504416690866, 19.10918332567963773 ) ) ;
#1363=ADVANCED_FACE ( 'NONE', ( #5296 ), #578, .T. ) ;
#1364=VERTEX_POINT ( 'NONE', #3408 ) ;
#1365=CYLINDRICAL_SURFACE ( 'NONE', #10553, 9.599999999999997868 ) ;
#1366=AXIS2_PLACEMENT_3D ( 'NONE', #6949, #2370, #8744 ) ;
#1367=VERTEX_POINT ( 'NONE', #2539 ) ;
#1368=ORIENTED_EDGE ( 'NONE', *, *, #9518, .F. ) ;
#1369=EDGE_CURVE ( 'NONE', #8857, #9360, #4251, .T. ) ;
#1370=FACE_OUTER_BOUND ( 'NONE', #11080, .T. ) ;
#1372=DIRECTION ( 'NONE',  ( 0.000000000000000000, 0.4067366430757948792, 0.9135454576426033091 ) ) ;
#1373=CIRCLE ( 'NONE', #583, 24.80000000000000071 ) ;
#1377=CARTESIAN_POINT ( 'NONE',  ( 3.000000000000000888, 0.000000000000000000, 0.000000000000000000 ) ) ;
#1378=CARTESIAN_POINT ( 'NONE',  ( 0.000000000000000000, 16.45023496161665122, 15.42759117534391322 ) ) ;
#1379=ORIENTED_EDGE ( 'NONE', *, *, #9289, .F. ) ;
#1380=ORIENTED_EDGE ( 'NONE', *, *, #4966, .T. ) ;
#1381=AXIS2_PLACEMENT_3D ( 'NONE', #9537, #976, #10331 ) ;
#1382=AXIS2_PLACEMENT_3D ( 'NONE', #12007, #934, #3687 ) ;
#1383=VERTEX_POINT ( 'NONE', #7979 ) ;
#1384=ADVANCED_FACE ( 'NONE', ( #10869 ), #10064, .T. ) ;
#1385=LINE ( 'NONE', #11548, #1205 ) ;
#1386=DIRECTION ( 'NONE',  ( -1.000000000000000000, -0.000000000000000000, -0.000000000000000000 ) ) ;
#1387=LINE ( 'NONE', #1323, #3883 ) ;
#1388=AXIS2_PLACEMENT_3D ( 'NONE', #8280, #12005, #8523 ) ;
#1390=CIRCLE ( 'NONE', #3157, 9.599999999999996092 ) ;
#1392=VECTOR ( 'NONE', #9347, 1000.000000000000000 ) ;
#1394=DIRECTION ( 'NONE',  ( -1.000000000000000000, 0.000000000000000000, 0.000000000000000000 ) ) ;
#1395=ORIENTED_EDGE ( 'NONE', *, *, #8378, .F. ) ;
#1396=ORIENTED_EDGE ( 'NONE', *, *, #5019, .F. ) ;
#1399=AXIS2_PLACEMENT_3D ( 'NONE', #4070, #511, #7050 ) ;
#1400=ORIENTED_EDGE ( 'NONE', *, *, #10170, .F. ) ;
#1401=FACE_OUTER_BOUND ( 'NONE', #3208, .T. ) ;
#1402=FACE_OUTER_BOUND ( 'NONE', #11929, .T. ) ;
#1403=AXIS2_PLACEMENT_3D ( 'NONE', #8748, #10457, #11318 ) ;
#1405=ORIENTED_EDGE ( 'NONE', *, *, #370, .F. ) ;
#1406=CARTESIAN_POINT ( 'NONE',  ( 0.000000000000000000, 1.039229259764488544, 24.77821629063822328 ) ) ;
#1407=DIRECTION ( 'NONE',  ( -1.000000000000000000, 0.000000000000000000, 0.000000000000000000 ) ) ;
#1409=VECTOR ( 'NONE', #10085, 1000.000000000000000 ) ;
#1410=ORIENTED_EDGE ( 'NONE', *, *, #4874, .T. ) ;
#1411=CARTESIAN_POINT ( 'NONE',  ( 0.000000000000000000, 13.79477846460820700, -18.40266524480574972 ) ) ;
#1412=DIRECTION ( 'NONE',  ( 0.000000000000000000, 0.000000000000000000, 1.000000000000000000 ) ) ;
#1413=ORIENTED_EDGE ( 'NONE', *, *, #3339, .T. ) ;
#1414=EDGE_CURVE ( 'NONE', #2229, #1487, #2418, .T. ) ;
#1416=AXIS2_PLACEMENT_3D ( 'NONE', #10027, #9910, #1524 ) ;
#1417=ORIENTED_EDGE ( 'NONE', *, *, #748, .F. ) ;
#1418=DIRECTION ( 'NONE',  ( -1.000000000000000000, 0.000000000000000000, 0.000000000000000000 ) ) ;
#1419=VERTEX_POINT ( 'NONE', #11897 ) ;
#1420=CARTESIAN_POINT ( 'NONE',  ( 3.000000000000000888, 0.000000000000000000, 0.000000000000000000 ) ) ;
#1421=CARTESIAN_POINT ( 'NONE',  ( 0.000000000000000000, -9.589108953447752270, -20.41249101028221702 ) ) ;
#1423=CARTESIAN_POINT ( 'NONE',  ( 0.000000000000000000, 18.40266524480607657, -13.79477846460777357 ) ) ;
#1426=DIRECTION ( 'NONE',  ( 0.000000000000000000, 0.5000000000000011102, -0.8660254037844381525 ) ) ;
#1427=AXIS2_PLACEMENT_3D ( 'NONE', #6376, #4415, #8147 ) ;
#1428=DIRECTION ( 'NONE',  ( 0.000000000000000000, 0.1045284632676469622, 0.9945218953682738450 ) ) ;
#1429=EDGE_CURVE ( 'NONE', #8745, #5789, #4378, .T. ) ;
#1430=VERTEX_POINT ( 'NONE', #7117 ) ;
#1431=CIRCLE ( 'NONE', #9634, 9.599999999999997868 ) ;
#1432=EDGE_CURVE ( 'NONE', #10038, #401, #4311, .T. ) ;
#1434=ORIENTED_EDGE ( 'NONE', *, *, #9981, .T. ) ;
#1435=CIRCLE ( 'NONE', #9067, 24.80000000000000071 ) ;
#1436=CARTESIAN_POINT ( 'NONE',  ( 0.000000000000000000, 0.000000000000000000, 0.000000000000000000 ) ) ;
#1437=DIRECTION ( 'NONE',  ( 0.000000000000000000, -0.8660254037844328234, -0.5000000000000099920 ) ) ;
#1440=CARTESIAN_POINT ( 'NONE',  ( 3.000000000000000888, 4.135161237383582211, 24.45282072769602166 ) ) ;
#1441=CARTESIAN_POINT ( 'NONE',  ( 1.500000000000000444, 19.10918332567978695, -15.80756504416671859 ) ) ;
#1442=ORIENTED_EDGE ( 'NONE', *, *, #10393, .T. ) ;
#1443=ORIENTED_EDGE ( 'NONE', *, *, #10130, .F. ) ;
#1444=VECTOR ( 'NONE', #11775, 1000.000000000000000 ) ;
#1445=VERTEX_POINT ( 'NONE', #9939 ) ;
#1448=CARTESIAN_POINT ( 'NONE',  ( 3.000000000000000888, 6.532525787311267429, -21.58580335785669746 ) ) ;
#1449=AXIS2_PLACEMENT_3D ( 'NONE', #10163, #9073, #4355 ) ;
#1451=EDGE_CURVE ( 'NONE', #2557, #11577, #3745, .T. ) ;
#1452=DIRECTION ( 'NONE',  ( -1.000000000000000000, 0.000000000000000000, 0.000000000000000000 ) ) ;
#1453=DIRECTION ( 'NONE',  ( 1.000000000000000000, 0.000000000000000000, 0.000000000000000000 ) ) ;
#1454=VERTEX_POINT ( 'NONE', #10988 ) ;
#1455=ORIENTED_EDGE ( 'NONE', *, *, #8279, .F. ) ;
#1457=ORIENTED_EDGE ( 'NONE', *, *, #6577, .T. ) ;
#1458=CARTESIAN_POINT ( 'NONE',  ( 1.499999999999999556, 6.168200451485757796, 24.02068490260614908 ) ) ;
#1459=DIRECTION ( 'NONE',  ( 0.000000000000000000, 0.000000000000000000, 1.000000000000000000 ) ) ;
#1460=CARTESIAN_POINT ( 'NONE',  ( 3.000000000000000888, 9.128825345753028842, 23.05871956130125255 ) ) ;
#1461=ADVANCED_FACE ( 'NONE', ( #6342 ), #1683, .T. ) ;
#1463=DIRECTION ( 'NONE',  ( 0.000000000000000000, 0.5877852522924742473, -0.8090169943749466741 ) ) ;
#1464=ORIENTED_EDGE ( 'NONE', *, *, #7745, .T. ) ;
#1465=CARTESIAN_POINT ( 'NONE',  ( 0.000000000000000000, 0.000000000000000000, 0.000000000000000000 ) ) ;
#1466=LINE ( 'NONE', #6847, #4148 ) ;
#1469=CARTESIAN_POINT ( 'NONE',  ( 0.000000000000000000, 0.000000000000000000, 0.000000000000000000 ) ) ;
#1471=DIRECTION ( 'NONE',  ( -1.000000000000000000, 0.000000000000000000, -0.000000000000000000 ) ) ;
#1472=ORIENTED_EDGE ( 'NONE', *, *, #2415, .T. ) ;
#1475=DIRECTION ( 'NONE',  ( 0.000000000000000000, 0.000000000000000000, 1.000000000000000000 ) ) ;
#1479=DIRECTION ( 'NONE',  ( -1.000000000000000000, 0.000000000000000000, 0.000000000000000000 ) ) ;
#1480=CARTESIAN_POINT ( 'NONE',  ( 3.000000000000000888, 22.54798042742717712, 0.4575788569255671012 ) ) ;
#1482=CYLINDRICAL_SURFACE ( 'NONE', #10001, 4.000000000000000000 ) ;
#1484=CARTESIAN_POINT ( 'NONE',  ( 0.000000000000000000, 5.135568396240338451, -21.96011696265485824 ) ) ;
#1485=AXIS2_PLACEMENT_3D ( 'NONE', #6008, #9736, #5088 ) ;
#1486=DIRECTION ( 'NONE',  ( 0.000000000000000000, 0.000000000000000000, 1.000000000000000000 ) ) ;
#1487=VERTEX_POINT ( 'NONE', #8231 ) ;
#1488=EDGE_CURVE ( 'NONE', #5509, #8343, #9992, .T. ) ;
#1489=CARTESIAN_POINT ( 'NONE',  ( 3.000000000000000888, -16.45023496161654819, -15.42759117534402513 ) ) ;
#1491=VERTEX_POINT ( 'NONE', #82 ) ;
#1494=EDGE_CURVE ( 'NONE', #10107, #3562, #11343, .T. ) ;
#1495=DIRECTION ( 'NONE',  ( -1.000000000000000000, -0.000000000000000000, 0.000000000000000000 ) ) ;
#1496=DIRECTION ( 'NONE',  ( 1.000000000000000000, 0.000000000000000000, -0.000000000000000000 ) ) ;
#1499=EDGE_CURVE ( 'NONE', #8706, #9548, #782, .T. ) ;
#1500=FACE_OUTER_BOUND ( 'NONE', #5662, .T. ) ;
#1501=ORIENTED_EDGE ( 'NONE', *, *, #218, .F. ) ;
#1504=ADVANCED_FACE ( 'NONE', ( #2721 ), #3827, .T. ) ;
#1506=CARTESIAN_POINT ( 'NONE',  ( 0.000000000000000000, 0.000000000000000000, 0.000000000000000000 ) ) ;
#1509=CARTESIAN_POINT ( 'NONE',  ( 3.000000000000000888, 17.06259499759944021, 14.74749645580017088 ) ) ;
#1510=DIRECTION ( 'NONE',  ( -1.000000000000000000, -0.000000000000000000, -0.000000000000000000 ) ) ;
#1511=ORIENTED_EDGE ( 'NONE', *, *, #6007, .T. ) ;
#1512=ORIENTED_EDGE ( 'NONE', *, *, #6587, .T. ) ;
#1513=ADVANCED_FACE ( 'NONE', ( #10185 ), #8484, .T. ) ;
#1516=ORIENTED_EDGE ( 'NONE', *, *, #1352, .F. ) ;
#1517=DIRECTION ( 'NONE',  ( -1.000000000000000000, -0.000000000000000000, 0.000000000000000000 ) ) ;
#1518=DIRECTION ( 'NONE',  ( -1.000000000000000000, 0.000000000000000000, -0.000000000000000000 ) ) ;
#1519=DIRECTION ( 'NONE',  ( -1.000000000000000000, -0.000000000000000000, -0.000000000000000000 ) ) ;
#1520=EDGE_CURVE ( 'NONE', #7759, #7087, #4731, .T. ) ;
#1521=CARTESIAN_POINT ( 'NONE',  ( 3.000000000000000888, 0.000000000000000000, 0.000000000000000000 ) ) ;
#1523=CYLINDRICAL_SURFACE ( 'NONE', #7282, 9.599999999999997868 ) ;
#1524=DIRECTION ( 'NONE',  ( 0.000000000000000000, -0.5877852522924799095, 0.8090169943749425663 ) ) ;
#1526=EDGE_CURVE ( 'NONE', #10640, #4392, #2950, .T. ) ;
#1527=DIRECTION ( 'NONE',  ( 0.000000000000000000, 0.000000000000000000, -1.000000000000000000 ) ) ;
#1528=AXIS2_PLACEMENT_3D ( 'NONE', #2441, #8255, #6180 ) ;
#1529=CARTESIAN_POINT ( 'NONE',  ( 3.000000000000000888, 14.74749645580011226, 17.06259499759949705 ) ) ;
#1532=ORIENTED_EDGE ( 'NONE', *, *, #10939, .T. ) ;
#1533=CARTESIAN_POINT ( 'NONE',  ( 0.000000000000000000, 0.000000000000000000, 0.000000000000000000 ) ) ;
#1534=LINE ( 'NONE', #5619, #5659 ) ;
#1535=ORIENTED_EDGE ( 'NONE', *, *, #10921, .F. ) ;
#1536=LINE ( 'NONE', #3443, #939 ) ;
#1537=AXIS2_PLACEMENT_3D ( 'NONE', #9337, #28, #7497 ) ;
#1538=CARTESIAN_POINT ( 'NONE',  ( 0.000000000000000000, -7.402892494506152943, -21.30300407174369681 ) ) ;
#1540=ADVANCED_FACE ( 'NONE', ( #1802 ), #888, .T. ) ;
#1541=CARTESIAN_POINT ( 'NONE',  ( 3.000000000000000888, 0.000000000000000000, 0.000000000000000000 ) ) ;
#1543=CYLINDRICAL_SURFACE ( 'NONE', #10955, 9.599999999999997868 ) ;
#1544=ORIENTED_EDGE ( 'NONE', *, *, #10259, .F. ) ;
#1545=ORIENTED_EDGE ( 'NONE', *, *, #1526, .F. ) ;
#1546=DIRECTION ( 'NONE',  ( 0.000000000000000000, 0.000000000000000000, 1.000000000000000000 ) ) ;
#1547=ORIENTED_EDGE ( 'NONE', *, *, #5991, .F. ) ;
#1549=DIRECTION ( 'NONE',  ( -1.000000000000000000, -0.000000000000000000, -0.000000000000000000 ) ) ;
#1550=CARTESIAN_POINT ( 'NONE',  ( 0.000000000000000000, 0.000000000000000000, 0.000000000000000000 ) ) ;
#1551=DIRECTION ( 'NONE',  ( 0.000000000000000000, 0.000000000000000000, 1.000000000000000000 ) ) ;
#1552=EDGE_LOOP ( 'NONE', ( #6559, #8552, #1255, #3557 ) ) ;
#1553=DIRECTION ( 'NONE',  ( 0.000000000000000000, 0.5877852522924742473, -0.8090169943749467851 ) ) ;
#1556=CIRCLE ( 'NONE', #9955, 24.80000000000000071 ) ;
#1558=CARTESIAN_POINT ( 'NONE',  ( 3.000000000000000888, 0.000000000000000000, 0.000000000000000000 ) ) ;
#1559=DIRECTION ( 'NONE',  ( 0.000000000000000000, 0.8090169943749485615, -0.5877852522924714718 ) ) ;
#1560=ORIENTED_EDGE ( 'NONE', *, *, #7387, .F. ) ;
#1561=ORIENTED_EDGE ( 'NONE', *, *, #1499, .T. ) ;
#1563=AXIS2_PLACEMENT_3D ( 'NONE', #516, #2481, #6095 ) ;
#1566=AXIS2_PLACEMENT_3D ( 'NONE', #9954, #714, #6293 ) ;
#1567=CARTESIAN_POINT ( 'NONE',  ( 0.000000000000000000, -9.667200211209685534, -20.86861857134744014 ) ) ;
#1568=FACE_OUTER_BOUND ( 'NONE', #1601, .T. ) ;
#1571=LINE ( 'NONE', #3421, #10572 ) ;
#1572=CIRCLE ( 'NONE', #10991, 22.99899999999999523 ) ;
#1573=AXIS2_PLACEMENT_3D ( 'NONE', #10974, #2594, #6329 ) ;
#1575=CARTESIAN_POINT ( 'NONE',  ( 3.000000000000000888, 22.83456483164692585, -2.745295967525759995 ) ) ;
#1576=EDGE_LOOP ( 'NONE', ( #4957, #154, #8345, #6343 ) ) ;
#1577=EDGE_LOOP ( 'NONE', ( #3409, #4019, #9660, #8524 ) ) ;
#1579=EDGE_CURVE ( 'NONE', #3895, #8886, #10368, .T. ) ;
#1581=CARTESIAN_POINT ( 'NONE',  ( 3.000000000000000888, -15.13242714128107913, -17.31945870441162683 ) ) ;
#1582=DIRECTION ( 'NONE',  ( 0.000000000000000000, -0.1045284632676401204, -0.9945218953682746221 ) ) ;
#1583=AXIS2_PLACEMENT_3D ( 'NONE', #2801, #4577, #10132 ) ;
#1585=LINE ( 'NONE', #11913, #7552 ) ;
#1586=AXIS2_PLACEMENT_3D ( 'NONE', #9346, #40, #3789 ) ;
#1587=VERTEX_POINT ( 'NONE', #2847 ) ;
#1588=VECTOR ( 'NONE', #7266, 1000.000000000000000 ) ;
#1589=DIRECTION ( 'NONE',  ( 0.000000000000000000, 0.9135454576425992013, 0.4067366430758040385 ) ) ;
#1590=DIRECTION ( 'NONE',  ( 0.000000000000000000, -0.3090169943749543902, 0.9510565162951514218 ) ) ;
#1592=CIRCLE ( 'NONE', #5306, 9.599999999999996092 ) ;
#1593=DIRECTION ( 'NONE',  ( -1.000000000000000000, -0.000000000000000000, -0.000000000000000000 ) ) ;
#1594=AXIS2_PLACEMENT_3D ( 'NONE', #9402, #8551, #1028 ) ;
#1595=FACE_OUTER_BOUND ( 'NONE', #8601, .T. ) ;
#1596=VECTOR ( 'NONE', #1496, 1000.000000000000000 ) ;
#1597=ORIENTED_EDGE ( 'NONE', *, *, #3540, .F. ) ;
#1598=CIRCLE ( 'NONE', #5898, 9.599999999999997868 ) ;
#1599=EDGE_LOOP ( 'NONE', ( #1380, #11703, #2636, #6901 ) ) ;
#1601=EDGE_LOOP ( 'NONE', ( #810, #8925, #10839, #2380 ) ) ;
#1602=CARTESIAN_POINT ( 'NONE',  ( 3.000000000000000888, -24.77821629063821263, -1.039229259764747004 ) ) ;
#1604=CIRCLE ( 'NONE', #6680, 9.599999999999999645 ) ;
#1605=DIRECTION ( 'NONE',  ( 0.000000000000000000, 0.000000000000000000, 1.000000000000000000 ) ) ;
#1606=VECTOR ( 'NONE', #11275, 1000.000000000000000 ) ;
#1607=CARTESIAN_POINT ( 'NONE',  ( 3.000000000000000888, 1.039229259764835600, -24.77821629063820907 ) ) ;
#1610=ADVANCED_FACE ( 'NONE', ( #7296 ), #2662, .T. ) ;
#1611=CARTESIAN_POINT ( 'NONE',  ( 3.000000000000000888, -19.75591328264879110, -10.87771529938182091 ) ) ;
#1612=ORIENTED_EDGE ( 'NONE', *, *, #5481, .T. ) ;
#1614=VECTOR ( 'NONE', #64, 1000.000000000000000 ) ;
#1618=CIRCLE ( 'NONE', #234, 9.599999999999999645 ) ;
#1619=CARTESIAN_POINT ( 'NONE',  ( 3.000000000000000888, -13.23915371906942440, -18.80635025205183197 ) ) ;
#1620=ORIENTED_EDGE ( 'NONE', *, *, #5353, .T. ) ;
#1621=EDGE_CURVE ( 'NONE', #3019, #10826, #10249, .T. ) ;
#1622=CARTESIAN_POINT ( 'NONE',  ( 0.000000000000000000, 23.05871956130122413, 9.128825345753107001 ) ) ;
#1623=FACE_OUTER_BOUND ( 'NONE', #2541, .T. ) ;
#1625=VECTOR ( 'NONE', #9340, 1000.000000000000000 ) ;
#1627=DIRECTION ( 'NONE',  ( 0.000000000000000000, 0.000000000000000000, 1.000000000000000000 ) ) ;
#1628=LINE ( 'NONE', #6160, #11534 ) ;
#1629=CIRCLE ( 'NONE', #254, 9.599999999999997868 ) ;
#1630=VERTEX_POINT ( 'NONE', #1862 ) ;
#1633=CARTESIAN_POINT ( 'NONE',  ( 0.000000000000000000, 2.745295967525994918, 22.83456483164690098 ) ) ;
#1634=CIRCLE ( 'NONE', #8485, 9.599999999999999645 ) ;
#1635=DIRECTION ( 'NONE',  ( 1.000000000000000000, -0.000000000000000000, -0.000000000000000000 ) ) ;
#1637=VECTOR ( 'NONE', #6960, 1000.000000000000000 ) ;
#1638=FACE_OUTER_BOUND ( 'NONE', #10224, .T. ) ;
#1639=CARTESIAN_POINT ( 'NONE',  ( 3.000000000000000888, 15.64281154287597353, 16.85990652506905363 ) ) ;
#1642=ORIENTED_EDGE ( 'NONE', *, *, #4409, .F. ) ;
#1643=DIRECTION ( 'NONE',  ( -1.000000000000000000, 0.000000000000000000, 0.000000000000000000 ) ) ;
#1645=DIRECTION ( 'NONE',  ( 1.000000000000000000, 0.000000000000000000, 0.000000000000000000 ) ) ;
#1646=AXIS2_PLACEMENT_3D ( 'NONE', #1177, #1120, #3877 ) ;
#1647=DIRECTION ( 'NONE',  ( 0.000000000000000000, 0.000000000000000000, 1.000000000000000000 ) ) ;
#1648=VERTEX_POINT ( 'NONE', #195 ) ;
#1649=EDGE_CURVE ( 'NONE', #845, #11767, #5039, .T. ) ;
#1650=CARTESIAN_POINT ( 'NONE',  ( 3.000000000000000888, -21.30300407174357957, -7.402892494506506438 ) ) ;
#1651=ADVANCED_FACE ( 'NONE', ( #4059, #6690 ), #2970, .F. ) ;
#1652=DIRECTION ( 'NONE',  ( 0.000000000000000000, 0.9781476007338049117, 0.2079116908177629230 ) ) ;
#1654=CARTESIAN_POINT ( 'NONE',  ( 3.000000000000000888, -7.432877647175354596, 21.76479567747239230 ) ) ;
#1655=ORIENTED_EDGE ( 'NONE', *, *, #8174, .F. ) ;
#1656=CARTESIAN_POINT ( 'NONE',  ( 0.000000000000000000, -11.79560690673858403, -19.74380051311552364 ) ) ;
#1657=VERTEX_POINT ( 'NONE', #10608 ) ;
#1658=ORIENTED_EDGE ( 'NONE', *, *, #3965, .F. ) ;
#1661=DIRECTION ( 'NONE',  ( 0.000000000000000000, 0.000000000000000000, 1.000000000000000000 ) ) ;
#1662=ORIENTED_EDGE ( 'NONE', *, *, #12112, .F. ) ;
#1663=CARTESIAN_POINT ( 'NONE',  ( 3.000000000000000888, -13.72351598154911478, 20.65684170206486669 ) ) ;
#1664=DIRECTION ( 'NONE',  ( -1.000000000000000000, 0.000000000000000000, -0.000000000000000000 ) ) ;
#1666=DIRECTION ( 'NONE',  ( 0.000000000000000000, -0.7431448254773999063, 0.6691306063588519093 ) ) ;
#1667=CARTESIAN_POINT ( 'NONE',  ( 3.000000000000000888, 22.47229024614977533, 1.901833551798334909 ) ) ;
#1668=CYLINDRICAL_SURFACE ( 'NONE', #996, 9.599999999999999645 ) ;
#1669=ORIENTED_EDGE ( 'NONE', *, *, #4258, .F. ) ;
#1670=EDGE_CURVE ( 'NONE', #6927, #2739, #11924, .T. ) ;
#1673=DIRECTION ( 'NONE',  ( -1.000000000000000000, -0.000000000000000000, -0.000000000000000000 ) ) ;
#1674=CARTESIAN_POINT ( 'NONE',  ( 0.000000000000000000, 0.000000000000000000, 0.000000000000000000 ) ) ;
#1675=ORIENTED_EDGE ( 'NONE', *, *, #2091, .F. ) ;
#1676=ADVANCED_FACE ( 'NONE', ( #8720 ), #2103, .T. ) ;
#1677=DIRECTION ( 'NONE',  ( 0.000000000000000000, 0.4067366430758009854, -0.9135454576426006446 ) ) ;
#1678=DIRECTION ( 'NONE',  ( 0.000000000000000000, 0.000000000000000000, 1.000000000000000000 ) ) ;
#1680=AXIS2_PLACEMENT_3D ( 'NONE', #5953, #9680, #8767 ) ;
#1682=CARTESIAN_POINT ( 'NONE',  ( -10.00000000000000000, 0.000000000000000000, 0.000000000000000000 ) ) ;
#1683=CYLINDRICAL_SURFACE ( 'NONE', #7220, 9.599999999999999645 ) ;
#1684=EDGE_LOOP ( 'NONE', ( #2344, #3840, #4959, #5878 ) ) ;
#1685=EDGE_CURVE ( 'NONE', #6263, #6662, #11724, .T. ) ;
#1686=ORIENTED_EDGE ( 'NONE', *, *, #3487, .T. ) ;
#1687=ORIENTED_EDGE ( 'NONE', *, *, #8757, .T. ) ;
#1690=CYLINDRICAL_SURFACE ( 'NONE', #8580, 22.99899999999999878 ) ;
#1691=CARTESIAN_POINT ( 'NONE',  ( 0.000000000000000000, 0.000000000000000000, 0.000000000000000000 ) ) ;
#1694=VERTEX_POINT ( 'NONE', #7730 ) ;
#1695=CIRCLE ( 'NONE', #6958, 22.99899999999999878 ) ;
#1696=CARTESIAN_POINT ( 'NONE',  ( 0.000000000000000000, -20.08719549084872824, 11.20082935824068038 ) ) ;
#1697=ORIENTED_EDGE ( 'NONE', *, *, #3079, .F. ) ;
#1698=EDGE_LOOP ( 'NONE', ( #10381, #4428, #11078, #5847 ) ) ;
#1699=DIRECTION ( 'NONE',  ( -1.000000000000000000, 0.000000000000000000, 0.000000000000000000 ) ) ;
#1700=CARTESIAN_POINT ( 'NONE',  ( 3.000000000000000888, -24.45282072769603587, 4.135161237383499611 ) ) ;
#1701=DIRECTION ( 'NONE',  ( 0.000000000000000000, -0.9510565162951565288, 0.3090169943749382364 ) ) ;
#1702=DIRECTION ( 'NONE',  ( -1.000000000000000000, -0.000000000000000000, -0.000000000000000000 ) ) ;
#1703=DIRECTION ( 'NONE',  ( 0.000000000000000000, 0.9945218953682729568, 0.1045284632676570929 ) ) ;
#1704=CARTESIAN_POINT ( 'NONE',  ( 0.000000000000000000, -22.54798042742717357, 9.142421143074578538 ) ) ;
#1705=DIRECTION ( 'NONE',  ( 0.000000000000000000, 0.8660254037844400399, -0.4999999999999978906 ) ) ;
#1707=CARTESIAN_POINT ( 'NONE',  ( 1.500000000000000444, 21.97817939804039611, 11.48910920600691732 ) ) ;
#1708=ORIENTED_EDGE ( 'NONE', *, *, #5083, .T. ) ;
#1710=ORIENTED_EDGE ( 'NONE', *, *, #8972, .F. ) ;
#1712=EDGE_CURVE ( 'NONE', #2147, #4846, #5476, .T. ) ;
#1713=DIRECTION ( 'NONE',  ( -1.000000000000000000, -0.000000000000000000, 0.000000000000000000 ) ) ;
#1714=ORIENTED_EDGE ( 'NONE', *, *, #10084, .T. ) ;
#1715=EDGE_CURVE ( 'NONE', #8966, #1364, #9588, .T. ) ;
#1716=DIRECTION ( 'NONE',  ( 0.000000000000000000, -0.7431448254773999063, 0.6691306063588519093 ) ) ;
#1717=DIRECTION ( 'NONE',  ( -1.000000000000000000, -0.000000000000000000, -0.000000000000000000 ) ) ;
#1719=AXIS2_PLACEMENT_3D ( 'NONE', #5033, #6010, #5893 ) ;
#1720=CARTESIAN_POINT ( 'NONE',  ( 0.000000000000000000, -20.41249101028218149, 9.589108953447823325 ) ) ;
#1721=VERTEX_POINT ( 'NONE', #135 ) ;
#1722=DIRECTION ( 'NONE',  ( 0.000000000000000000, 0.9510565162951543083, -0.3090169943749450643 ) ) ;
#1723=EDGE_LOOP ( 'NONE', ( #5800, #6317, #4097, #7504 ) ) ;
#1727=CARTESIAN_POINT ( 'NONE',  ( 3.000000000000000888, -2.811977935937640005, -22.37663021667346896 ) ) ;
#1728=CARTESIAN_POINT ( 'NONE',  ( 0.000000000000000000, 6.668524164681629784, 23.88662356770117512 ) ) ;
#1729=CYLINDRICAL_SURFACE ( 'NONE', #9021, 9.599999999999997868 ) ;
#1730=DIRECTION ( 'NONE',  ( 0.000000000000000000, 0.5877852522924741363, -0.8090169943749467851 ) ) ;
#1731=DIRECTION ( 'NONE',  ( -1.000000000000000000, 0.000000000000000000, -0.000000000000000000 ) ) ;
#1732=ADVANCED_FACE ( 'NONE', ( #9631 ), #263, .T. ) ;
#1734=CARTESIAN_POINT ( 'NONE',  ( 0.000000000000000000, 0.000000000000000000, 0.000000000000000000 ) ) ;
#1735=CIRCLE ( 'NONE', #2120, 4.000000000000000000 ) ;
#1736=DIRECTION ( 'NONE',  ( 0.000000000000000000, 0.000000000000000000, 1.000000000000000000 ) ) ;
#1738=EDGE_CURVE ( 'NONE', #5993, #4594, #9452, .T. ) ;
#1745=AXIS2_PLACEMENT_3D ( 'NONE', #8867, #1394, #470 ) ;
#1747=LINE ( 'NONE', #11244, #3378 ) ;
#1749=CARTESIAN_POINT ( 'NONE',  ( 1.499999999999999556, -6.668524164681792321, 23.88662356770113249 ) ) ;
#1750=ADVANCED_FACE ( 'NONE', ( #6806 ), #4985, .T. ) ;
#1751=VERTEX_POINT ( 'NONE', #3947 ) ;
#1752=VERTEX_POINT ( 'NONE', #1304 ) ;
#1753=AXIS2_PLACEMENT_3D ( 'NONE', #8898, #6983, #1486 ) ;
#1754=ORIENTED_EDGE ( 'NONE', *, *, #2693, .F. ) ;
#1755=DIRECTION ( 'NONE',  ( 0.000000000000000000, 0.000000000000000000, 1.000000000000000000 ) ) ;
#1756=CARTESIAN_POINT ( 'NONE',  ( 1.500000000000000444, -21.97817939804047427, 11.48910920600676278 ) ) ;
#1758=CYLINDRICAL_SURFACE ( 'NONE', #5639, 22.99899999999999878 ) ;
#1760=AXIS2_PLACEMENT_3D ( 'NONE', #9269, #3584, #4744 ) ;
#1762=CIRCLE ( 'NONE', #4121, 9.599999999999996092 ) ;
#1766=DIRECTION ( 'NONE',  ( -1.000000000000000000, 0.000000000000000000, -0.000000000000000000 ) ) ;
#1767=ORIENTED_EDGE ( 'NONE', *, *, #10478, .T. ) ;
#1768=VERTEX_POINT ( 'NONE', #10670 ) ;
#1770=CIRCLE ( 'NONE', #10376, 9.599999999999997868 ) ;
#1771=ORIENTED_EDGE ( 'NONE', *, *, #1917, .F. ) ;
#1772=ORIENTED_EDGE ( 'NONE', *, *, #2240, .F. ) ;
#1774=AXIS2_PLACEMENT_3D ( 'NONE', #10838, #8885, #1412 ) ;
#1775=CARTESIAN_POINT ( 'NONE',  ( 3.000000000000000888, 0.000000000000000000, 0.000000000000000000 ) ) ;
#1776=ORIENTED_EDGE ( 'NONE', *, *, #1341, .F. ) ;
#1778=CARTESIAN_POINT ( 'NONE',  ( 3.000000000000000888, 0.000000000000000000, 0.000000000000000000 ) ) ;
#1780=AXIS2_PLACEMENT_3D ( 'NONE', #8730, #10620, #390 ) ;
#1781=CIRCLE ( 'NONE', #4917, 19.99999999999999645 ) ;
#1782=CARTESIAN_POINT ( 'NONE',  ( 3.000000000000000888, 0.000000000000000000, 0.000000000000000000 ) ) ;
#1783=VECTOR ( 'NONE', #9935, 1000.000000000000000 ) ;
#1784=AXIS2_PLACEMENT_3D ( 'NONE', #280, #5923, #2119 ) ;
#1785=CARTESIAN_POINT ( 'NONE',  ( 0.000000000000000000, 0.000000000000000000, 0.000000000000000000 ) ) ;
#1786=ORIENTED_EDGE ( 'NONE', *, *, #11985, .T. ) ;
#1788=DIRECTION ( 'NONE',  ( -1.000000000000000000, 0.000000000000000000, -0.000000000000000000 ) ) ;
#1791=EDGE_CURVE ( 'NONE', #10729, #10168, #4304, .T. ) ;
#1792=DIRECTION ( 'NONE',  ( -1.000000000000000000, -0.000000000000000000, -0.000000000000000000 ) ) ;
#1793=AXIS2_PLACEMENT_3D ( 'NONE', #1469, #8995, #9792 ) ;
#1794=DIRECTION ( 'NONE',  ( 0.000000000000000000, 0.000000000000000000, 1.000000000000000000 ) ) ;
#1795=LINE ( 'NONE', #6271, #11992 ) ;
#1797=EDGE_CURVE ( 'NONE', #5220, #2390, #6079, .T. ) ;
#1799=CARTESIAN_POINT ( 'NONE',  ( 0.000000000000000000, 0.000000000000000000, 0.000000000000000000 ) ) ;
#1800=EDGE_CURVE ( 'NONE', #4256, #411, #6650, .T. ) ;
#1801=VECTOR ( 'NONE', #10905, 1000.000000000000000 ) ;
#1802=FACE_OUTER_BOUND ( 'NONE', #604, .T. ) ;
#1803=VECTOR ( 'NONE', #243, 1000.000000000000000 ) ;
#1804=VERTEX_POINT ( 'NONE', #6200 ) ;
#1805=ADVANCED_FACE ( 'NONE', ( #11823 ), #10906, .T. ) ;
#1806=VECTOR ( 'NONE', #4300, 1000.000000000000000 ) ;
#1807=ORIENTED_EDGE ( 'NONE', *, *, #8560, .T. ) ;
#1808=CARTESIAN_POINT ( 'NONE',  ( 3.000000000000000888, 18.80635025205187816, -13.23915371906935867 ) ) ;
#1810=DIRECTION ( 'NONE',  ( -1.000000000000000000, 0.000000000000000000, -0.000000000000000000 ) ) ;
#1813=LINE ( 'NONE', #29, #6233 ) ;
#1815=DIRECTION ( 'NONE',  ( -1.000000000000000000, 0.000000000000000000, -0.000000000000000000 ) ) ;
#1816=CARTESIAN_POINT ( 'NONE',  ( 1.499999999999999556, 9.128825345753025289, 23.05871956130125611 ) ) ;
#1817=ORIENTED_EDGE ( 'NONE', *, *, #4224, .F. ) ;
#1819=ORIENTED_EDGE ( 'NONE', *, *, #4948, .T. ) ;
#1820=ORIENTED_EDGE ( 'NONE', *, *, #10170, .T. ) ;
#1821=LINE ( 'NONE', #5560, #2215 ) ;
#1822=AXIS2_PLACEMENT_3D ( 'NONE', #3542, #5380, #3360 ) ;
#1823=VECTOR ( 'NONE', #2939, 1000.000000000000000 ) ;
#1824=CARTESIAN_POINT ( 'NONE',  ( 3.000000000000000888, 0.000000000000000000, 0.000000000000000000 ) ) ;
#1827=FACE_OUTER_BOUND ( 'NONE', #3222, .T. ) ;
#1828=EDGE_CURVE ( 'NONE', #4090, #1430, #9987, .T. ) ;
#1829=CYLINDRICAL_SURFACE ( 'NONE', #3983, 22.99899999999999878 ) ;
#1832=DIRECTION ( 'NONE',  ( -1.000000000000000000, -0.000000000000000000, -0.000000000000000000 ) ) ;
#1833=VERTEX_POINT ( 'NONE', #9925 ) ;
#1834=ORIENTED_EDGE ( 'NONE', *, *, #1494, .T. ) ;
#1835=DIRECTION ( 'NONE',  ( 0.000000000000000000, 0.000000000000000000, -1.000000000000000000 ) ) ;
#1836=EDGE_CURVE ( 'NONE', #7635, #8246, #9077, .T. ) ;
#1837=ORIENTED_EDGE ( 'NONE', *, *, #5702, .T. ) ;
#1838=AXIS2_PLACEMENT_3D ( 'NONE', #7608, #1076, #11240 ) ;
#1839=AXIS2_PLACEMENT_3D ( 'NONE', #10180, #12015, #7172 ) ;
#1840=ORIENTED_EDGE ( 'NONE', *, *, #11141, .T. ) ;
#1842=DIRECTION ( 'NONE',  ( -1.000000000000000000, 0.000000000000000000, 0.000000000000000000 ) ) ;
#1847=CIRCLE ( 'NONE', #6534, 9.599999999999997868 ) ;
#1848=CARTESIAN_POINT ( 'NONE',  ( 3.000000000000000888, -20.08719549084872824, 11.20082935824068038 ) ) ;
#1849=DIRECTION ( 'NONE',  ( 0.000000000000000000, 0.3090169943749415671, 0.9510565162951555296 ) ) ;
#1850=DIRECTION ( 'NONE',  ( -1.000000000000000000, -0.000000000000000000, -0.000000000000000000 ) ) ;
#1851=VERTEX_POINT ( 'NONE', #11700 ) ;
#1853=CARTESIAN_POINT ( 'NONE',  ( 3.000000000000000888, 7.402892494506291499, 21.30300407174365063 ) ) ;
#1856=AXIS2_PLACEMENT_3D ( 'NONE', #1538, #1904, #11391 ) ;
#1858=DIRECTION ( 'NONE',  ( -1.000000000000000000, 0.000000000000000000, 0.000000000000000000 ) ) ;
#1859=LINE ( 'NONE', #2901, #11618 ) ;
#1860=CARTESIAN_POINT ( 'NONE',  ( 3.000000000000000000, 0.000000000000000000, 0.000000000000000000 ) ) ;
#1862=CARTESIAN_POINT ( 'NONE',  ( 0.000000000000000000, -15.64281154287585807, -16.85990652506916021 ) ) ;
#1863=ORIENTED_EDGE ( 'NONE', *, *, #2587, .T. ) ;
#1864=VERTEX_POINT ( 'NONE', #9873 ) ;
#1865=EDGE_CURVE ( 'NONE', #4536, #2001, #7627, .T. ) ;
#1866=CARTESIAN_POINT ( 'NONE',  ( 1.500000000000000444, -20.65684170206500170, 13.72351598154890873 ) ) ;
#1868=ADVANCED_FACE ( 'NONE', ( #5219 ), #8152, .T. ) ;
#1869=CARTESIAN_POINT ( 'NONE',  ( 1.499999999999999556, 22.21333432029578603, -11.02759168516723065 ) ) ;
#1870=CARTESIAN_POINT ( 'NONE',  ( 3.000000000000000888, -15.13242714128107913, -17.31945870441162683 ) ) ;
#1871=DIRECTION ( 'NONE',  ( 0.000000000000000000, 0.000000000000000000, 1.000000000000000000 ) ) ;
#1872=AXIS2_PLACEMENT_3D ( 'NONE', #1310, #9877, #6152 ) ;
#1873=EDGE_CURVE ( 'NONE', #9943, #8329, #2159, .T. ) ;
#1874=ADVANCED_FACE ( 'NONE', ( #5347 ), #5159, .T. ) ;
#1876=CARTESIAN_POINT ( 'NONE',  ( 3.000000000000000888, -21.30300407174367905, 7.402892494506218668 ) ) ;
#1877=CARTESIAN_POINT ( 'NONE',  ( 1.499999999999999556, 23.88662356770124262, -6.668524164681381095 ) ) ;
#1878=ORIENTED_EDGE ( 'NONE', *, *, #2996, .T. ) ;
#1879=ORIENTED_EDGE ( 'NONE', *, *, #10996, .T. ) ;
#1880=ORIENTED_EDGE ( 'NONE', *, *, #10259, .T. ) ;
#1881=VERTEX_POINT ( 'NONE', #1362 ) ;
#1882=EDGE_CURVE ( 'NONE', #4541, #3273, #3926, .T. ) ;
#1883=DIRECTION ( 'NONE',  ( 0.000000000000000000, 0.3090169943749479509, -0.9510565162951534202 ) ) ;
#1884=CYLINDRICAL_SURFACE ( 'NONE', #10765, 9.599999999999997868 ) ;
#1885=DIRECTION ( 'NONE',  ( 0.000000000000000000, 0.000000000000000000, -1.000000000000000000 ) ) ;
#1886=CARTESIAN_POINT ( 'NONE',  ( 3.000000000000000888, 22.47229024614980020, -1.901833551798019162 ) ) ;
#1887=DIRECTION ( 'NONE',  ( 1.000000000000000000, 0.000000000000000000, 0.000000000000000000 ) ) ;
#1888=VECTOR ( 'NONE', #9428, 1000.000000000000000 ) ;
#1891=ADVANCED_FACE ( 'NONE', ( #4240 ), #1543, .T. ) ;
#1892=DIRECTION ( 'NONE',  ( 0.000000000000000000, 0.000000000000000000, 1.000000000000000000 ) ) ;
#1893=ORIENTED_EDGE ( 'NONE', *, *, #10184, .T. ) ;
#1894=ORIENTED_EDGE ( 'NONE', *, *, #8228, .T. ) ;
#1895=DIRECTION ( 'NONE',  ( 0.000000000000000000, 0.000000000000000000, 1.000000000000000000 ) ) ;
#1896=VERTEX_POINT ( 'NONE', #3508 ) ;
#1897=ADVANCED_FACE ( 'NONE', ( #4185 ), #6017, .T. ) ;
#1899=CARTESIAN_POINT ( 'NONE',  ( 3.000000000000000888, 0.000000000000000000, 0.000000000000000000 ) ) ;
#1900=FACE_OUTER_BOUND ( 'NONE', #10052, .T. ) ;
#1901=EDGE_LOOP ( 'NONE', ( #10810, #447, #290, #2117 ) ) ;
#1902=DIRECTION ( 'NONE',  ( -1.000000000000000000, 0.000000000000000000, -0.000000000000000000 ) ) ;
#1903=EDGE_CURVE ( 'NONE', #1167, #6070, #1966, .T. ) ;
#1904=DIRECTION ( 'NONE',  ( -1.000000000000000000, -0.000000000000000000, 0.000000000000000000 ) ) ;
#1906=DIRECTION ( 'NONE',  ( 1.000000000000000000, 0.000000000000000000, 0.000000000000000000 ) ) ;
#1907=CARTESIAN_POINT ( 'NONE',  ( 0.000000000000000000, -4.135161237383401911, -24.45282072769605364 ) ) ;
#1908=AXIS2_PLACEMENT_3D ( 'NONE', #3517, #10863, #1677 ) ;
#1909=DIRECTION ( 'NONE',  ( -1.000000000000000000, -0.000000000000000000, 0.000000000000000000 ) ) ;
#1910=VERTEX_POINT ( 'NONE', #7912 ) ;
#1912=VERTEX_POINT ( 'NONE', #3321 ) ;
#1914=CARTESIAN_POINT ( 'NONE',  ( 3.000000000000000888, -22.37663021667346186, 2.811977935937707063 ) ) ;
#1915=AXIS2_PLACEMENT_3D ( 'NONE', #4053, #11517, #11693 ) ;
#1916=DIRECTION ( 'NONE',  ( -1.000000000000000000, -0.000000000000000000, -0.000000000000000000 ) ) ;
#1917=EDGE_CURVE ( 'NONE', #862, #7927, #2364, .T. ) ;
#1918=CARTESIAN_POINT ( 'NONE',  ( 3.000000000000000888, -9.667200211209964422, 20.86861857134731579 ) ) ;
#1921=CARTESIAN_POINT ( 'NONE',  ( 0.000000000000000000, 18.40266524480588473, 13.79477846460802226 ) ) ;
#1922=DIRECTION ( 'NONE',  ( -1.000000000000000000, 0.000000000000000000, 0.000000000000000000 ) ) ;
#1923=ORIENTED_EDGE ( 'NONE', *, *, #5774, .T. ) ;
#1924=AXIS2_PLACEMENT_3D ( 'NONE', #343, #5983, #9767 ) ;
#1925=VECTOR ( 'NONE', #3531, 1000.000000000000000 ) ;
#1926=ORIENTED_EDGE ( 'NONE', *, *, #5951, .F. ) ;
#1927=CYLINDRICAL_SURFACE ( 'NONE', #5822, 24.80000000000000071 ) ;
#1929=DIRECTION ( 'NONE',  ( -1.000000000000000000, -0.000000000000000000, -0.000000000000000000 ) ) ;
#1931=AXIS2_PLACEMENT_3D ( 'NONE', #9338, #8429, #3711 ) ;
#1932=AXIS2_PLACEMENT_3D ( 'NONE', #6931, #3095, #6814 ) ;
#1934=DIRECTION ( 'NONE',  ( -1.000000000000000000, 0.000000000000000000, 0.000000000000000000 ) ) ;
#1935=ORIENTED_EDGE ( 'NONE', *, *, #72, .F. ) ;
#1936=VERTEX_POINT ( 'NONE', #6982 ) ;
#1937=ORIENTED_EDGE ( 'NONE', *, *, #6948, .F. ) ;
#1938=EDGE_CURVE ( 'NONE', #401, #1454, #7836, .T. ) ;
#1939=ORIENTED_EDGE ( 'NONE', *, *, #3598, .T. ) ;
#1941=AXIS2_PLACEMENT_3D ( 'NONE', #850, #11123, #2811 ) ;
#1942=DIRECTION ( 'NONE',  ( 1.000000000000000000, 0.000000000000000000, 0.000000000000000000 ) ) ;
#1943=EDGE_CURVE ( 'NONE', #6070, #10397, #9210, .T. ) ;
#1944=CYLINDRICAL_SURFACE ( 'NONE', #12102, 9.599999999999997868 ) ;
#1945=FACE_OUTER_BOUND ( 'NONE', #10754, .T. ) ;
#1946=DIRECTION ( 'NONE',  ( -1.000000000000000000, -0.000000000000000000, 0.000000000000000000 ) ) ;
#1948=CARTESIAN_POINT ( 'NONE',  ( 0.000000000000000000, 0.000000000000000000, 0.000000000000000000 ) ) ;
#1949=ADVANCED_FACE ( 'NONE', ( #9315 ), #9130, .T. ) ;
#1950=EDGE_CURVE ( 'NONE', #5661, #11556, #1770, .T. ) ;
#1951=LINE ( 'NONE', #11378, #8221 ) ;
#1952=ORIENTED_EDGE ( 'NONE', *, *, #5226, .F. ) ;
#1953=ORIENTED_EDGE ( 'NONE', *, *, #7931, .F. ) ;
#1956=CARTESIAN_POINT ( 'NONE',  ( 0.000000000000000000, 7.432877647175492264, -21.76479567747234256 ) ) ;
#1957=VECTOR ( 'NONE', #8675, 1000.000000000000000 ) ;
#1958=LINE ( 'NONE', #5700, #1888 ) ;
#1960=AXIS2_PLACEMENT_3D ( 'NONE', #10366, #10075, #8245 ) ;
#1962=FACE_OUTER_BOUND ( 'NONE', #472, .T. ) ;
#1964=EDGE_CURVE ( 'NONE', #1098, #9240, #601, .T. ) ;
#1965=LINE ( 'NONE', #1108, #1614 ) ;
#1966=CIRCLE ( 'NONE', #804, 9.599999999999996092 ) ;
#1967=DIRECTION ( 'NONE',  ( 0.000000000000000000, -0.8090169943749407899, -0.5877852522924824630 ) ) ;
#1968=ORIENTED_EDGE ( 'NONE', *, *, #9908, .F. ) ;
#1969=ORIENTED_EDGE ( 'NONE', *, *, #1273, .T. ) ;
#1970=CARTESIAN_POINT ( 'NONE',  ( 3.000000000000000888, 22.54798042742718067, 9.142421143074731305 ) ) ;
#1971=VECTOR ( 'NONE', #5712, 1000.000000000000000 ) ;
#1972=VERTEX_POINT ( 'NONE', #7406 ) ;
#1974=DIRECTION ( 'NONE',  ( 0.000000000000000000, -0.5000000000000072164, 0.8660254037844344888 ) ) ;
#1976=ORIENTED_EDGE ( 'NONE', *, *, #8938, .F. ) ;
#1977=AXIS2_PLACEMENT_3D ( 'NONE', #12060, #5523, #3627 ) ;
#1978=LINE ( 'NONE', #1176, #2690 ) ;
#1979=VECTOR ( 'NONE', #12029, 1000.000000000000000 ) ;
#1980=DIRECTION ( 'NONE',  ( -1.000000000000000000, 0.000000000000000000, 0.000000000000000000 ) ) ;
#1981=DIRECTION ( 'NONE',  ( 0.000000000000000000, 0.000000000000000000, 1.000000000000000000 ) ) ;
#1982=EDGE_CURVE ( 'NONE', #11898, #12091, #9401, .T. ) ;
#1983=CYLINDRICAL_SURFACE ( 'NONE', #4542, 22.99899999999999878 ) ;
#1984=CARTESIAN_POINT ( 'NONE',  ( 3.000000000000000888, 0.000000000000000000, 0.000000000000000000 ) ) ;
#1985=DIRECTION ( 'NONE',  ( -1.000000000000000000, -0.000000000000000000, 0.000000000000000000 ) ) ;
#1986=DIRECTION ( 'NONE',  ( 0.000000000000000000, -0.9781476007338079093, 0.2079116908177492118 ) ) ;
#1988=VECTOR ( 'NONE', #4940, 1000.000000000000000 ) ;
#1989=EDGE_CURVE ( 'NONE', #10458, #1768, #9984, .T. ) ;
#1990=AXIS2_PLACEMENT_3D ( 'NONE', #9826, #9644, #11479 ) ;
#1991=ORIENTED_EDGE ( 'NONE', *, *, #8419, .T. ) ;
#1992=DIRECTION ( 'NONE',  ( -1.000000000000000000, 0.000000000000000000, 0.000000000000000000 ) ) ;
#1994=DIRECTION ( 'NONE',  ( 1.000000000000000000, -0.000000000000000000, -0.000000000000000000 ) ) ;
#1995=COLOUR_RGB ( '', 0.09019608, 0.27058824, 0.51372549) ;
#1998=FACE_OUTER_BOUND ( 'NONE', #612, .T. ) ;
#1999=ORIENTED_EDGE ( 'NONE', *, *, #12034, .F. ) ;
#2000=ORIENTED_EDGE ( 'NONE', *, *, #10571, .T. ) ;
#2001=VERTEX_POINT ( 'NONE', #1907 ) ;
#2002=DIRECTION ( 'NONE',  ( 1.000000000000000000, -0.000000000000000000, -0.000000000000000000 ) ) ;
#2003=CIRCLE ( 'NONE', #240, 22.99899999999999523 ) ;
#2004=DIRECTION ( 'NONE',  ( 1.000000000000000000, 0.000000000000000000, 0.000000000000000000 ) ) ;
#2005=VERTEX_POINT ( 'NONE', #11088 ) ;
#2006=DIRECTION ( 'NONE',  ( 0.000000000000000000, 0.000000000000000000, 1.000000000000000000 ) ) ;
#2007=CARTESIAN_POINT ( 'NONE',  ( 3.000000000000000888, -22.42251312757882786, 5.117118920208413968 ) ) ;
#2008=DIRECTION ( 'NONE',  ( 0.000000000000000000, 0.000000000000000000, 1.000000000000000000 ) ) ;
#2011=DIRECTION ( 'NONE',  ( -1.000000000000000000, 0.000000000000000000, 0.000000000000000000 ) ) ;
#2013=ORIENTED_EDGE ( 'NONE', *, *, #8582, .T. ) ;
#2014=ORIENTED_EDGE ( 'NONE', *, *, #6579, .T. ) ;
#2015=AXIS2_PLACEMENT_3D ( 'NONE', #5362, #10868, #576 ) ;
#2016=DIRECTION ( 'NONE',  ( 0.000000000000000000, 0.000000000000000000, 1.000000000000000000 ) ) ;
#2017=ORIENTED_EDGE ( 'NONE', *, *, #3256, .T. ) ;
#2018=DIRECTION ( 'NONE',  ( -1.000000000000000000, -0.000000000000000000, 0.000000000000000000 ) ) ;
#2020=DIRECTION ( 'NONE',  ( -1.000000000000000000, 0.000000000000000000, -0.000000000000000000 ) ) ;
#2022=EDGE_CURVE ( 'NONE', #8329, #2802, #2767, .T. ) ;
#2023=LINE ( 'NONE', #1051, #9639 ) ;
#2024=CIRCLE ( 'NONE', #7286, 9.599999999999997868 ) ;
#2026=CARTESIAN_POINT ( 'NONE',  ( 3.000000000000000888, 20.86861857134747922, -9.667200211209612704 ) ) ;
#2028=CYLINDRICAL_SURFACE ( 'NONE', #8632, 9.599999999999997868 ) ;
#2029=CYLINDRICAL_SURFACE ( 'NONE', #1026, 24.80000000000000071 ) ;
#2030=AXIS2_PLACEMENT_3D ( 'NONE', #2475, #10803, #5807 ) ;
#2032=ORIENTED_EDGE ( 'NONE', *, *, #8017, .T. ) ;
#2034=ORIENTED_EDGE ( 'NONE', *, *, #11659, .T. ) ;
#2036=ADVANCED_FACE ( 'NONE', ( #2833 ), #6326, .T. ) ;
#2037=DIRECTION ( 'NONE',  ( -1.000000000000000000, 0.000000000000000000, 0.000000000000000000 ) ) ;
#2040=ORIENTED_EDGE ( 'NONE', *, *, #11742, .T. ) ;
#2041=AXIS2_PLACEMENT_3D ( 'NONE', #1068, #2043, #5654 ) ;
#2042=DIRECTION ( 'NONE',  ( -1.000000000000000000, -0.000000000000000000, 0.000000000000000000 ) ) ;
#2043=DIRECTION ( 'NONE',  ( 1.000000000000000000, 0.000000000000000000, 0.000000000000000000 ) ) ;
#2045=CARTESIAN_POINT ( 'NONE',  ( 0.000000000000000000, -21.14796121233190362, -9.039786367039052806 ) ) ;
#2046=CARTESIAN_POINT ( 'NONE',  ( 1.500000000000000444, -24.77821629063820907, -1.039229259764747004 ) ) ;
#2047=CARTESIAN_POINT ( 'NONE',  ( 3.000000000000000888, 6.779701584702736206, 21.97702544527760082 ) ) ;
#2048=EDGE_CURVE ( 'NONE', #7011, #246, #10570, .T. ) ;
#2049=DIRECTION ( 'NONE',  ( 1.000000000000000000, -0.000000000000000000, 0.000000000000000000 ) ) ;
#2051=ORIENTED_EDGE ( 'NONE', *, *, #7677, .T. ) ;
#2052=EDGE_CURVE ( 'NONE', #2472, #5179, #7, .T. ) ;
#2053=CARTESIAN_POINT ( 'NONE',  ( 0.000000000000000000, 15.13242714128119459, 17.31945870441152380 ) ) ;
#2055=CARTESIAN_POINT ( 'NONE',  ( 3.000000000000000888, 20.41249101028211754, -9.589108953447965433 ) ) ;
#2058=EDGE_CURVE ( 'NONE', #8966, #3995, #7638, .T. ) ;
#2059=DIRECTION ( 'NONE',  ( 0.000000000000000000, 0.4999999999999950040, 0.8660254037844415942 ) ) ;
#2060=EDGE_LOOP ( 'NONE', ( #4600, #1218, #10442, #2040 ) ) ;
#2061=VERTEX_POINT ( 'NONE', #5643 ) ;
#2063=CIRCLE ( 'NONE', #3232, 24.80000000000000071 ) ;
#2064=LINE ( 'NONE', #10323, #4912 ) ;
#2065=ORIENTED_EDGE ( 'NONE', *, *, #4728, .T. ) ;
#2066=DIRECTION ( 'NONE',  ( -1.000000000000000000, 0.000000000000000000, 0.000000000000000000 ) ) ;
#2068=ADVANCED_FACE ( 'NONE', ( #9373 ), #808, .T. ) ;
#2069=DIRECTION ( 'NONE',  ( 0.000000000000000000, 0.4067366430757948792, 0.9135454576426033091 ) ) ;
#2073=VERTEX_POINT ( 'NONE', #7531 ) ;
#2074=ORIENTED_EDGE ( 'NONE', *, *, #7931, .T. ) ;
#2078=CARTESIAN_POINT ( 'NONE',  ( 3.000000000000000888, -6.168200451485917668, 24.02068490260610645 ) ) ;
#2079=LINE ( 'NONE', #5816, #7884 ) ;
#2080=CARTESIAN_POINT ( 'NONE',  ( 3.000000000000000888, 0.000000000000000000, 0.000000000000000000 ) ) ;
#2081=AXIS2_PLACEMENT_3D ( 'NONE', #4601, #11754, #9123 ) ;
#2082=VERTEX_POINT ( 'NONE', #2592 ) ;
#2084=DIRECTION ( 'NONE',  ( 0.000000000000000000, 0.9945218953682729568, 0.1045284632676570929 ) ) ;
#2087=ORIENTED_EDGE ( 'NONE', *, *, #9712, .T. ) ;
#2088=CARTESIAN_POINT ( 'NONE',  ( 3.000000000000000888, 19.75591328264900781, -10.87771529938142123 ) ) ;
#2090=CARTESIAN_POINT ( 'NONE',  ( 1.499999999999999556, -20.93895013827591001, 13.28910708463121360 ) ) ;
#2091=EDGE_CURVE ( 'NONE', #712, #429, #743, .T. ) ;
#2092=ORIENTED_EDGE ( 'NONE', *, *, #6618, .T. ) ;
#2093=ADVANCED_FACE ( 'NONE', ( #11034 ), #10103, .T. ) ;
#2095=CARTESIAN_POINT ( 'NONE',  ( 3.000000000000000888, 21.30300407174352983, 7.402892494506653875 ) ) ;
#2097=DIRECTION ( 'NONE',  ( -1.000000000000000000, 0.000000000000000000, 0.000000000000000000 ) ) ;
#2098=DIRECTION ( 'NONE',  ( 0.000000000000000000, 0.4067366430757948792, 0.9135454576426033091 ) ) ;
#2100=DIRECTION ( 'NONE',  ( 0.000000000000000000, -0.9510565162951504226, -0.3090169943749574433 ) ) ;
#2103=CYLINDRICAL_SURFACE ( 'NONE', #8012, 19.99999999999999645 ) ;
#2104=VERTEX_POINT ( 'NONE', #9619 ) ;
#2105=DIRECTION ( 'NONE',  ( 0.000000000000000000, -0.2079116908177665313, 0.9781476007338041345 ) ) ;
#2106=ADVANCED_FACE ( 'NONE', ( #3927 ), #5026, .T. ) ;
#2107=ORIENTED_EDGE ( 'NONE', *, *, #4414, .T. ) ;
#2108=VECTOR ( 'NONE', #3820, 1000.000000000000000 ) ;
#2109=DIRECTION ( 'NONE',  ( 0.000000000000000000, 0.000000000000000000, 1.000000000000000000 ) ) ;
#2111=DIRECTION ( 'NONE',  ( 1.000000000000000000, 0.000000000000000000, 0.000000000000000000 ) ) ;
#2114=DIRECTION ( 'NONE',  ( -1.000000000000000000, 0.000000000000000000, 0.000000000000000000 ) ) ;
#2115=EDGE_CURVE ( 'NONE', #2610, #9943, #1189, .T. ) ;
#2116=ORIENTED_EDGE ( 'NONE', *, *, #10951, .F. ) ;
#2117=ORIENTED_EDGE ( 'NONE', *, *, #2320, .T. ) ;
#2119=DIRECTION ( 'NONE',  ( 0.000000000000000000, -0.6691306063588644548, 0.7431448254773886930 ) ) ;
#2120=AXIS2_PLACEMENT_3D ( 'NONE', #3280, #5240, #11722 ) ;
#2121=FACE_OUTER_BOUND ( 'NONE', #9248, .T. ) ;
#2122=CYLINDRICAL_SURFACE ( 'NONE', #6223, 24.80000000000000071 ) ;
#2123=CIRCLE ( 'NONE', #11311, 9.599999999999996092 ) ;
#2125=EDGE_CURVE ( 'NONE', #6397, #4202, #122, .T. ) ;
#2127=AXIS2_PLACEMENT_3D ( 'NONE', #12096, #12038, #11690 ) ;
#2128=ORIENTED_EDGE ( 'NONE', *, *, #3793, .F. ) ;
#2132=VERTEX_POINT ( 'NONE', #6613 ) ;
#2133=DIRECTION ( 'NONE',  ( 0.000000000000000000, 0.000000000000000000, 1.000000000000000000 ) ) ;
#2135=ADVANCED_FACE ( 'NONE', ( #7770, #180 ), #7655, .T. ) ;
#2136=CARTESIAN_POINT ( 'NONE',  ( 1.500000000000000444, 11.48910920600714469, -21.97817939804027176 ) ) ;
#2137=ORIENTED_EDGE ( 'NONE', *, *, #8799, .F. ) ;
#2138=CIRCLE ( 'NONE', #5658, 24.80000000000000071 ) ;
#2139=AXIS2_PLACEMENT_3D ( 'NONE', #7625, #2990, #6713 ) ;
#2140=CARTESIAN_POINT ( 'NONE',  ( 0.000000000000000000, -23.88662356770110762, -6.668524164681871369 ) ) ;
#2141=AXIS2_PLACEMENT_3D ( 'NONE', #5008, #11728, #7818 ) ;
#2142=DIRECTION ( 'NONE',  ( 0.000000000000000000, 0.000000000000000000, 1.000000000000000000 ) ) ;
#2144=CARTESIAN_POINT ( 'NONE',  ( 0.000000000000000000, -11.20082935824089354, 20.08719549084861455 ) ) ;
#2145=ORIENTED_EDGE ( 'NONE', *, *, #10045, .T. ) ;
#2147=VERTEX_POINT ( 'NONE', #6674 ) ;
#2148=ORIENTED_EDGE ( 'NONE', *, *, #10394, .F. ) ;
#2149=DIRECTION ( 'NONE',  ( -1.000000000000000000, 0.000000000000000000, -0.000000000000000000 ) ) ;
#2150=ORIENTED_EDGE ( 'NONE', *, *, #11846, .T. ) ;
#2156=DIRECTION ( 'NONE',  ( -1.000000000000000000, -0.000000000000000000, 0.000000000000000000 ) ) ;
#2157=FACE_OUTER_BOUND ( 'NONE', #1552, .T. ) ;
#2159=CIRCLE ( 'NONE', #11542, 9.599999999999997868 ) ;
#2160=FACE_OUTER_BOUND ( 'NONE', #70, .T. ) ;
#2161=CARTESIAN_POINT ( 'NONE',  ( 1.499999999999999556, 24.53384959170462665, -3.623565124516855640 ) ) ;
#2162=AXIS2_PLACEMENT_3D ( 'NONE', #8154, #7163, #4241 ) ;
#2163=DIRECTION ( 'NONE',  ( 0.000000000000000000, 0.000000000000000000, 1.000000000000000000 ) ) ;
#2164=CYLINDRICAL_SURFACE ( 'NONE', #8214, 22.99899999999999878 ) ;
#2165=ORIENTED_EDGE ( 'NONE', *, *, #2658, .T. ) ;
#2167=CARTESIAN_POINT ( 'NONE',  ( 3.000000000000000888, 22.54798042742718067, 9.142421143074731305 ) ) ;
#2169=VECTOR ( 'NONE', #11989, 1000.000000000000000 ) ;
#2170=ADVANCED_FACE ( 'NONE', ( #8646 ), #3073, .F. ) ;
#2171=DIRECTION ( 'NONE',  ( 0.000000000000000000, 0.000000000000000000, -1.000000000000000000 ) ) ;
#2172=EDGE_CURVE ( 'NONE', #1367, #5220, #2562, .T. ) ;
#2175=EDGE_CURVE ( 'NONE', #9118, #11061, #11358, .T. ) ;
#2176=DIRECTION ( 'NONE',  ( 0.000000000000000000, -0.9135454576426046414, 0.4067366430757920481 ) ) ;
#2177=CIRCLE ( 'NONE', #6094, 9.599999999999997868 ) ;
#2178=DIRECTION ( 'NONE',  ( -1.000000000000000000, 0.000000000000000000, -0.000000000000000000 ) ) ;
#2179=ORIENTED_EDGE ( 'NONE', *, *, #5689, .T. ) ;
#2180=VECTOR ( 'NONE', #8739, 1000.000000000000000 ) ;
#2181=EDGE_LOOP ( 'NONE', ( #5177, #2087, #5827, #4027 ) ) ;
#2184=VECTOR ( 'NONE', #3030, 1000.000000000000000 ) ;
#2186=FACE_OUTER_BOUND ( 'NONE', #645, .T. ) ;
#2188=AXIS2_PLACEMENT_3D ( 'NONE', #10952, #10274, #1892 ) ;
#2190=AXIS2_PLACEMENT_3D ( 'NONE', #6040, #9372, #7717 ) ;
#2192=ORIENTED_EDGE ( 'NONE', *, *, #9874, .F. ) ;
#2193=CIRCLE ( 'NONE', #8251, 22.99899999999999878 ) ;
#2194=ORIENTED_EDGE ( 'NONE', *, *, #8938, .T. ) ;
#2197=ORIENTED_EDGE ( 'NONE', *, *, #7960, .F. ) ;
#2198=CARTESIAN_POINT ( 'NONE',  ( 3.000000000000000888, 2.062268319295869290, -22.90635393027944033 ) ) ;
#2200=ADVANCED_FACE ( 'NONE', ( #6789 ), #5885, .T. ) ;
#2201=CYLINDRICAL_SURFACE ( 'NONE', #10292, 9.599999999999997868 ) ;
#2202=ORIENTED_EDGE ( 'NONE', *, *, #6230, .T. ) ;
#2203=CARTESIAN_POINT ( 'NONE',  ( 3.000000000000000888, 22.47229024614980020, -1.901833551798019162 ) ) ;
#2204=DIRECTION ( 'NONE',  ( -1.000000000000000000, -0.000000000000000000, -0.000000000000000000 ) ) ;
#2206=AXIS2_PLACEMENT_3D ( 'NONE', #1984, #11345, #133 ) ;
#2207=ORIENTED_EDGE ( 'NONE', *, *, #9421, .F. ) ;
#2208=ADVANCED_FACE ( 'NONE', ( #307 ), #9492, .T. ) ;
#2209=LINE ( 'NONE', #5710, #1 ) ;
#2210=EDGE_LOOP ( 'NONE', ( #4328, #11960, #9693, #7652 ) ) ;
#2211=CYLINDRICAL_SURFACE ( 'NONE', #6653, 24.80000000000000071 ) ;
#2212=VERTEX_POINT ( 'NONE', #364 ) ;
#2213=VECTOR ( 'NONE', #7893, 1000.000000000000000 ) ;
#2215=VECTOR ( 'NONE', #5616, 1000.000000000000000 ) ;
#2217=FACE_OUTER_BOUND ( 'NONE', #8088, .T. ) ;
#2219=DIRECTION ( 'NONE',  ( 0.000000000000000000, 0.000000000000000000, 1.000000000000000000 ) ) ;
#2220=EDGE_CURVE ( 'NONE', #10972, #4464, #2209, .T. ) ;
#2221=DIRECTION ( 'NONE',  ( -1.000000000000000000, 0.000000000000000000, 0.000000000000000000 ) ) ;
#2223=CIRCLE ( 'NONE', #8865, 22.99900000000000233 ) ;
#2224=DIRECTION ( 'NONE',  ( -1.000000000000000000, 0.000000000000000000, -0.000000000000000000 ) ) ;
#2227=DIRECTION ( 'NONE',  ( -1.000000000000000000, 0.000000000000000000, 0.000000000000000000 ) ) ;
#2228=ORIENTED_EDGE ( 'NONE', *, *, #3598, .F. ) ;
#2229=VERTEX_POINT ( 'NONE', #5948 ) ;
#2230=ORIENTED_EDGE ( 'NONE', *, *, #9945, .T. ) ;
#2231=AXIS2_PLACEMENT_3D ( 'NONE', #11166, #11341, #11286 ) ;
#2232=DIRECTION ( 'NONE',  ( 0.000000000000000000, 0.000000000000000000, 1.000000000000000000 ) ) ;
#2233=CYLINDRICAL_SURFACE ( 'NONE', #3504, 22.99899999999999878 ) ;
#2236=CIRCLE ( 'NONE', #2632, 22.99899999999999878 ) ;
#2237=CARTESIAN_POINT ( 'NONE',  ( 3.000000000000000888, -18.51065745848386968, 12.88318129270172818 ) ) ;
#2239=ORIENTED_EDGE ( 'NONE', *, *, #1092, .T. ) ;
#2240=EDGE_CURVE ( 'NONE', #6844, #8735, #8583, .T. ) ;
#2241=ORIENTED_EDGE ( 'NONE', *, *, #4648, .T. ) ;
#2242=DIRECTION ( 'NONE',  ( 0.000000000000000000, 0.000000000000000000, -1.000000000000000000 ) ) ;
#2243=ADVANCED_FACE ( 'NONE', ( #5769 ), #4785, .T. ) ;
#2244=DIRECTION ( 'NONE',  ( 0.000000000000000000, 0.000000000000000000, 1.000000000000000000 ) ) ;
#2245=ADVANCED_FACE ( 'NONE', ( #10411 ), #2029, .T. ) ;
#2246=ORIENTED_EDGE ( 'NONE', *, *, #10256, .T. ) ;
#2247=DIRECTION ( 'NONE',  ( 0.000000000000000000, 0.8090169943749486725, -0.5877852522924714718 ) ) ;
#2248=DIRECTION ( 'NONE',  ( -1.000000000000000000, -0.000000000000000000, -0.000000000000000000 ) ) ;
#2250=EDGE_CURVE ( 'NONE', #6885, #5042, #544, .T. ) ;
#2251=DIRECTION ( 'NONE',  ( 1.000000000000000000, 0.000000000000000000, 0.000000000000000000 ) ) ;
#2252=VERTEX_POINT ( 'NONE', #6913 ) ;
#2253=VERTEX_POINT ( 'NONE', #7952 ) ;
#2254=AXIS2_PLACEMENT_3D ( 'NONE', #11771, #1258, #6024 ) ;
#2257=ORIENTED_EDGE ( 'NONE', *, *, #11298, .T. ) ;
#2258=CARTESIAN_POINT ( 'NONE',  ( 3.000000000000000888, -8.753070780933015271, -20.78471918669869467 ) ) ;
#2260=FACE_OUTER_BOUND ( 'NONE', #2060, .T. ) ;
#2263=EDGE_CURVE ( 'NONE', #10872, #1804, #11184, .T. ) ;
#2265=DIRECTION ( 'NONE',  ( 0.000000000000000000, 0.000000000000000000, 1.000000000000000000 ) ) ;
#2267=EDGE_LOOP ( 'NONE', ( #4964, #1999, #2034, #3151 ) ) ;
#2268=EDGE_CURVE ( 'NONE', #6248, #9359, #1214, .T. ) ;
#2269=CARTESIAN_POINT ( 'NONE',  ( 50.00005079999999680, 4.898587196589412829E-16, -4.000000000000000000 ) ) ;
#2270=LINE ( 'NONE', #5829, #5879 ) ;
#2271=ORIENTED_EDGE ( 'NONE', *, *, #5420, .F. ) ;
#2272=AXIS2_PLACEMENT_3D ( 'NONE', #10040, #868, #1661 ) ;
#2275=EDGE_CURVE ( 'NONE', #8500, #3964, #8456, .T. ) ;
#2276=CARTESIAN_POINT ( 'NONE',  ( 3.000000000000000888, -11.20082935824061110, -20.08719549084876732 ) ) ;
#2277=CARTESIAN_POINT ( 'NONE',  ( 0.000000000000000000, -4.135161237383746524, 24.45282072769599679 ) ) ;
#2279=VECTOR ( 'NONE', #5383, 1000.000000000000000 ) ;
#2280=CYLINDRICAL_SURFACE ( 'NONE', #11572, 24.80000000000000071 ) ;
#2281=CARTESIAN_POINT ( 'NONE',  ( 0.000000000000000000, -14.74749645580022772, 17.06259499759939402 ) ) ;
#2282=EDGE_CURVE ( 'NONE', #1912, #6126, #4346, .T. ) ;
#2284=VERTEX_POINT ( 'NONE', #11576 ) ;
#2285=DIRECTION ( 'NONE',  ( 0.000000000000000000, -0.4999999999999887867, -0.8660254037844452579 ) ) ;
#2286=ORIENTED_EDGE ( 'NONE', *, *, #1989, .F. ) ;
#2287=DIRECTION ( 'NONE',  ( -1.000000000000000000, -0.000000000000000000, 0.000000000000000000 ) ) ;
#2288=EDGE_CURVE ( 'NONE', #4846, #11898, #486, .T. ) ;
#2289=DIRECTION ( 'NONE',  ( -1.000000000000000000, -0.000000000000000000, -0.000000000000000000 ) ) ;
#2290=DIRECTION ( 'NONE',  ( -1.000000000000000000, 0.000000000000000000, 0.000000000000000000 ) ) ;
#2295=AXIS2_PLACEMENT_3D ( 'NONE', #11427, #1549, #216 ) ;
#2296=ORIENTED_EDGE ( 'NONE', *, *, #6795, .F. ) ;
#2298=ORIENTED_EDGE ( 'NONE', *, *, #3148, .T. ) ;
#2299=CARTESIAN_POINT ( 'NONE',  ( 0.000000000000000000, 20.78471918669872665, -8.753070780932940664 ) ) ;
#2300=DIRECTION ( 'NONE',  ( -1.000000000000000000, -0.000000000000000000, -0.000000000000000000 ) ) ;
#2301=CYLINDRICAL_SURFACE ( 'NONE', #1924, 9.599999999999997868 ) ;
#2302=VECTOR ( 'NONE', #11462, 1000.000000000000000 ) ;
#2304=EDGE_CURVE ( 'NONE', #11132, #1084, #2325, .T. ) ;
#2305=EDGE_CURVE ( 'NONE', #1364, #4173, #3245, .T. ) ;
#2306=CARTESIAN_POINT ( 'NONE',  ( 3.000000000000002665, 0.000000000000000000, 0.000000000000000000 ) ) ;
#2307=ORIENTED_EDGE ( 'NONE', *, *, #4636, .F. ) ;
#2308=VERTEX_POINT ( 'NONE', #8822 ) ;
#2310=VERTEX_POINT ( 'NONE', #4171 ) ;
#2313=VECTOR ( 'NONE', #6165, 1000.000000000000000 ) ;
#2314=LINE ( 'NONE', #5069, #3108 ) ;
#2316=DIRECTION ( 'NONE',  ( 1.000000000000000000, 0.000000000000000000, -0.000000000000000000 ) ) ;
#2317=VERTEX_POINT ( 'NONE', #7837 ) ;
#2318=EDGE_CURVE ( 'NONE', #6367, #9845, #8645, .T. ) ;
#2319=CARTESIAN_POINT ( 'NONE',  ( 3.000000000000000888, -13.28910708463113366, -20.93895013827595264 ) ) ;
#2320=EDGE_CURVE ( 'NONE', #10471, #2327, #9034, .T. ) ;
#2321=CARTESIAN_POINT ( 'NONE',  ( 3.000000000000000888, 0.000000000000000000, 0.000000000000000000 ) ) ;
#2323=AXIS2_PLACEMENT_3D ( 'NONE', #2487, #5183, #7245 ) ;
#2324=EDGE_CURVE ( 'NONE', #8063, #7835, #8049, .T. ) ;
#2325=LINE ( 'NONE', #2269, #223 ) ;
#2326=ORIENTED_EDGE ( 'NONE', *, *, #7091, .T. ) ;
#2327=VERTEX_POINT ( 'NONE', #2446 ) ;
#2328=CARTESIAN_POINT ( 'NONE',  ( -10.00000000000000000, 0.000000000000000000, 0.000000000000000000 ) ) ;
#2329=VERTEX_POINT ( 'NONE', #2388 ) ;
#2331=AXIS2_PLACEMENT_3D ( 'NONE', #6956, #3236, #9667 ) ;
#2333=EDGE_LOOP ( 'NONE', ( #4156, #5133, #1265, #1708 ) ) ;
#2335=AXIS2_PLACEMENT_3D ( 'NONE', #2306, #10693, #5128 ) ;
#2337=DIRECTION ( 'NONE',  ( 0.000000000000000000, -0.8090169943749406789, -0.5877852522924823520 ) ) ;
#2339=DIRECTION ( 'NONE',  ( -1.000000000000000000, -0.000000000000000000, 0.000000000000000000 ) ) ;
#2341=DIRECTION ( 'NONE',  ( 0.000000000000000000, 0.000000000000000000, 1.000000000000000000 ) ) ;
#2342=DIRECTION ( 'NONE',  ( -1.000000000000000000, 0.000000000000000000, 0.000000000000000000 ) ) ;
#2343=CIRCLE ( 'NONE', #3324, 9.599999999999997868 ) ;
#2344=ORIENTED_EDGE ( 'NONE', *, *, #9652, .F. ) ;
#2346=VERTEX_POINT ( 'NONE', #6966 ) ;
#2347=EDGE_CURVE ( 'NONE', #9529, #6518, #4151, .T. ) ;
#2352=DIRECTION ( 'NONE',  ( 0.000000000000000000, 0.000000000000000000, 1.000000000000000000 ) ) ;
#2353=DIRECTION ( 'NONE',  ( -1.000000000000000000, 0.000000000000000000, 0.000000000000000000 ) ) ;
#2354=ORIENTED_EDGE ( 'NONE', *, *, #7955, .T. ) ;
#2355=EDGE_CURVE ( 'NONE', #8745, #2754, #7862, .T. ) ;
#2356=AXIS2_PLACEMENT_3D ( 'NONE', #11643, #6259, #5097 ) ;
#2357=AXIS2_PLACEMENT_3D ( 'NONE', #289, #9478, #3798 ) ;
#2358=AXIS2_PLACEMENT_3D ( 'NONE', #7457, #2820, #5389 ) ;
#2359=ORIENTED_EDGE ( 'NONE', *, *, #10785, .F. ) ;
#2361=DIRECTION ( 'NONE',  ( -1.000000000000000000, -0.000000000000000000, -0.000000000000000000 ) ) ;
#2362=LINE ( 'NONE', #6103, #10517 ) ;
#2363=CARTESIAN_POINT ( 'NONE',  ( 8.000000000000000000, 0.000000000000000000, 0.000000000000000000 ) ) ;
#2364=CIRCLE ( 'NONE', #10177, 24.80000000000000071 ) ;
#2366=CIRCLE ( 'NONE', #4918, 9.599999999999997868 ) ;
#2368=CIRCLE ( 'NONE', #11752, 22.99899999999999878 ) ;
#2369=CARTESIAN_POINT ( 'NONE',  ( 0.000000000000000000, 0.000000000000000000, 0.000000000000000000 ) ) ;
#2370=DIRECTION ( 'NONE',  ( -1.000000000000000000, -0.000000000000000000, 0.000000000000000000 ) ) ;
#2372=ORIENTED_EDGE ( 'NONE', *, *, #10243, .F. ) ;
#2374=VECTOR ( 'NONE', #4855, 1000.000000000000000 ) ;
#2375=ORIENTED_EDGE ( 'NONE', *, *, #3248, .T. ) ;
#2376=CARTESIAN_POINT ( 'NONE',  ( 3.000000000000000888, -15.42759117534397006, 16.45023496161660148 ) ) ;
#2377=DIRECTION ( 'NONE',  ( -1.000000000000000000, 0.000000000000000000, 0.000000000000000000 ) ) ;
#2379=CARTESIAN_POINT ( 'NONE',  ( 1.500000000000000444, -24.53384959170454849, -3.623565124517358793 ) ) ;
#2380=ORIENTED_EDGE ( 'NONE', *, *, #2571, .T. ) ;
#2381=FACE_OUTER_BOUND ( 'NONE', #5079, .T. ) ;
#2382=LINE ( 'NONE', #3241, #1803 ) ;
#2384=CIRCLE ( 'NONE', #2979, 22.99899999999999878 ) ;
#2385=EDGE_CURVE ( 'NONE', #5574, #10348, #3141, .T. ) ;
#2387=EDGE_LOOP ( 'NONE', ( #3785, #6172, #12021, #6330 ) ) ;
#2388=CARTESIAN_POINT ( 'NONE',  ( 3.000000000000000888, -15.40502424595158537, 19.43515443678397503 ) ) ;
#2389=LINE ( 'NONE', #10895, #9795 ) ;
#2390=VERTEX_POINT ( 'NONE', #1411 ) ;
#2392=ADVANCED_FACE ( 'NONE', ( #10894 ), #5204, .T. ) ;
#2393=VERTEX_POINT ( 'NONE', #3436 ) ;
#2394=CYLINDRICAL_SURFACE ( 'NONE', #3836, 22.99899999999999878 ) ;
#2395=CARTESIAN_POINT ( 'NONE',  ( 3.000000000000000888, 22.21333432029578248, -11.02759168516722887 ) ) ;
#2397=DIRECTION ( 'NONE',  ( -1.000000000000000000, 0.000000000000000000, -0.000000000000000000 ) ) ;
#2400=DIRECTION ( 'NONE',  ( 0.000000000000000000, 0.000000000000000000, -1.000000000000000000 ) ) ;
#2402=DIRECTION ( 'NONE',  ( -1.000000000000000000, 0.000000000000000000, -0.000000000000000000 ) ) ;
#2403=CIRCLE ( 'NONE', #3971, 22.99899999999999878 ) ;
#2404=DIRECTION ( 'NONE',  ( 1.000000000000000000, -0.000000000000000000, -0.000000000000000000 ) ) ;
#2405=ORIENTED_EDGE ( 'NONE', *, *, #4443, .T. ) ;
#2406=EDGE_CURVE ( 'NONE', #712, #2737, #1572, .T. ) ;
#2409=ORIENTED_EDGE ( 'NONE', *, *, #256, .F. ) ;
#2410=VECTOR ( 'NONE', #6538, 1000.000000000000000 ) ;
#2411=DIRECTION ( 'NONE',  ( 0.000000000000000000, 0.3090169943749479509, -0.9510565162951534202 ) ) ;
#2412=CARTESIAN_POINT ( 'NONE',  ( 1.500000000000000444, 24.77821629063821973, -1.039229259764577140 ) ) ;
#2415=EDGE_CURVE ( 'NONE', #1082, #5236, #5720, .T. ) ;
#2417=CYLINDRICAL_SURFACE ( 'NONE', #11947, 9.599999999999997868 ) ;
#2418=LINE ( 'NONE', #9032, #1017 ) ;
#2419=VERTEX_POINT ( 'NONE', #11986 ) ;
#2420=EDGE_CURVE ( 'NONE', #4090, #4817, #3363, .T. ) ;
#2421=ORIENTED_EDGE ( 'NONE', *, *, #5046, .F. ) ;
#2422=CIRCLE ( 'NONE', #10241, 24.80000000000000071 ) ;
#2425=CARTESIAN_POINT ( 'NONE',  ( 3.000000000000000888, 11.20082935824103387, -20.08719549084852929 ) ) ;
#2426=DIRECTION ( 'NONE',  ( -1.000000000000000000, -0.000000000000000000, 0.000000000000000000 ) ) ;
#2427=EDGE_CURVE ( 'NONE', #6354, #8063, #8137, .T. ) ;
#2430=CYLINDRICAL_SURFACE ( 'NONE', #6472, 9.599999999999997868 ) ;
#2431=FACE_OUTER_BOUND ( 'NONE', #9331, .T. ) ;
#2432=ORIENTED_EDGE ( 'NONE', *, *, #1003, .T. ) ;
#2433=ORIENTED_EDGE ( 'NONE', *, *, #1414, .T. ) ;
#2436=ORIENTED_EDGE ( 'NONE', *, *, #11340, .F. ) ;
#2437=CARTESIAN_POINT ( 'NONE',  ( 3.000000000000000888, -13.62355943574031869, 17.97274125076070206 ) ) ;
#2438=AXIS2_PLACEMENT_3D ( 'NONE', #7154, #2519, #4545 ) ;
#2439=LINE ( 'NONE', #8298, #7007 ) ;
#2440=CARTESIAN_POINT ( 'NONE',  ( 0.000000000000000000, 16.45023496161686438, -15.42759117534368407 ) ) ;
#2441=CARTESIAN_POINT ( 'NONE',  ( 3.000000000000000888, -22.15038895030651744, 4.240409074144028345 ) ) ;
#2442=ORIENTED_EDGE ( 'NONE', *, *, #7387, .T. ) ;
#2443=DIRECTION ( 'NONE',  ( -1.000000000000000000, -0.000000000000000000, 0.000000000000000000 ) ) ;
#2444=DIRECTION ( 'NONE',  ( -1.000000000000000000, 0.000000000000000000, 0.000000000000000000 ) ) ;
#2446=CARTESIAN_POINT ( 'NONE',  ( 0.000000000000000000, -1.039229259764660407, 24.77821629063821263 ) ) ;
#2447=EDGE_LOOP ( 'NONE', ( #7209, #1560, #7375, #3832 ) ) ;
#2448=CARTESIAN_POINT ( 'NONE',  ( 3.000000000000000888, 0.000000000000000000, 0.000000000000000000 ) ) ;
#2449=ORIENTED_EDGE ( 'NONE', *, *, #5083, .F. ) ;
#2451=EDGE_LOOP ( 'NONE', ( #5692, #7493, #1820, #3021 ) ) ;
#2452=LINE ( 'NONE', #3620, #5793 ) ;
#2453=CIRCLE ( 'NONE', #7141, 22.99900000000000233 ) ;
#2454=CARTESIAN_POINT ( 'NONE',  ( 0.000000000000000000, 12.88318129270205148, -18.51065745848364230 ) ) ;
#2455=ORIENTED_EDGE ( 'NONE', *, *, #2734, .F. ) ;
#2457=DIRECTION ( 'NONE',  ( 0.000000000000000000, 0.4067366430758009854, -0.9135454576426006446 ) ) ;
#2459=CARTESIAN_POINT ( 'NONE',  ( 3.000000000000000888, 21.96011696265484403, 5.135568396240393518 ) ) ;
#2461=EDGE_CURVE ( 'NONE', #9359, #3469, #2553, .T. ) ;
#2462=DIRECTION ( 'NONE',  ( 0.000000000000000000, 0.000000000000000000, 1.000000000000000000 ) ) ;
#2463=ORIENTED_EDGE ( 'NONE', *, *, #10939, .F. ) ;
#2464=CIRCLE ( 'NONE', #2864, 22.99899999999999523 ) ;
#2466=EDGE_CURVE ( 'NONE', #10699, #9213, #10198, .T. ) ;
#2467=DIRECTION ( 'NONE',  ( -1.000000000000000000, 0.000000000000000000, 0.000000000000000000 ) ) ;
#2469=ORIENTED_EDGE ( 'NONE', *, *, #4802, .F. ) ;
#2470=CARTESIAN_POINT ( 'NONE',  ( 0.000000000000000000, 0.000000000000000000, 0.000000000000000000 ) ) ;
#2471=DIRECTION ( 'NONE',  ( 0.000000000000000000, -0.9510565162951566398, 0.3090169943749382919 ) ) ;
#2472=VERTEX_POINT ( 'NONE', #5438 ) ;
#2473=DIRECTION ( 'NONE',  ( 0.000000000000000000, 0.000000000000000000, 1.000000000000000000 ) ) ;
#2474=CIRCLE ( 'NONE', #9317, 9.599999999999997868 ) ;
#2475=CARTESIAN_POINT ( 'NONE',  ( 3.000000000000000888, 13.62355943574044481, -17.97274125076060258 ) ) ;
#2476=LINE ( 'NONE', #6210, #1783 ) ;
#2477=EDGE_CURVE ( 'NONE', #2132, #7388, #11759, .T. ) ;
#2479=DIRECTION ( 'NONE',  ( -1.000000000000000000, 0.000000000000000000, 0.000000000000000000 ) ) ;
#2481=DIRECTION ( 'NONE',  ( -1.000000000000000000, -0.000000000000000000, 0.000000000000000000 ) ) ;
#2482=ORIENTED_EDGE ( 'NONE', *, *, #11815, .F. ) ;
#2483=ORIENTED_EDGE ( 'NONE', *, *, #5860, .T. ) ;
#2484=ORIENTED_EDGE ( 'NONE', *, *, #901, .F. ) ;
#2487=CARTESIAN_POINT ( 'NONE',  ( 3.000000000000000888, 0.000000000000000000, 0.000000000000000000 ) ) ;
#2489=AXIS2_PLACEMENT_3D ( 'NONE', #8607, #953, #11297 ) ;
#2490=DIRECTION ( 'NONE',  ( -1.000000000000000000, -0.000000000000000000, -0.000000000000000000 ) ) ;
#2491=CARTESIAN_POINT ( 'NONE',  ( 3.000000000000000888, -8.645255683529166291, 23.24434456306322261 ) ) ;
#2494=ORIENTED_EDGE ( 'NONE', *, *, #8157, .T. ) ;
#2495=LINE ( 'NONE', #1581, #10778 ) ;
#2496=CARTESIAN_POINT ( 'NONE',  ( 0.000000000000000000, -13.62355943574031869, 17.97274125076070206 ) ) ;
#2497=CARTESIAN_POINT ( 'NONE',  ( 0.000000000000000000, 0.000000000000000000, 0.000000000000000000 ) ) ;
#2498=CIRCLE ( 'NONE', #1324, 9.599999999999997868 ) ;
#2499=DIRECTION ( 'NONE',  ( 0.000000000000000000, 0.000000000000000000, 1.000000000000000000 ) ) ;
#2501=ADVANCED_FACE ( 'NONE', ( #11073 ), #2573, .T. ) ;
#2502=CARTESIAN_POINT ( 'NONE',  ( 3.000000000000000888, -22.54798042742717357, -0.4575788569254196636 ) ) ;
#2503=LINE ( 'NONE', #9166, #1035 ) ;
#2506=AXIS2_PLACEMENT_3D ( 'NONE', #3532, #6166, #7125 ) ;
#2509=EDGE_CURVE ( 'NONE', #11319, #1445, #7458, .T. ) ;
#2510=ORIENTED_EDGE ( 'NONE', *, *, #10571, .F. ) ;
#2511=ORIENTED_EDGE ( 'NONE', *, *, #8650, .T. ) ;
#2513=ORIENTED_EDGE ( 'NONE', *, *, #9356, .T. ) ;
#2514=LINE ( 'NONE', #11930, #6190 ) ;
#2515=ORIENTED_EDGE ( 'NONE', *, *, #3657, .T. ) ;
#2516=AXIS2_PLACEMENT_3D ( 'NONE', #2258, #11499, #10459 ) ;
#2517=DIRECTION ( 'NONE',  ( 1.000000000000000000, 0.000000000000000000, 0.000000000000000000 ) ) ;
#2518=VECTOR ( 'NONE', #4069, 1000.000000000000000 ) ;
#2519=DIRECTION ( 'NONE',  ( -1.000000000000000000, 0.000000000000000000, 0.000000000000000000 ) ) ;
#2522=EDGE_CURVE ( 'NONE', #5068, #2284, #11352, .T. ) ;
#2523=CARTESIAN_POINT ( 'NONE',  ( 3.000000000000000888, 22.15038895030654942, -4.240409074143872914 ) ) ;
#2524=VERTEX_POINT ( 'NONE', #9357 ) ;
#2525=DIRECTION ( 'NONE',  ( -1.000000000000000000, 0.000000000000000000, 0.000000000000000000 ) ) ;
#2526=VERTEX_POINT ( 'NONE', #1654 ) ;
#2527=AXIS2_PLACEMENT_3D ( 'NONE', #599, #3429, #2791 ) ;
#2529=FACE_OUTER_BOUND ( 'NONE', #6695, .T. ) ;
#2530=EDGE_LOOP ( 'NONE', ( #7673, #11425, #9407, #859 ) ) ;
#2531=CARTESIAN_POINT ( 'NONE',  ( 0.000000000000000000, -2.811977935937640005, -22.37663021667346896 ) ) ;
#2532=DIRECTION ( 'NONE',  ( -1.000000000000000000, -0.000000000000000000, 0.000000000000000000 ) ) ;
#2533=CARTESIAN_POINT ( 'NONE',  ( 3.000000000000000888, -17.97274125076064877, -13.62355943574037731 ) ) ;
#2535=AXIS2_PLACEMENT_3D ( 'NONE', #600, #664, #4334 ) ;
#2537=CARTESIAN_POINT ( 'NONE',  ( 1.500000000000000444, -21.97817939804031795, -11.48910920600707009 ) ) ;
#2538=AXIS2_PLACEMENT_3D ( 'NONE', #11261, #10510, #108 ) ;
#2539=CARTESIAN_POINT ( 'NONE',  ( 3.000000000000000888, 15.40502424595171327, -19.43515443678387555 ) ) ;
#2540=ORIENTED_EDGE ( 'NONE', *, *, #6499, .T. ) ;
#2541=EDGE_LOOP ( 'NONE', ( #847, #6542, #9288, #5997 ) ) ;
#2542=EDGE_LOOP ( 'NONE', ( #9524, #788, #830, #11863 ) ) ;
#2543=AXIS2_PLACEMENT_3D ( 'NONE', #10742, #10002, #8965 ) ;
#2546=EDGE_CURVE ( 'NONE', #5965, #9994, #10370, .T. ) ;
#2547=AXIS2_PLACEMENT_3D ( 'NONE', #11291, #9455, #1073 ) ;
#2548=CARTESIAN_POINT ( 'NONE',  ( 3.000000000000000888, 0.000000000000000000, 0.000000000000000000 ) ) ;
#2550=EDGE_CURVE ( 'NONE', #1912, #11191, #2954, .T. ) ;
#2552=DIRECTION ( 'NONE',  ( 0.000000000000000000, 0.1045284632676469622, 0.9945218953682738450 ) ) ;
#2553=CIRCLE ( 'NONE', #9394, 9.599999999999997868 ) ;
#2554=AXIS2_PLACEMENT_3D ( 'NONE', #10908, #2525, #11880 ) ;
#2555=DIRECTION ( 'NONE',  ( -1.000000000000000000, 0.000000000000000000, 0.000000000000000000 ) ) ;
#2556=ORIENTED_EDGE ( 'NONE', *, *, #4478, .T. ) ;
#2557=VERTEX_POINT ( 'NONE', #11920 ) ;
#2559=EDGE_LOOP ( 'NONE', ( #1863, #1284, #11117, #1939 ) ) ;
#2560=CARTESIAN_POINT ( 'NONE',  ( 3.000000000000000888, 21.14796121233196402, 9.039786367038912474 ) ) ;
#2561=CARTESIAN_POINT ( 'NONE',  ( 0.000000000000000000, -20.41249101028205004, -9.589108953448107542 ) ) ;
#2562=CIRCLE ( 'NONE', #4519, 9.599999999999996092 ) ;
#2563=VECTOR ( 'NONE', #7503, 1000.000000000000000 ) ;
#2565=DIRECTION ( 'NONE',  ( -1.000000000000000000, -0.000000000000000000, -0.000000000000000000 ) ) ;
#2566=ORIENTED_EDGE ( 'NONE', *, *, #6432, .F. ) ;
#2567=VECTOR ( 'NONE', #4717, 1000.000000000000000 ) ;
#2568=FACE_OUTER_BOUND ( 'NONE', #6706, .T. ) ;
#2569=CARTESIAN_POINT ( 'NONE',  ( 0.000000000000000000, 0.000000000000000000, 0.000000000000000000 ) ) ;
#2571=EDGE_CURVE ( 'NONE', #1140, #5646, #4510, .T. ) ;
#2572=CIRCLE ( 'NONE', #414, 24.80000000000000071 ) ;
#2573=CYLINDRICAL_SURFACE ( 'NONE', #2188, 9.599999999999997868 ) ;
#2575=FACE_OUTER_BOUND ( 'NONE', #7463, .T. ) ;
#2576=AXIS2_PLACEMENT_3D ( 'NONE', #1100, #6660, #6720 ) ;
#2577=ORIENTED_EDGE ( 'NONE', *, *, #3677, .F. ) ;
#2578=EDGE_CURVE ( 'NONE', #1648, #6277, #11927, .T. ) ;
#2579=ORIENTED_EDGE ( 'NONE', *, *, #10478, .F. ) ;
#2581=DIRECTION ( 'NONE',  ( 0.000000000000000000, 0.9135454576426018658, -0.4067366430757979323 ) ) ;
#2582=ORIENTED_EDGE ( 'NONE', *, *, #10346, .F. ) ;
#2583=ORIENTED_EDGE ( 'NONE', *, *, #11480, .T. ) ;
#2584=AXIS2_PLACEMENT_3D ( 'NONE', #12059, #2832, #6554 ) ;
#2585=AXIS2_PLACEMENT_3D ( 'NONE', #8520, #1052, #119 ) ;
#2586=DIRECTION ( 'NONE',  ( -1.000000000000000000, 0.000000000000000000, 0.000000000000000000 ) ) ;
#2587=EDGE_CURVE ( 'NONE', #9333, #10794, #3551, .T. ) ;
#2588=VECTOR ( 'NONE', #6003, 1000.000000000000000 ) ;
#2589=CARTESIAN_POINT ( 'NONE',  ( 0.000000000000000000, 0.000000000000000000, 0.000000000000000000 ) ) ;
#2592=CARTESIAN_POINT ( 'NONE',  ( 3.000000000000000888, 23.24434456306324748, 8.645255683529086355 ) ) ;
#2593=ORIENTED_EDGE ( 'NONE', *, *, #1685, .F. ) ;
#2594=DIRECTION ( 'NONE',  ( -1.000000000000000000, 0.000000000000000000, 0.000000000000000000 ) ) ;
#2595=ORIENTED_EDGE ( 'NONE', *, *, #7737, .F. ) ;
#2596=CIRCLE ( 'NONE', #48, 9.599999999999997868 ) ;
#2598=CARTESIAN_POINT ( 'NONE',  ( 0.000000000000000000, -5.117118920208643118, 22.42251312757878168 ) ) ;
#2601=CYLINDRICAL_SURFACE ( 'NONE', #11293, 24.80000000000000071 ) ;
#2602=CARTESIAN_POINT ( 'NONE',  ( 3.000000000000000888, 0.000000000000000000, 0.000000000000000000 ) ) ;
#2604=AXIS2_PLACEMENT_3D ( 'NONE', #7142, #670, #1652 ) ;
#2606=FACE_OUTER_BOUND ( 'NONE', #11035, .T. ) ;
#2607=CARTESIAN_POINT ( 'NONE',  ( 0.000000000000000000, 0.000000000000000000, 0.000000000000000000 ) ) ;
#2608=AXIS2_PLACEMENT_3D ( 'NONE', #824, #7544, #4623 ) ;
#2609=ORIENTED_EDGE ( 'NONE', *, *, #2320, .F. ) ;
#2610=VERTEX_POINT ( 'NONE', #7325 ) ;
#2611=CIRCLE ( 'NONE', #10025, 9.599999999999996092 ) ;
#2613=DIRECTION ( 'NONE',  ( 0.000000000000000000, 0.000000000000000000, 1.000000000000000000 ) ) ;
#2614=DIRECTION ( 'NONE',  ( 0.000000000000000000, 0.000000000000000000, 1.000000000000000000 ) ) ;
#2616=AXIS2_PLACEMENT_3D ( 'NONE', #9855, #6121, #3548 ) ;
#2617=LINE ( 'NONE', #9896, #5894 ) ;
#2619=EDGE_CURVE ( 'NONE', #3033, #4684, #6419, .T. ) ;
#2620=DIRECTION ( 'NONE',  ( -1.000000000000000000, -0.000000000000000000, -0.000000000000000000 ) ) ;
#2621=ORIENTED_EDGE ( 'NONE', *, *, #4113, .T. ) ;
#2622=EDGE_CURVE ( 'NONE', #9863, #5773, #4119, .T. ) ;
#2623=ORIENTED_EDGE ( 'NONE', *, *, #2619, .T. ) ;
#2625=CARTESIAN_POINT ( 'NONE',  ( 3.000000000000000888, 0.000000000000000000, 0.000000000000000000 ) ) ;
#2627=CARTESIAN_POINT ( 'NONE',  ( 0.000000000000000000, 0.000000000000000000, 0.000000000000000000 ) ) ;
#2631=DIRECTION ( 'NONE',  ( -1.000000000000000000, 0.000000000000000000, 0.000000000000000000 ) ) ;
#2632=AXIS2_PLACEMENT_3D ( 'NONE', #6862, #8946, #4180 ) ;
#2634=LINE ( 'NONE', #10152, #8624 ) ;
#2635=VERTEX_POINT ( 'NONE', #11434 ) ;
#2636=ORIENTED_EDGE ( 'NONE', *, *, #1030, .T. ) ;
#2639=EDGE_CURVE ( 'NONE', #5055, #2557, #6076, .T. ) ;
#2640=DIRECTION ( 'NONE',  ( -1.000000000000000000, 0.000000000000000000, 0.000000000000000000 ) ) ;
#2641=ORIENTED_EDGE ( 'NONE', *, *, #2825, .F. ) ;
#2642=DIRECTION ( 'NONE',  ( 0.000000000000000000, -0.8090169943749406789, -0.5877852522924823520 ) ) ;
#2643=CARTESIAN_POINT ( 'NONE',  ( 3.000000000000000888, 0.000000000000000000, 0.000000000000000000 ) ) ;
#2645=EDGE_CURVE ( 'NONE', #5516, #8218, #9196, .T. ) ;
#2646=CARTESIAN_POINT ( 'NONE',  ( 3.000000000000000888, -0.4575788569253416149, 22.54798042742717712 ) ) ;
#2647=DIRECTION ( 'NONE',  ( -1.000000000000000000, 0.000000000000000000, 0.000000000000000000 ) ) ;
#2648=CARTESIAN_POINT ( 'NONE',  ( 0.000000000000000000, 24.77821629063821973, -1.039229259764575364 ) ) ;
#2649=ORIENTED_EDGE ( 'NONE', *, *, #12031, .F. ) ;
#2652=CARTESIAN_POINT ( 'NONE',  ( 1.500000000000000444, 13.28910708463157420, -20.93895013827567553 ) ) ;
#2653=DIRECTION ( 'NONE',  ( 1.000000000000000000, 0.000000000000000000, 0.000000000000000000 ) ) ;
#2654=DIRECTION ( 'NONE',  ( 0.000000000000000000, 0.000000000000000000, 1.000000000000000000 ) ) ;
#2655=DIRECTION ( 'NONE',  ( 1.000000000000000000, 0.000000000000000000, 0.000000000000000000 ) ) ;
#2656=DIRECTION ( 'NONE',  ( -1.000000000000000000, -0.000000000000000000, 0.000000000000000000 ) ) ;
#2658=EDGE_CURVE ( 'NONE', #8897, #12050, #3929, .T. ) ;
#2659=VECTOR ( 'NONE', #11814, 1000.000000000000000 ) ;
#2661=CARTESIAN_POINT ( 'NONE',  ( 0.000000000000000000, 0.4575788569251889593, 22.54798042742718067 ) ) ;
#2662=CYLINDRICAL_SURFACE ( 'NONE', #6841, 9.599999999999997868 ) ;
#2663=ORIENTED_EDGE ( 'NONE', *, *, #10393, .F. ) ;
#2664=EDGE_CURVE ( 'NONE', #2526, #8541, #1951, .T. ) ;
#2666=VECTOR ( 'NONE', #1048, 1000.000000000000000 ) ;
#2668=DIRECTION ( 'NONE',  ( 1.000000000000000000, 0.000000000000000000, 0.000000000000000000 ) ) ;
#2669=CARTESIAN_POINT ( 'NONE',  ( 3.000000000000000888, 20.78471918669860941, 8.753070780933226658 ) ) ;
#2672=FACE_OUTER_BOUND ( 'NONE', #4102, .T. ) ;
#2673=DIRECTION ( 'NONE',  ( -1.000000000000000000, -0.000000000000000000, -0.000000000000000000 ) ) ;
#2674=ORIENTED_EDGE ( 'NONE', *, *, #5866, .T. ) ;
#2675=ORIENTED_EDGE ( 'NONE', *, *, #1223, .T. ) ;
#2676=CYLINDRICAL_SURFACE ( 'NONE', #4956, 9.599999999999997868 ) ;
#2677=FACE_OUTER_BOUND ( 'NONE', #8457, .T. ) ;
#2678=AXIS2_PLACEMENT_3D ( 'NONE', #5922, #3397, #2242 ) ;
#2681=CARTESIAN_POINT ( 'NONE',  ( 0.000000000000000000, 0.000000000000000000, 0.000000000000000000 ) ) ;
#2682=ADVANCED_FACE ( 'NONE', ( #4889 ), #8627, .T. ) ;
#2683=CARTESIAN_POINT ( 'NONE',  ( 0.000000000000000000, 0.000000000000000000, 0.000000000000000000 ) ) ;
#2685=DIRECTION ( 'NONE',  ( 0.000000000000000000, 0.7431448254773954654, -0.6691306063588569053 ) ) ;
#2686=ORIENTED_EDGE ( 'NONE', *, *, #1882, .T. ) ;
#2687=ORIENTED_EDGE ( 'NONE', *, *, #9609, .T. ) ;
#2688=CARTESIAN_POINT ( 'NONE',  ( 3.000000000000000888, -19.75591328264879110, -10.87771529938182091 ) ) ;
#2689=ORIENTED_EDGE ( 'NONE', *, *, #2844, .F. ) ;
#2690=VECTOR ( 'NONE', #4114, 1000.000000000000000 ) ;
#2691=ORIENTED_EDGE ( 'NONE', *, *, #11991, .F. ) ;
#2693=EDGE_CURVE ( 'NONE', #5571, #4684, #7997, .T. ) ;
#2694=ORIENTED_EDGE ( 'NONE', *, *, #9281, .F. ) ;
#2695=DIRECTION ( 'NONE',  ( -1.000000000000000000, 0.000000000000000000, -0.000000000000000000 ) ) ;
#2696=ORIENTED_EDGE ( 'NONE', *, *, #11963, .F. ) ;
#2697=ADVANCED_FACE ( 'NONE', ( #7517 ), #5809, .T. ) ;
#2698=CARTESIAN_POINT ( 'NONE',  ( 0.000000000000000000, -15.80756504416678432, -19.10918332567973721 ) ) ;
#2699=EDGE_CURVE ( 'NONE', #10972, #5532, #4484, .T. ) ;
#2700=DIRECTION ( 'NONE',  ( -1.000000000000000000, -0.000000000000000000, -0.000000000000000000 ) ) ;
#2702=AXIS2_PLACEMENT_3D ( 'NONE', #7626, #9413, #7568 ) ;
#2703=DIRECTION ( 'NONE',  ( 0.000000000000000000, 0.000000000000000000, -1.000000000000000000 ) ) ;
#2704=DIRECTION ( 'NONE',  ( 0.000000000000000000, 0.6691306063588593478, -0.7431448254773932449 ) ) ;
#2705=EDGE_LOOP ( 'NONE', ( #3783, #7591, #7363, #126 ) ) ;
#2706=CARTESIAN_POINT ( 'NONE',  ( 1.499999999999999556, 1.039229259764835600, -24.77821629063820907 ) ) ;
#2707=ORIENTED_EDGE ( 'NONE', *, *, #10507, .F. ) ;
#2710=CIRCLE ( 'NONE', #10129, 24.80000000000000071 ) ;
#2713=ORIENTED_EDGE ( 'NONE', *, *, #7207, .F. ) ;
#2714=CYLINDRICAL_SURFACE ( 'NONE', #8561, 22.99899999999999878 ) ;
#2715=DIRECTION ( 'NONE',  ( 0.000000000000000000, 0.000000000000000000, -1.000000000000000000 ) ) ;
#2716=DIRECTION ( 'NONE',  ( -1.000000000000000000, 0.000000000000000000, 0.000000000000000000 ) ) ;
#2717=CYLINDRICAL_SURFACE ( 'NONE', #9212, 9.599999999999997868 ) ;
#2719=CARTESIAN_POINT ( 'NONE',  ( 3.000000000000000888, -24.53384959170460178, 3.623565124517029279 ) ) ;
#2720=CIRCLE ( 'NONE', #8394, 22.99899999999999878 ) ;
#2721=FACE_OUTER_BOUND ( 'NONE', #2447, .T. ) ;
#2722=ORIENTED_EDGE ( 'NONE', *, *, #7395, .F. ) ;
#2723=ORIENTED_EDGE ( 'NONE', *, *, #3657, .F. ) ;
#2724=ORIENTED_EDGE ( 'NONE', *, *, #8230, .T. ) ;
#2726=CARTESIAN_POINT ( 'NONE',  ( 3.000000000000000888, 0.000000000000000000, 0.000000000000000000 ) ) ;
#2728=CIRCLE ( 'NONE', #8597, 9.599999999999997868 ) ;
#2729=AXIS2_PLACEMENT_3D ( 'NONE', #10568, #3051, #8505 ) ;
#2730=DIRECTION ( 'NONE',  ( -1.000000000000000000, -0.000000000000000000, -0.000000000000000000 ) ) ;
#2731=CARTESIAN_POINT ( 'NONE',  ( 3.000000000000000888, 15.80756504416690866, 19.10918332567963418 ) ) ;
#2732=CIRCLE ( 'NONE', #9573, 22.99899999999999523 ) ;
#2734=EDGE_CURVE ( 'NONE', #1630, #8186, #10547, .T. ) ;
#2736=CARTESIAN_POINT ( 'NONE',  ( 3.000000000000000888, 17.31945870441147406, 15.13242714128125499 ) ) ;
#2737=VERTEX_POINT ( 'NONE', #1217 ) ;
#2738=CIRCLE ( 'NONE', #3717, 22.99900000000000233 ) ;
#2739=VERTEX_POINT ( 'NONE', #4827 ) ;
#2740=LINE ( 'NONE', #10383, #1241 ) ;
#2741=CARTESIAN_POINT ( 'NONE',  ( 1.500000000000000444, 6.668524164681940647, -23.88662356770108630 ) ) ;
#2744=CARTESIAN_POINT ( 'NONE',  ( 3.000000000000000888, 20.78471918669872665, -8.753070780932940664 ) ) ;
#2745=AXIS2_PLACEMENT_3D ( 'NONE', #1853, #8401, #5527 ) ;
#2748=DIRECTION ( 'NONE',  ( 0.000000000000000000, 0.9135454576426018658, -0.4067366430757981544 ) ) ;
#2749=VERTEX_POINT ( 'NONE', #3852 ) ;
#2750=ORIENTED_EDGE ( 'NONE', *, *, #12034, .T. ) ;
#2751=DIRECTION ( 'NONE',  ( 0.000000000000000000, 0.2079116908177532086, 0.9781476007338069101 ) ) ;
#2752=VECTOR ( 'NONE', #3016, 1000.000000000000000 ) ;
#2753=ORIENTED_EDGE ( 'NONE', *, *, #9125, .F. ) ;
#2754=VERTEX_POINT ( 'NONE', #11314 ) ;
#2756=AXIS2_PLACEMENT_3D ( 'NONE', #11332, #2956, #3075 ) ;
#2758=ORIENTED_EDGE ( 'NONE', *, *, #2263, .T. ) ;
#2759=EDGE_CURVE ( 'NONE', #11368, #3881, #10741, .T. ) ;
#2760=DIRECTION ( 'NONE',  ( -1.000000000000000000, -0.000000000000000000, -0.000000000000000000 ) ) ;
#2763=VECTOR ( 'NONE', #8595, 1000.000000000000000 ) ;
#2764=CIRCLE ( 'NONE', #11551, 24.80000000000000071 ) ;
#2765=AXIS2_PLACEMENT_3D ( 'NONE', #402, #3050, #11428 ) ;
#2766=EDGE_CURVE ( 'NONE', #10279, #8218, #9379, .T. ) ;
#2767=LINE ( 'NONE', #6495, #1002 ) ;
#2768=ORIENTED_EDGE ( 'NONE', *, *, #1499, .F. ) ;
#2770=CARTESIAN_POINT ( 'NONE',  ( 3.000000000000000888, 22.37663021667344054, -2.811977935937859385 ) ) ;
#2775=FACE_OUTER_BOUND ( 'NONE', #3857, .T. ) ;
#2776=VERTEX_POINT ( 'NONE', #49 ) ;
#2777=AXIS2_PLACEMENT_3D ( 'NONE', #8384, #3666, #1705 ) ;
#2778=CARTESIAN_POINT ( 'NONE',  ( 3.000000000000000888, 0.3433949777331667397, 22.99643626497956816 ) ) ;
#2782=AXIS2_PLACEMENT_3D ( 'NONE', #9129, #7342, #741 ) ;
#2783=EDGE_CURVE ( 'NONE', #9137, #1367, #577, .T. ) ;
#2784=DIRECTION ( 'NONE',  ( -1.000000000000000000, 0.000000000000000000, -0.000000000000000000 ) ) ;
#2785=AXIS2_PLACEMENT_3D ( 'NONE', #6493, #4781, #10408 ) ;
#2786=ORIENTED_EDGE ( 'NONE', *, *, #3366, .F. ) ;
#2787=AXIS2_PLACEMENT_3D ( 'NONE', #5978, #9707, #9591 ) ;
#2789=ORIENTED_EDGE ( 'NONE', *, *, #370, .T. ) ;
#2791=DIRECTION ( 'NONE',  ( 0.000000000000000000, 0.9135454576425990902, 0.4067366430758040385 ) ) ;
#2793=CIRCLE ( 'NONE', #11777, 9.599999999999999645 ) ;
#2794=DIRECTION ( 'NONE',  ( 0.000000000000000000, 0.3090169943749417336, 0.9510565162951555296 ) ) ;
#2795=EDGE_CURVE ( 'NONE', #9064, #5856, #769, .T. ) ;
#2796=LINE ( 'NONE', #5606, #6420 ) ;
#2798=CIRCLE ( 'NONE', #4757, 9.599999999999997868 ) ;
#2799=LINE ( 'NONE', #5485, #1625 ) ;
#2800=ADVANCED_FACE ( 'NONE', ( #9772 ), #6042, .T. ) ;
#2801=CARTESIAN_POINT ( 'NONE',  ( 3.000000000000000888, 0.000000000000000000, 0.000000000000000000 ) ) ;
#2802=VERTEX_POINT ( 'NONE', #8803 ) ;
#2803=ORIENTED_EDGE ( 'NONE', *, *, #8473, .F. ) ;
#2805=ORIENTED_EDGE ( 'NONE', *, *, #7362, .T. ) ;
#2807=CARTESIAN_POINT ( 'NONE',  ( 0.000000000000000000, 22.37663021667344054, 6.788022064062137595 ) ) ;
#2808=VECTOR ( 'NONE', #3185, 1000.000000000000000 ) ;
#2809=DIRECTION ( 'NONE',  ( 0.000000000000000000, 0.9510565162951523099, 0.3090169943749513370 ) ) ;
#2810=EDGE_CURVE ( 'NONE', #4929, #5661, #4326, .T. ) ;
#2811=DIRECTION ( 'NONE',  ( 0.000000000000000000, 0.4999999999999948375, 0.8660254037844415942 ) ) ;
#2813=CIRCLE ( 'NONE', #66, 9.599999999999997868 ) ;
#2814=CARTESIAN_POINT ( 'NONE',  ( 3.000000000000000888, 9.667200211210106531, -20.86861857134724474 ) ) ;
#2818=ORIENTED_EDGE ( 'NONE', *, *, #8790, .F. ) ;
#2819=EDGE_LOOP ( 'NONE', ( #3914, #9286, #2148, #9287 ) ) ;
#2820=DIRECTION ( 'NONE',  ( -1.000000000000000000, -0.000000000000000000, -0.000000000000000000 ) ) ;
#2821=ORIENTED_EDGE ( 'NONE', *, *, #10767, .F. ) ;
#2822=CIRCLE ( 'NONE', #2231, 22.99899999999999878 ) ;
#2823=ORIENTED_EDGE ( 'NONE', *, *, #823, .F. ) ;
#2825=EDGE_CURVE ( 'NONE', #6662, #8629, #5074, .T. ) ;
#2826=CARTESIAN_POINT ( 'NONE',  ( 3.000000000000000888, 0.000000000000000000, 0.000000000000000000 ) ) ;
#2827=VERTEX_POINT ( 'NONE', #7938 ) ;
#2828=CARTESIAN_POINT ( 'NONE',  ( 3.000000000000000888, -8.753070780933295936, 20.78471918669858098 ) ) ;
#2829=DIRECTION ( 'NONE',  ( 0.000000000000000000, -0.6691306063588644548, 0.7431448254773885820 ) ) ;
#2831=VECTOR ( 'NONE', #624, 1000.000000000000000 ) ;
#2832=DIRECTION ( 'NONE',  ( -1.000000000000000000, 0.000000000000000000, 0.000000000000000000 ) ) ;
#2833=FACE_OUTER_BOUND ( 'NONE', #9045, .T. ) ;
#2835=ORIENTED_EDGE ( 'NONE', *, *, #2699, .T. ) ;
#2836=CARTESIAN_POINT ( 'NONE',  ( 3.000000000000000888, 21.97702544527767188, -6.779701584702504391 ) ) ;
#2837=ORIENTED_EDGE ( 'NONE', *, *, #7522, .T. ) ;
#2840=CARTESIAN_POINT ( 'NONE',  ( 3.000000000000000888, 8.753070780933430939, -20.78471918669851703 ) ) ;
#2841=DIRECTION ( 'NONE',  ( 0.000000000000000000, 1.000000000000000000, 3.491481338843133355E-15 ) ) ;
#2844=EDGE_CURVE ( 'NONE', #5571, #4018, #7606, .T. ) ;
#2845=DIRECTION ( 'NONE',  ( -1.000000000000000000, -0.000000000000000000, -0.000000000000000000 ) ) ;
#2846=EDGE_CURVE ( 'NONE', #1751, #11132, #6253, .T. ) ;
#2847=CARTESIAN_POINT ( 'NONE',  ( 0.000000000000000000, 22.42251312757886694, -5.117118920208269195 ) ) ;
#2848=VERTEX_POINT ( 'NONE', #11793 ) ;
#2849=AXIS2_PLACEMENT_3D ( 'NONE', #5223, #7863, #5103 ) ;
#2850=ORIENTED_EDGE ( 'NONE', *, *, #7778, .F. ) ;
#2851=ORIENTED_EDGE ( 'NONE', *, *, #5853, .T. ) ;
#2854=EDGE_CURVE ( 'NONE', #8297, #3718, #5667, .T. ) ;
#2855=DIRECTION ( 'NONE',  ( 0.000000000000000000, -0.6691306063588644548, 0.7431448254773886930 ) ) ;
#2856=CYLINDRICAL_SURFACE ( 'NONE', #5640, 9.599999999999996092 ) ;
#2857=ADVANCED_FACE ( 'NONE', ( #2431 ), #7129, .T. ) ;
#2861=ORIENTED_EDGE ( 'NONE', *, *, #3225, .T. ) ;
#2863=ORIENTED_EDGE ( 'NONE', *, *, #4074, .F. ) ;
#2864=AXIS2_PLACEMENT_3D ( 'NONE', #4111, #3201, #433 ) ;
#2865=VERTEX_POINT ( 'NONE', #8979 ) ;
#2867=CARTESIAN_POINT ( 'NONE',  ( 0.000000000000000000, -8.753070780933015271, -20.78471918669869467 ) ) ;
#2868=CARTESIAN_POINT ( 'NONE',  ( 3.000000000000000888, 23.05871956130134848, -9.128825345752797915 ) ) ;
#2869=DIRECTION ( 'NONE',  ( -1.000000000000000000, 0.000000000000000000, -0.000000000000000000 ) ) ;
#2871=VECTOR ( 'NONE', #9979, 1000.000000000000000 ) ;
#2873=CARTESIAN_POINT ( 'NONE',  ( 0.000000000000000000, -22.90635393027944744, -2.062268319295799568 ) ) ;
#2874=CARTESIAN_POINT ( 'NONE',  ( 3.000000000000000888, 0.000000000000000000, 0.000000000000000000 ) ) ;
#2876=ORIENTED_EDGE ( 'NONE', *, *, #8305, .F. ) ;
#2877=ORIENTED_EDGE ( 'NONE', *, *, #10619, .T. ) ;
#2878=CARTESIAN_POINT ( 'NONE',  ( 3.000000000000000888, -15.13242714128131361, 17.31945870441142077 ) ) ;
#2879=ORIENTED_EDGE ( 'NONE', *, *, #1828, .F. ) ;
#2880=DIRECTION ( 'NONE',  ( -1.000000000000000000, 0.000000000000000000, -0.000000000000000000 ) ) ;
#2881=EDGE_CURVE ( 'NONE', #3787, #67, #6108, .T. ) ;
#2882=CYLINDRICAL_SURFACE ( 'NONE', #1302, 24.80000000000000071 ) ;
#2885=CARTESIAN_POINT ( 'NONE',  ( 3.000000000000000888, -0.3433949777330061459, -22.99643626497957172 ) ) ;
#2888=LINE ( 'NONE', #11274, #8823 ) ;
#2889=ADVANCED_FACE ( 'NONE', ( #6895 ), #10881, .T. ) ;
#2890=CARTESIAN_POINT ( 'NONE',  ( -10.00000000000000000, 0.000000000000000000, 0.000000000000000000 ) ) ;
#2892=VERTEX_POINT ( 'NONE', #10639 ) ;
#2893=VERTEX_POINT ( 'NONE', #8060 ) ;
#2894=LINE ( 'NONE', #1059, #3144 ) ;
#2895=VERTEX_POINT ( 'NONE', #2491 ) ;
#2897=DIRECTION ( 'NONE',  ( -1.000000000000000000, 0.000000000000000000, 0.000000000000000000 ) ) ;
#2898=SHAPE_REPRESENTATION_RELATIONSHIP ( 'NONE' , 'NONE' ,  #842, #323 ) ;
#2899=AXIS2_PLACEMENT_3D ( 'NONE', #6860, #496, #8714 ) ;
#2900=LINE ( 'NONE', #6623, #344 ) ;
#2901=CARTESIAN_POINT ( 'NONE',  ( 1.500000000000000444, -11.48910920600699015, 21.97817939804034992 ) ) ;
#2903=LINE ( 'NONE', #10485, #2374 ) ;
#2904=CARTESIAN_POINT ( 'NONE',  ( 1.499999999999999556, -4.135161237383748301, 24.45282072769599679 ) ) ;
#2905=DIRECTION ( 'NONE',  ( -1.000000000000000000, 0.000000000000000000, 0.000000000000000000 ) ) ;
#2906=ORIENTED_EDGE ( 'NONE', *, *, #7311, .F. ) ;
#2908=AXIS2_PLACEMENT_3D ( 'NONE', #5122, #4950, #1148 ) ;
#2909=CIRCLE ( 'NONE', #10526, 24.80000000000000071 ) ;
#2910=ORIENTED_EDGE ( 'NONE', *, *, #5420, .T. ) ;
#2911=FACE_OUTER_BOUND ( 'NONE', #5246, .T. ) ;
#2913=CARTESIAN_POINT ( 'NONE',  ( 3.000000000000000888, -11.20082935824089354, 20.08719549084861455 ) ) ;
#2915=AXIS2_PLACEMENT_3D ( 'NONE', #8919, #8175, #7986 ) ;
#2916=ADVANCED_FACE ( 'NONE', ( #9713 ), #7006, .T. ) ;
#2917=CIRCLE ( 'NONE', #1345, 22.99899999999999523 ) ;
#2918=CARTESIAN_POINT ( 'NONE',  ( 3.000000000000000888, -11.20082935824089354, 20.08719549084861455 ) ) ;
#2919=EDGE_LOOP ( 'NONE', ( #7470, #11671, #9718, #3230 ) ) ;
#2920=EDGE_CURVE ( 'NONE', #1233, #11333, #2732, .T. ) ;
#2922=EDGE_CURVE ( 'NONE', #9017, #9796, #3229, .T. ) ;
#2923=ORIENTED_EDGE ( 'NONE', *, *, #9421, .T. ) ;
#2925=AXIS2_PLACEMENT_3D ( 'NONE', #2454, #9232, #3659 ) ;
#2926=DIRECTION ( 'NONE',  ( 0.000000000000000000, 0.9135454576426019768, -0.4067366430757979878 ) ) ;
#2927=EDGE_CURVE ( 'NONE', #11246, #531, #4289, .T. ) ;
#2928=AXIS2_PLACEMENT_3D ( 'NONE', #7633, #4954, #7754 ) ;
#2929=VERTEX_POINT ( 'NONE', #9659 ) ;
#2930=DIRECTION ( 'NONE',  ( 1.000000000000000000, 0.000000000000000000, 0.000000000000000000 ) ) ;
#2934=DIRECTION ( 'NONE',  ( 0.000000000000000000, 0.000000000000000000, 1.000000000000000000 ) ) ;
#2935=ORIENTED_EDGE ( 'NONE', *, *, #7095, .T. ) ;
#2937=DIRECTION ( 'NONE',  ( -1.000000000000000000, 0.000000000000000000, 0.000000000000000000 ) ) ;
#2938=ORIENTED_EDGE ( 'NONE', *, *, #11707, .T. ) ;
#2939=DIRECTION ( 'NONE',  ( 1.000000000000000000, -0.000000000000000000, 0.000000000000000000 ) ) ;
#2940=VECTOR ( 'NONE', #8167, 1000.000000000000000 ) ;
#2943=VERTEX_POINT ( 'NONE', #9843 ) ;
#2944=CIRCLE ( 'NONE', #6452, 24.80000000000000071 ) ;
#2945=CARTESIAN_POINT ( 'NONE',  ( 0.000000000000000000, -24.53384959170460178, 3.623565124517029279 ) ) ;
#2946=EDGE_CURVE ( 'NONE', #2802, #12019, #10148, .T. ) ;
#2947=DIRECTION ( 'NONE',  ( -1.000000000000000000, -0.000000000000000000, -0.000000000000000000 ) ) ;
#2950=CIRCLE ( 'NONE', #11350, 22.99899999999999878 ) ;
#2951=EDGE_CURVE ( 'NONE', #2739, #2827, #3353, .T. ) ;
#2954=CIRCLE ( 'NONE', #9782, 22.99899999999999878 ) ;
#2955=EDGE_LOOP ( 'NONE', ( #11604, #11561, #1097, #11687 ) ) ;
#2956=DIRECTION ( 'NONE',  ( -1.000000000000000000, -0.000000000000000000, 0.000000000000000000 ) ) ;
#2957=ORIENTED_EDGE ( 'NONE', *, *, #2951, .T. ) ;
#2958=AXIS2_PLACEMENT_3D ( 'NONE', #5748, #11366, #2988 ) ;
#2961=FACE_OUTER_BOUND ( 'NONE', #1577, .T. ) ;
#2962=EDGE_CURVE ( 'NONE', #3365, #6277, #7188, .T. ) ;
#2963=CYLINDRICAL_SURFACE ( 'NONE', #4842, 24.80000000000000071 ) ;
#2965=VECTOR ( 'NONE', #3374, 1000.000000000000000 ) ;
#2966=FACE_OUTER_BOUND ( 'NONE', #9587, .T. ) ;
#2968=DIRECTION ( 'NONE',  ( 0.000000000000000000, 0.000000000000000000, 1.000000000000000000 ) ) ;
#2969=CARTESIAN_POINT ( 'NONE',  ( 0.000000000000000000, 0.000000000000000000, 0.000000000000000000 ) ) ;
#2970=PLANE ( 'NONE',  #10560 ) ;
#2971=ORIENTED_EDGE ( 'NONE', *, *, #9082, .T. ) ;
#2972=DIRECTION ( 'NONE',  ( -1.000000000000000000, -0.000000000000000000, -0.000000000000000000 ) ) ;
#2973=CIRCLE ( 'NONE', #10786, 24.80000000000000071 ) ;
#2974=AXIS2_PLACEMENT_3D ( 'NONE', #9143, #6275, #8963 ) ;
#2975=VERTEX_POINT ( 'NONE', #11849 ) ;
#2978=DIRECTION ( 'NONE',  ( -1.000000000000000000, 0.000000000000000000, 0.000000000000000000 ) ) ;
#2979=AXIS2_PLACEMENT_3D ( 'NONE', #11697, #5156, #9870 ) ;
#2981=CIRCLE ( 'NONE', #3178, 24.80000000000000071 ) ;
#2983=CARTESIAN_POINT ( 'NONE',  ( 3.000000000000000888, 22.47229024614977533, 1.901833551798334909 ) ) ;
#2984=VERTEX_POINT ( 'NONE', #9044 ) ;
#2986=CYLINDRICAL_SURFACE ( 'NONE', #6402, 24.80000000000000071 ) ;
#2987=CIRCLE ( 'NONE', #4946, 9.599999999999996092 ) ;
#2988=DIRECTION ( 'NONE',  ( 0.000000000000000000, 0.000000000000000000, 1.000000000000000000 ) ) ;
#2989=ORIENTED_EDGE ( 'NONE', *, *, #2946, .T. ) ;
#2990=DIRECTION ( 'NONE',  ( -1.000000000000000000, 0.000000000000000000, 0.000000000000000000 ) ) ;
#2991=CARTESIAN_POINT ( 'NONE',  ( 3.000000000000000888, -4.445336973061013275, 22.56530478845647991 ) ) ;
#2992=DIRECTION ( 'NONE',  ( -1.000000000000000000, 0.000000000000000000, 0.000000000000000000 ) ) ;
#2993=EDGE_CURVE ( 'NONE', #8735, #2776, #3712, .T. ) ;
#2995=CIRCLE ( 'NONE', #4174, 9.599999999999997868 ) ;
#2996=EDGE_CURVE ( 'NONE', #3964, #2005, #9155, .T. ) ;
#2997=CARTESIAN_POINT ( 'NONE',  ( 3.000000000000000888, 0.000000000000000000, 0.000000000000000000 ) ) ;
#2999=ORIENTED_EDGE ( 'NONE', *, *, #2881, .T. ) ;
#3003=VERTEX_POINT ( 'NONE', #137 ) ;
#3004=LINE ( 'NONE', #11619, #12087 ) ;
#3005=CARTESIAN_POINT ( 'NONE',  ( 1.500000000000000444, 9.128825345753341480, -23.05871956130112821 ) ) ;
#3006=CIRCLE ( 'NONE', #6130, 9.599999999999997868 ) ;
#3007=CARTESIAN_POINT ( 'NONE',  ( 3.000000000000000888, -20.78471918669866270, 8.753070780933086326 ) ) ;
#3008=ORIENTED_EDGE ( 'NONE', *, *, #8254, .F. ) ;
#3010=CARTESIAN_POINT ( 'NONE',  ( 3.000000000000000888, 4.240409074144393387, -22.15038895030644639 ) ) ;
#3011=EDGE_CURVE ( 'NONE', #7440, #4186, #7224, .T. ) ;
#3014=DIRECTION ( 'NONE',  ( -1.000000000000000000, 0.000000000000000000, 0.000000000000000000 ) ) ;
#3015=ORIENTED_EDGE ( 'NONE', *, *, #2466, .T. ) ;
#3016=DIRECTION ( 'NONE',  ( -1.000000000000000000, -0.000000000000000000, 0.000000000000000000 ) ) ;
#3017=CIRCLE ( 'NONE', #9263, 9.599999999999997868 ) ;
#3019=VERTEX_POINT ( 'NONE', #5376 ) ;
#3020=DIRECTION ( 'NONE',  ( -1.000000000000000000, 0.000000000000000000, 0.000000000000000000 ) ) ;
#3021=ORIENTED_EDGE ( 'NONE', *, *, #2250, .T. ) ;
#3022=EDGE_CURVE ( 'NONE', #5920, #5848, #8609, .T. ) ;
#3024=DIRECTION ( 'NONE',  ( 0.000000000000000000, -0.9781476007338034684, -0.2079116908177699174 ) ) ;
#3025=ORIENTED_EDGE ( 'NONE', *, *, #11966, .F. ) ;
#3026=DIRECTION ( 'NONE',  ( -1.000000000000000000, 0.000000000000000000, 0.000000000000000000 ) ) ;
#3027=ADVANCED_FACE ( 'NONE', ( #8487 ), #4512, .T. ) ;
#3028=DIRECTION ( 'NONE',  ( 0.000000000000000000, 0.000000000000000000, 1.000000000000000000 ) ) ;
#3030=DIRECTION ( 'NONE',  ( -1.000000000000000000, 0.000000000000000000, 0.000000000000000000 ) ) ;
#3032=DIRECTION ( 'NONE',  ( 1.000000000000000000, 0.000000000000000000, 0.000000000000000000 ) ) ;
#3033=VERTEX_POINT ( 'NONE', #1575 ) ;
#3034=DIRECTION ( 'NONE',  ( -1.000000000000000000, 0.000000000000000000, 0.000000000000000000 ) ) ;
#3035=AXIS2_PLACEMENT_3D ( 'NONE', #2589, #9252, #3385 ) ;
#3036=ORIENTED_EDGE ( 'NONE', *, *, #6940, .F. ) ;
#3037=ORIENTED_EDGE ( 'NONE', *, *, #114, .F. ) ;
#3038=LINE ( 'NONE', #2167, #4652 ) ;
#3040=EDGE_CURVE ( 'NONE', #3003, #2082, #12116, .T. ) ;
#3045=ORIENTED_EDGE ( 'NONE', *, *, #1115, .F. ) ;
#3046=ADVANCED_FACE ( 'NONE', ( #6353 ), #3538, .T. ) ;
#3047=ORIENTED_EDGE ( 'NONE', *, *, #5684, .T. ) ;
#3048=FACE_OUTER_BOUND ( 'NONE', #5578, .T. ) ;
#3049=CIRCLE ( 'NONE', #301, 9.599999999999997868 ) ;
#3050=DIRECTION ( 'NONE',  ( -1.000000000000000000, -0.000000000000000000, -0.000000000000000000 ) ) ;
#3051=DIRECTION ( 'NONE',  ( -1.000000000000000000, -0.000000000000000000, -0.000000000000000000 ) ) ;
#3054=AXIS2_PLACEMENT_3D ( 'NONE', #620, #4352, #8270 ) ;
#3055=DIRECTION ( 'NONE',  ( 1.000000000000000000, 0.000000000000000000, 0.000000000000000000 ) ) ;
#3056=VERTEX_POINT ( 'NONE', #1696 ) ;
#3057=ORIENTED_EDGE ( 'NONE', *, *, #1238, .F. ) ;
#3059=CARTESIAN_POINT ( 'NONE',  ( -10.00000000000000000, 0.000000000000000000, 0.000000000000000000 ) ) ;
#3061=CARTESIAN_POINT ( 'NONE',  ( 3.000000000000000888, 1.039229259764488544, 24.77821629063822328 ) ) ;
#3063=DIRECTION ( 'NONE',  ( -1.000000000000000000, -0.000000000000000000, 0.000000000000000000 ) ) ;
#3064=AXIS2_PLACEMENT_3D ( 'NONE', #3007, #1842, #10461 ) ;
#3065=ORIENTED_EDGE ( 'NONE', *, *, #1526, .T. ) ;
#3066=EDGE_CURVE ( 'NONE', #3787, #3750, #7421, .T. ) ;
#3067=CARTESIAN_POINT ( 'NONE',  ( 3.000000000000000888, 17.31945870441167301, -15.13242714128102406 ) ) ;
#3068=DIRECTION ( 'NONE',  ( -1.000000000000000000, -0.000000000000000000, -0.000000000000000000 ) ) ;
#3070=EDGE_CURVE ( 'NONE', #8369, #11808, #6408, .T. ) ;
#3071=LINE ( 'NONE', #4207, #3766 ) ;
#3072=ORIENTED_EDGE ( 'NONE', *, *, #11884, .T. ) ;
#3073=CYLINDRICAL_SURFACE ( 'NONE', #4313, 4.000000000000000000 ) ;
#3075=DIRECTION ( 'NONE',  ( 0.000000000000000000, -0.9781476007338034684, -0.2079116908177697509 ) ) ;
#3076=VERTEX_POINT ( 'NONE', #8182 ) ;
#3077=EDGE_CURVE ( 'NONE', #11191, #5192, #3882, .T. ) ;
#3079=EDGE_CURVE ( 'NONE', #2393, #4550, #8416, .T. ) ;
#3080=CARTESIAN_POINT ( 'NONE',  ( 0.000000000000000000, 7.402892494506579268, -21.30300407174355115 ) ) ;
#3081=ADVANCED_FACE ( 'NONE', ( #4448 ), #9224, .T. ) ;
#3083=CYLINDRICAL_SURFACE ( 'NONE', #11489, 22.99899999999999878 ) ;
#3086=FACE_OUTER_BOUND ( 'NONE', #11136, .T. ) ;
#3089=CARTESIAN_POINT ( 'NONE',  ( 3.000000000000000888, 16.45023496161686438, -15.42759117534368407 ) ) ;
#3090=EDGE_LOOP ( 'NONE', ( #4394, #8170, #6767, #5287 ) ) ;
#3091=ORIENTED_EDGE ( 'NONE', *, *, #9839, .F. ) ;
#3092=AXIS2_PLACEMENT_3D ( 'NONE', #12069, #4675, #3695 ) ;
#3093=DIRECTION ( 'NONE',  ( -1.000000000000000000, 0.000000000000000000, 0.000000000000000000 ) ) ;
#3095=DIRECTION ( 'NONE',  ( -1.000000000000000000, -0.000000000000000000, -0.000000000000000000 ) ) ;
#3096=CARTESIAN_POINT ( 'NONE',  ( 0.000000000000000000, 4.445336973061169594, -22.56530478845644438 ) ) ;
#3099=DIRECTION ( 'NONE',  ( 0.000000000000000000, 0.000000000000000000, 1.000000000000000000 ) ) ;
#3100=CIRCLE ( 'NONE', #9543, 9.599999999999996092 ) ;
#3101=CARTESIAN_POINT ( 'NONE',  ( 0.000000000000000000, 7.402892494506291499, 21.30300407174365063 ) ) ;
#3102=ORIENTED_EDGE ( 'NONE', *, *, #1127, .T. ) ;
#3106=CARTESIAN_POINT ( 'NONE',  ( 0.000000000000000000, 21.58580335785676496, 6.532525787311040943 ) ) ;
#3108=VECTOR ( 'NONE', #4214, 1000.000000000000000 ) ;
#3109=DIRECTION ( 'NONE',  ( -1.000000000000000000, 0.000000000000000000, 0.000000000000000000 ) ) ;
#3110=CYLINDRICAL_SURFACE ( 'NONE', #7783, 18.49999999999999645 ) ;
#3112=EDGE_CURVE ( 'NONE', #4077, #2329, #7817, .T. ) ;
#3114=DIRECTION ( 'NONE',  ( 0.000000000000000000, 0.000000000000000000, -1.000000000000000000 ) ) ;
#3115=ORIENTED_EDGE ( 'NONE', *, *, #2795, .T. ) ;
#3116=ORIENTED_EDGE ( 'NONE', *, *, #4369, .F. ) ;
#3118=EDGE_LOOP ( 'NONE', ( #10774, #3702, #10024, #902 ) ) ;
#3120=CARTESIAN_POINT ( 'NONE',  ( 3.000000000000000888, -0.4575788569250363036, -22.54798042742718778 ) ) ;
#3121=CARTESIAN_POINT ( 'NONE',  ( 0.000000000000000000, 0.000000000000000000, 4.000000000000000000 ) ) ;
#3123=ORIENTED_EDGE ( 'NONE', *, *, #4897, .F. ) ;
#3125=AXIS2_PLACEMENT_3D ( 'NONE', #10449, #2066, #283 ) ;
#3126=FACE_OUTER_BOUND ( 'NONE', #9611, .T. ) ;
#3127=DIRECTION ( 'NONE',  ( 0.000000000000000000, 0.000000000000000000, -1.000000000000000000 ) ) ;
#3129=ORIENTED_EDGE ( 'NONE', *, *, #4791, .F. ) ;
#3130=DIRECTION ( 'NONE',  ( -1.000000000000000000, 0.000000000000000000, 0.000000000000000000 ) ) ;
#3131=DIRECTION ( 'NONE',  ( 1.000000000000000000, 0.000000000000000000, 0.000000000000000000 ) ) ;
#3132=CIRCLE ( 'NONE', #2543, 22.99900000000000233 ) ;
#3135=DIRECTION ( 'NONE',  ( 1.000000000000000000, 0.000000000000000000, 0.000000000000000000 ) ) ;
#3136=CARTESIAN_POINT ( 'NONE',  ( 3.000000000000000888, 22.90635393027949007, -2.062268319295327057 ) ) ;
#3137=CARTESIAN_POINT ( 'NONE',  ( 3.000000000000000888, -10.87771529938174808, 19.75591328264882662 ) ) ;
#3139=VECTOR ( 'NONE', #3262, 1000.000000000000000 ) ;
#3140=CYLINDRICAL_SURFACE ( 'NONE', #10977, 9.599999999999997868 ) ;
#3141=CIRCLE ( 'NONE', #1793, 22.99900000000000233 ) ;
#3142=DIRECTION ( 'NONE',  ( 0.000000000000000000, 0.4067366430757948792, 0.9135454576426033091 ) ) ;
#3143=EDGE_CURVE ( 'NONE', #8458, #2310, #11336, .T. ) ;
#3144=VECTOR ( 'NONE', #8213, 1000.000000000000000 ) ;
#3145=DIRECTION ( 'NONE',  ( -1.000000000000000000, 0.000000000000000000, 0.000000000000000000 ) ) ;
#3147=ORIENTED_EDGE ( 'NONE', *, *, #11513, .F. ) ;
#3148=EDGE_CURVE ( 'NONE', #916, #4929, #9765, .T. ) ;
#3149=DIRECTION ( 'NONE',  ( 0.000000000000000000, 0.000000000000000000, 1.000000000000000000 ) ) ;
#3150=ORIENTED_EDGE ( 'NONE', *, *, #9355, .F. ) ;
#3151=ORIENTED_EDGE ( 'NONE', *, *, #3784, .T. ) ;
#3152=ORIENTED_EDGE ( 'NONE', *, *, #5032, .F. ) ;
#3153=AXIS2_PLACEMENT_3D ( 'NONE', #1169, #248, #11453 ) ;
#3154=VECTOR ( 'NONE', #3479, 1000.000000000000000 ) ;
#3155=DIRECTION ( 'NONE',  ( -1.000000000000000000, 0.000000000000000000, 0.000000000000000000 ) ) ;
#3157=AXIS2_PLACEMENT_3D ( 'NONE', #2688, #12049, #3669 ) ;
#3161=EDGE_CURVE ( 'NONE', #2212, #7191, #6867, .T. ) ;
#3164=CARTESIAN_POINT ( 'NONE',  ( 3.000000000000000888, 0.000000000000000000, 0.000000000000000000 ) ) ;
#3165=VECTOR ( 'NONE', #9887, 1000.000000000000000 ) ;
#3166=VERTEX_POINT ( 'NONE', #9572 ) ;
#3167=ORIENTED_EDGE ( 'NONE', *, *, #1272, .T. ) ;
#3168=DIRECTION ( 'NONE',  ( -1.000000000000000000, 0.000000000000000000, 0.000000000000000000 ) ) ;
#3169=EDGE_CURVE ( 'NONE', #3019, #2610, #2343, .T. ) ;
#3173=AXIS2_PLACEMENT_3D ( 'NONE', #1347, #10655, #7026 ) ;
#3174=EDGE_CURVE ( 'NONE', #6126, #1881, #5675, .T. ) ;
#3176=DIRECTION ( 'NONE',  ( 0.000000000000000000, 0.000000000000000000, 1.000000000000000000 ) ) ;
#3177=ORIENTED_EDGE ( 'NONE', *, *, #11615, .T. ) ;
#3178=AXIS2_PLACEMENT_3D ( 'NONE', #8006, #11860, #11745 ) ;
#3179=ORIENTED_EDGE ( 'NONE', *, *, #6335, .F. ) ;
#3182=EDGE_CURVE ( 'NONE', #6885, #9763, #3529, .T. ) ;
#3184=CARTESIAN_POINT ( 'NONE',  ( 3.000000000000000888, -16.45023496161675780, 15.42759117534379953 ) ) ;
#3185=DIRECTION ( 'NONE',  ( -1.000000000000000000, 0.000000000000000000, 0.000000000000000000 ) ) ;
#3186=DIRECTION ( 'NONE',  ( 0.000000000000000000, 0.000000000000000000, 1.000000000000000000 ) ) ;
#3187=VERTEX_POINT ( 'NONE', #1128 ) ;
#3189=DIRECTION ( 'NONE',  ( -1.000000000000000000, -0.000000000000000000, 0.000000000000000000 ) ) ;
#3190=CYLINDRICAL_SURFACE ( 'NONE', #7662, 9.599999999999997868 ) ;
#3192=CIRCLE ( 'NONE', #10020, 22.99899999999999523 ) ;
#3193=CARTESIAN_POINT ( 'NONE',  ( 0.000000000000000000, -22.37663021667341923, -2.811977935938010376 ) ) ;
#3194=ORIENTED_EDGE ( 'NONE', *, *, #4791, .T. ) ;
#3195=EDGE_CURVE ( 'NONE', #2893, #1721, #10362, .T. ) ;
#3197=ADVANCED_FACE ( 'NONE', ( #4860 ), #1365, .T. ) ;
#3198=ORIENTED_EDGE ( 'NONE', *, *, #11230, .T. ) ;
#3199=AXIS2_PLACEMENT_3D ( 'NONE', #1105, #11169, #6492 ) ;
#3201=DIRECTION ( 'NONE',  ( -1.000000000000000000, -0.000000000000000000, 0.000000000000000000 ) ) ;
#3202=DIRECTION ( 'NONE',  ( 0.000000000000000000, -0.1045284632676607151, 0.9945218953682726237 ) ) ;
#3203=DIRECTION ( 'NONE',  ( -1.000000000000000000, 0.000000000000000000, -0.000000000000000000 ) ) ;
#3205=DIRECTION ( 'NONE',  ( -1.000000000000000000, 0.000000000000000000, -0.000000000000000000 ) ) ;
#3206=LINE ( 'NONE', #2046, #6892 ) ;
#3207=DIRECTION ( 'NONE',  ( -1.000000000000000000, 0.000000000000000000, -0.000000000000000000 ) ) ;
#3208=EDGE_LOOP ( 'NONE', ( #9036, #11751, #11869, #2989 ) ) ;
#3209=CARTESIAN_POINT ( 'NONE',  ( 0.000000000000000000, 20.08719549084865008, 11.20082935824082249 ) ) ;
#3210=ORIENTED_EDGE ( 'NONE', *, *, #7311, .T. ) ;
#3211=CIRCLE ( 'NONE', #6345, 9.599999999999997868 ) ;
#3212=CARTESIAN_POINT ( 'NONE',  ( 3.000000000000000888, -20.65684170206499815, 13.72351598154890873 ) ) ;
#3213=DIRECTION ( 'NONE',  ( -1.000000000000000000, 0.000000000000000000, 0.000000000000000000 ) ) ;
#3214=EDGE_CURVE ( 'NONE', #6896, #1851, #5086, .T. ) ;
#3215=CARTESIAN_POINT ( 'NONE',  ( 0.000000000000000000, 16.85990652506920995, -15.64281154287580655 ) ) ;
#3218=FACE_OUTER_BOUND ( 'NONE', #8138, .T. ) ;
#3219=CIRCLE ( 'NONE', #8101, 22.99900000000000233 ) ;
#3220=DIRECTION ( 'NONE',  ( 0.000000000000000000, 0.000000000000000000, 1.000000000000000000 ) ) ;
#3221=VERTEX_POINT ( 'NONE', #7674 ) ;
#3222=EDGE_LOOP ( 'NONE', ( #4062, #1669, #3129, #10941 ) ) ;
#3223=EDGE_CURVE ( 'NONE', #3003, #9318, #4125, .T. ) ;
#3224=FACE_OUTER_BOUND ( 'NONE', #9802, .T. ) ;
#3225=EDGE_CURVE ( 'NONE', #9776, #2419, #6057, .T. ) ;
#3226=CARTESIAN_POINT ( 'NONE',  ( 3.000000000000000888, 11.02759168516745270, 22.21333432029567945 ) ) ;
#3227=CARTESIAN_POINT ( 'NONE',  ( 3.000000000000000888, -9.589108953447752270, -20.41249101028221702 ) ) ;
#3229=LINE ( 'NONE', #10753, #3313 ) ;
#3230=ORIENTED_EDGE ( 'NONE', *, *, #9191, .T. ) ;
#3231=ORIENTED_EDGE ( 'NONE', *, *, #338, .T. ) ;
#3232=AXIS2_PLACEMENT_3D ( 'NONE', #10434, #9515, #1132 ) ;
#3234=VERTEX_POINT ( 'NONE', #4986 ) ;
#3235=DIRECTION ( 'NONE',  ( -1.000000000000000000, 0.000000000000000000, -0.000000000000000000 ) ) ;
#3236=DIRECTION ( 'NONE',  ( -1.000000000000000000, 0.000000000000000000, 0.000000000000000000 ) ) ;
#3237=CARTESIAN_POINT ( 'NONE',  ( 0.000000000000000000, -9.128825345753185161, 23.05871956130119571 ) ) ;
#3238=ORIENTED_EDGE ( 'NONE', *, *, #9057, .T. ) ;
#3239=DIRECTION ( 'NONE',  ( 0.000000000000000000, 0.8660254037844363761, 0.5000000000000039968 ) ) ;
#3240=AXIS2_PLACEMENT_3D ( 'NONE', #733, #7273, #10900 ) ;
#3241=CARTESIAN_POINT ( 'NONE',  ( 3.000000000000000888, 22.99643626497956816, -0.3433949777332470088 ) ) ;
#3243=ORIENTED_EDGE ( 'NONE', *, *, #8781, .T. ) ;
#3245=LINE ( 'NONE', #4225, #2588 ) ;
#3246=DIRECTION ( 'NONE',  ( 0.000000000000000000, 0.000000000000000000, 1.000000000000000000 ) ) ;
#3247=ORIENTED_EDGE ( 'NONE', *, *, #8564, .T. ) ;
#3248=EDGE_CURVE ( 'NONE', #8050, #1912, #11144, .T. ) ;
#3249=AXIS2_PLACEMENT_3D ( 'NONE', #6957, #11675, #4035 ) ;
#3251=ORIENTED_EDGE ( 'NONE', *, *, #590, .T. ) ;
#3252=FACE_OUTER_BOUND ( 'NONE', #4890, .T. ) ;
#3254=VERTEX_POINT ( 'NONE', #6807 ) ;
#3255=DIRECTION ( 'NONE',  ( -1.000000000000000000, -0.000000000000000000, 0.000000000000000000 ) ) ;
#3256=EDGE_CURVE ( 'NONE', #10797, #12019, #1373, .T. ) ;
#3257=CARTESIAN_POINT ( 'NONE',  ( 3.000000000000000888, -18.40266524480597710, 13.79477846460790147 ) ) ;
#3260=CARTESIAN_POINT ( 'NONE',  ( 0.000000000000000000, 22.54798042742718067, 9.142421143074731305 ) ) ;
#3262=DIRECTION ( 'NONE',  ( -1.000000000000000000, 0.000000000000000000, -0.000000000000000000 ) ) ;
#3264=ORIENTED_EDGE ( 'NONE', *, *, #3419, .F. ) ;
#3265=CIRCLE ( 'NONE', #2678, 9.599999999999997868 ) ;
#3266=FACE_OUTER_BOUND ( 'NONE', #1599, .T. ) ;
#3268=CARTESIAN_POINT ( 'NONE',  ( 3.000000000000000888, 11.79560690673899970, -19.74380051311527495 ) ) ;
#3271=CYLINDRICAL_SURFACE ( 'NONE', #4733, 9.599999999999997868 ) ;
#3272=CARTESIAN_POINT ( 'NONE',  ( 3.000000000000000888, 0.000000000000000000, 0.000000000000000000 ) ) ;
#3273=VERTEX_POINT ( 'NONE', #3209 ) ;
#3274=AXIS2_PLACEMENT_3D ( 'NONE', #1119, #1858, #940 ) ;
#3275=ORIENTED_EDGE ( 'NONE', *, *, #2509, .F. ) ;
#3278=ADVANCED_FACE ( 'NONE', ( #6753 ), #2164, .T. ) ;
#3279=DIRECTION ( 'NONE',  ( 0.000000000000000000, 0.000000000000000000, 1.000000000000000000 ) ) ;
#3280=CARTESIAN_POINT ( 'NONE',  ( 0.000000000000000000, 0.000000000000000000, 0.000000000000000000 ) ) ;
#3281=VECTOR ( 'NONE', #6415, 1000.000000000000000 ) ;
#3283=CYLINDRICAL_SURFACE ( 'NONE', #6490, 24.80000000000000071 ) ;
#3284=ADVANCED_FACE ( 'NONE', ( #10673 ), #8722, .T. ) ;
#3285=CARTESIAN_POINT ( 'NONE',  ( 1.500000000000000444, 17.71842311621530186, 17.35216073792446423 ) ) ;
#3286=VERTEX_POINT ( 'NONE', #9633 ) ;
#3287=EDGE_LOOP ( 'NONE', ( #6319, #3619, #6295, #2432 ) ) ;
#3289=EDGE_CURVE ( 'NONE', #10186, #9734, #2944, .T. ) ;
#3290=ORIENTED_EDGE ( 'NONE', *, *, #6642, .T. ) ;
#3291=CIRCLE ( 'NONE', #7785, 9.599999999999997868 ) ;
#3292=CARTESIAN_POINT ( 'NONE',  ( 3.000000000000000888, 17.06259499759964271, -14.74749645579993995 ) ) ;
#3293=CARTESIAN_POINT ( 'NONE',  ( 3.000000000000000888, 21.14796121233196402, 9.039786367038912474 ) ) ;
#3295=CARTESIAN_POINT ( 'NONE',  ( 3.000000000000000888, 2.745295967525994918, 22.83456483164690098 ) ) ;
#3296=VERTEX_POINT ( 'NONE', #322 ) ;
#3297=DIRECTION ( 'NONE',  ( 0.000000000000000000, 0.000000000000000000, 1.000000000000000000 ) ) ;
#3298=CARTESIAN_POINT ( 'NONE',  ( 0.000000000000000000, 0.000000000000000000, 0.000000000000000000 ) ) ;
#3301=AXIS2_PLACEMENT_3D ( 'NONE', #10748, #2426, #2614 ) ;
#3302=CARTESIAN_POINT ( 'NONE',  ( 3.000000000000000888, 21.76479567747252020, -7.432877647174977120 ) ) ;
#3304=CARTESIAN_POINT ( 'NONE',  ( 3.000000000000000888, -22.83456483164687256, -2.745295967526231173 ) ) ;
#3305=ORIENTED_EDGE ( 'NONE', *, *, #7322, .T. ) ;
#3307=CIRCLE ( 'NONE', #3513, 9.599999999999997868 ) ;
#3308=AXIS2_PLACEMENT_3D ( 'NONE', #11195, #9919, #11755 ) ;
#3309=ORIENTED_EDGE ( 'NONE', *, *, #2304, .F. ) ;
#3310=ADVANCED_FACE ( 'NONE', ( #3393 ), #504, .T. ) ;
#3311=CARTESIAN_POINT ( 'NONE',  ( 0.000000000000000000, 22.21333432029563681, 11.02759168516752908 ) ) ;
#3312=CARTESIAN_POINT ( 'NONE',  ( 0.000000000000000000, -21.96011696265487600, -5.135568396240250522 ) ) ;
#3313=VECTOR ( 'NONE', #7068, 1000.000000000000000 ) ;
#3317=ADVANCED_FACE ( 'NONE', ( #10728 ), #4422, .T. ) ;
#3318=AXIS2_PLACEMENT_3D ( 'NONE', #3773, #4687, #5790 ) ;
#3319=CARTESIAN_POINT ( 'NONE',  ( 0.000000000000000000, -22.47229024614976112, -1.901833551798492561 ) ) ;
#3321=CARTESIAN_POINT ( 'NONE',  ( 3.000000000000000888, 15.13242714128119459, 17.31945870441152380 ) ) ;
#3322=ORIENTED_EDGE ( 'NONE', *, *, #1903, .T. ) ;
#3323=CYLINDRICAL_SURFACE ( 'NONE', #6845, 22.99899999999999878 ) ;
#3324=AXIS2_PLACEMENT_3D ( 'NONE', #11526, #8777, #2285 ) ;
#3325=ORIENTED_EDGE ( 'NONE', *, *, #5385, .T. ) ;
#3326=EDGE_CURVE ( 'NONE', #384, #900, #5867, .T. ) ;
#3327=DIRECTION ( 'NONE',  ( 0.000000000000000000, 0.9135454576426019768, -0.4067366430757979878 ) ) ;
#3328=EDGE_LOOP ( 'NONE', ( #5144, #5130, #11701, #8794 ) ) ;
#3329=CARTESIAN_POINT ( 'NONE',  ( 3.000000000000000888, -14.74749645580022772, 17.06259499759939402 ) ) ;
#3332=DIRECTION ( 'NONE',  ( 0.000000000000000000, 0.000000000000000000, 1.000000000000000000 ) ) ;
#3333=LINE ( 'NONE', #6156, #1596 ) ;
#3337=FACE_OUTER_BOUND ( 'NONE', #6109, .T. ) ;
#3338=ORIENTED_EDGE ( 'NONE', *, *, #5457, .T. ) ;
#3339=EDGE_CURVE ( 'NONE', #3644, #8566, #2738, .T. ) ;
#3340=AXIS2_PLACEMENT_3D ( 'NONE', #11217, #11939, #10048 ) ;
#3342=CIRCLE ( 'NONE', #11552, 24.80000000000000071 ) ;
#3343=ORIENTED_EDGE ( 'NONE', *, *, #1341, .T. ) ;
#3345=DIRECTION ( 'NONE',  ( -1.000000000000000000, 0.000000000000000000, 0.000000000000000000 ) ) ;
#3346=DIRECTION ( 'NONE',  ( 0.000000000000000000, 0.000000000000000000, 1.000000000000000000 ) ) ;
#3347=VECTOR ( 'NONE', #12014, 1000.000000000000000 ) ;
#3348=AXIS2_PLACEMENT_3D ( 'NONE', #6351, #9101, #9154 ) ;
#3349=AXIS2_PLACEMENT_3D ( 'NONE', #1377, #4138, #394 ) ;
#3351=CIRCLE ( 'NONE', #9608, 9.599999999999997868 ) ;
#3352=CARTESIAN_POINT ( 'NONE',  ( 3.000000000000000888, -2.745295967525840375, -22.83456483164691875 ) ) ;
#3353=LINE ( 'NONE', #1749, #7414 ) ;
#3354=ORIENTED_EDGE ( 'NONE', *, *, #3195, .F. ) ;
#3355=ORIENTED_EDGE ( 'NONE', *, *, #9344, .T. ) ;
#3358=AXIS2_PLACEMENT_3D ( 'NONE', #6198, #11821, #3387 ) ;
#3359=EDGE_LOOP ( 'NONE', ( #4223, #7168, #1880, #7456 ) ) ;
#3360=DIRECTION ( 'NONE',  ( 0.000000000000000000, 0.9510565162951544194, -0.3090169943749449533 ) ) ;
#3363=CIRCLE ( 'NONE', #11543, 22.99899999999999878 ) ;
#3364=DIRECTION ( 'NONE',  ( 0.000000000000000000, 0.000000000000000000, 1.000000000000000000 ) ) ;
#3365=VERTEX_POINT ( 'NONE', #6081 ) ;
#3366=EDGE_CURVE ( 'NONE', #8825, #9990, #5282, .T. ) ;
#3367=DIRECTION ( 'NONE',  ( 0.000000000000000000, 0.000000000000000000, 1.000000000000000000 ) ) ;
#3368=ADVANCED_FACE ( 'NONE', ( #5350 ), #5162, .T. ) ;
#3369=DIRECTION ( 'NONE',  ( -1.000000000000000000, -0.000000000000000000, -0.000000000000000000 ) ) ;
#3371=VECTOR ( 'NONE', #11665, 1000.000000000000000 ) ;
#3372=AXIS2_PLACEMENT_3D ( 'NONE', #10706, #10523, #4168 ) ;
#3373=DIRECTION ( 'NONE',  ( 0.000000000000000000, 0.000000000000000000, 1.000000000000000000 ) ) ;
#3374=DIRECTION ( 'NONE',  ( 1.000000000000000000, -0.000000000000000000, -0.000000000000000000 ) ) ;
#3375=ORIENTED_EDGE ( 'NONE', *, *, #455, .F. ) ;
#3377=ADVANCED_FACE ( 'NONE', ( #7968 ), #1668, .T. ) ;
#3378=VECTOR ( 'NONE', #8494, 1000.000000000000000 ) ;
#3379=CARTESIAN_POINT ( 'NONE',  ( 3.000000000000000888, 6.168200451486087310, -24.02068490260606382 ) ) ;
#3380=CARTESIAN_POINT ( 'NONE',  ( 3.000000000000000888, -9.128825345753185161, 23.05871956130119216 ) ) ;
#3381=ORIENTED_EDGE ( 'NONE', *, *, #6288, .F. ) ;
#3382=ADVANCED_FACE ( 'NONE', ( #4362 ), #9080, .T. ) ;
#3383=LINE ( 'NONE', #11818, #8366 ) ;
#3384=CIRCLE ( 'NONE', #8477, 24.80000000000000071 ) ;
#3385=DIRECTION ( 'NONE',  ( 0.000000000000000000, 0.3090169943749480064, -0.9510565162951533091 ) ) ;
#3387=DIRECTION ( 'NONE',  ( 0.000000000000000000, 0.000000000000000000, 1.000000000000000000 ) ) ;
#3389=DIRECTION ( 'NONE',  ( -1.000000000000000000, -0.000000000000000000, 0.000000000000000000 ) ) ;
#3390=AXIS2_PLACEMENT_3D ( 'NONE', #9007, #623, #4471 ) ;
#3391=ORIENTED_EDGE ( 'NONE', *, *, #4685, .F. ) ;
#3393=FACE_OUTER_BOUND ( 'NONE', #6614, .T. ) ;
#3394=ORIENTED_EDGE ( 'NONE', *, *, #7697, .T. ) ;
#3395=AXIS2_PLACEMENT_3D ( 'NONE', #2437, #718, #11975 ) ;
#3396=AXIS2_PLACEMENT_3D ( 'NONE', #2281, #320, #3142 ) ;
#3397=DIRECTION ( 'NONE',  ( 1.000000000000000000, 0.000000000000000000, 0.000000000000000000 ) ) ;
#3398=ADVANCED_FACE ( 'NONE', ( #11702 ), #3323, .T. ) ;
#3399=CARTESIAN_POINT ( 'NONE',  ( 3.000000000000000888, -15.42759117534374447, -16.45023496161680754 ) ) ;
#3400=FILL_AREA_STYLE ('',( #816 ) ) ;
#3401=ORIENTED_EDGE ( 'NONE', *, *, #4065, .F. ) ;
#3402=CIRCLE ( 'NONE', #9256, 24.80000000000000071 ) ;
#3403=CARTESIAN_POINT ( 'NONE',  ( 3.000000000000000888, -1.556492618230808089, 24.75110766671651419 ) ) ;
#3404=CARTESIAN_POINT ( 'NONE',  ( 0.000000000000000000, 2.745295967526300451, -22.83456483164686546 ) ) ;
#3408=CARTESIAN_POINT ( 'NONE',  ( 0.000000000000000000, -11.48910920600668462, -21.97817939804051690 ) ) ;
#3409=ORIENTED_EDGE ( 'NONE', *, *, #9344, .F. ) ;
#3410=AXIS2_PLACEMENT_3D ( 'NONE', #10493, #3952, #8668 ) ;
#3411=ORIENTED_EDGE ( 'NONE', *, *, #11974, .F. ) ;
#3412=AXIS2_PLACEMENT_3D ( 'NONE', #453, #512, #7974 ) ;
#3413=ORIENTED_EDGE ( 'NONE', *, *, #5617, .F. ) ;
#3414=EDGE_CURVE ( 'NONE', #7118, #4299, #11646, .T. ) ;
#3417=CARTESIAN_POINT ( 'NONE',  ( 3.000000000000000888, 18.80635025205169697, 13.23915371906961447 ) ) ;
#3418=CIRCLE ( 'NONE', #5766, 22.99899999999999878 ) ;
#3419=EDGE_CURVE ( 'NONE', #3959, #10471, #9926, .T. ) ;
#3421=CARTESIAN_POINT ( 'NONE',  ( 3.000000000000000888, 0.3433949777334901476, -22.99643626497956461 ) ) ;
#3422=DIRECTION ( 'NONE',  ( 0.000000000000000000, 0.000000000000000000, -1.000000000000000000 ) ) ;
#3423=ORIENTED_EDGE ( 'NONE', *, *, #1149, .T. ) ;
#3424=ORIENTED_EDGE ( 'NONE', *, *, #7207, .T. ) ;
#3428=AXIS2_PLACEMENT_3D ( 'NONE', #5580, #4838, #11147 ) ;
#3429=DIRECTION ( 'NONE',  ( -1.000000000000000000, 0.000000000000000000, 0.000000000000000000 ) ) ;
#3430=DIRECTION ( 'NONE',  ( 1.000000000000000000, 0.000000000000000000, -0.000000000000000000 ) ) ;
#3431=CYLINDRICAL_SURFACE ( 'NONE', #4851, 24.80000000000000071 ) ;
#3432=EDGE_LOOP ( 'NONE', ( #6111, #4906, #2197, #6743 ) ) ;
#3433=CARTESIAN_POINT ( 'NONE',  ( 3.000000000000000888, -9.128825345752879628, -23.05871956130131650 ) ) ;
#3434=DIRECTION ( 'NONE',  ( 0.000000000000000000, -0.8660254037844433705, 0.4999999999999919509 ) ) ;
#3436=CARTESIAN_POINT ( 'NONE',  ( 0.000000000000000000, 13.23915371906955052, 18.80635025205174671 ) ) ;
#3437=DIRECTION ( 'NONE',  ( 0.000000000000000000, 0.000000000000000000, 1.000000000000000000 ) ) ;
#3438=ORIENTED_EDGE ( 'NONE', *, *, #901, .T. ) ;
#3441=DIRECTION ( 'NONE',  ( -1.000000000000000000, 0.000000000000000000, -0.000000000000000000 ) ) ;
#3442=EDGE_CURVE ( 'NONE', #4464, #4944, #5290, .T. ) ;
#3443=CARTESIAN_POINT ( 'NONE',  ( 1.499999999999999556, 24.45282072769601101, 4.135161237383664812 ) ) ;
#3444=CARTESIAN_POINT ( 'NONE',  ( 0.000000000000000000, 0.000000000000000000, 0.000000000000000000 ) ) ;
#3446=DIRECTION ( 'NONE',  ( -1.000000000000000000, 0.000000000000000000, 0.000000000000000000 ) ) ;
#3448=EDGE_CURVE ( 'NONE', #994, #6849, #11727, .T. ) ;
#3449=CARTESIAN_POINT ( 'NONE',  ( 3.000000000000000888, -18.40266524480579236, -13.79477846460815194 ) ) ;
#3451=VECTOR ( 'NONE', #11224, 1000.000000000000000 ) ;
#3452=ORIENTED_EDGE ( 'NONE', *, *, #3256, .F. ) ;
#3454=EDGE_CURVE ( 'NONE', #1309, #215, #3, .T. ) ;
#3456=EDGE_CURVE ( 'NONE', #10077, #4242, #8427, .T. ) ;
#3458=DIRECTION ( 'NONE',  ( 1.000000000000000000, -0.000000000000000000, 0.000000000000000000 ) ) ;
#3459=( NAMED_UNIT ( * ) SI_UNIT ( $, .STERADIAN. ) SOLID_ANGLE_UNIT ( ) );
#3460=VERTEX_POINT ( 'NONE', #10051 ) ;
#3461=FACE_OUTER_BOUND ( 'NONE', #9345, .T. ) ;
#3462=CIRCLE ( 'NONE', #2272, 24.80000000000000071 ) ;
#3463=DIRECTION ( 'NONE',  ( 0.000000000000000000, -0.9781476007338034684, -0.2079116908177697509 ) ) ;
#3464=CARTESIAN_POINT ( 'NONE',  ( 0.000000000000000000, 20.93895013827599882, -13.28910708463105728 ) ) ;
#3467=CARTESIAN_POINT ( 'NONE',  ( 0.000000000000000000, -1.901833551798412847, 22.47229024614976822 ) ) ;
#3468=DIRECTION ( 'NONE',  ( -1.000000000000000000, 0.000000000000000000, 0.000000000000000000 ) ) ;
#3469=VERTEX_POINT ( 'NONE', #2836 ) ;
#3473=DIRECTION ( 'NONE',  ( -1.000000000000000000, 0.000000000000000000, 0.000000000000000000 ) ) ;
#3474=EDGE_CURVE ( 'NONE', #7835, #9404, #9258, .T. ) ;
#3475=DIRECTION ( 'NONE',  ( 1.000000000000000000, 0.000000000000000000, 0.000000000000000000 ) ) ;
#3477=ADVANCED_FACE ( 'NONE', ( #11220 ), #10350, .T. ) ;
#3478=AXIS2_PLACEMENT_3D ( 'NONE', #9264, #11888, #11774 ) ;
#3479=DIRECTION ( 'NONE',  ( 1.000000000000000000, -0.000000000000000000, 0.000000000000000000 ) ) ;
#3480=DIRECTION ( 'NONE',  ( 1.000000000000000000, 0.000000000000000000, 0.000000000000000000 ) ) ;
#3481=ORIENTED_EDGE ( 'NONE', *, *, #510, .T. ) ;
#3483=EDGE_CURVE ( 'NONE', #10348, #11545, #5096, .T. ) ;
#3484=ORIENTED_EDGE ( 'NONE', *, *, #1488, .T. ) ;
#3486=FACE_OUTER_BOUND ( 'NONE', #4348, .T. ) ;
#3487=EDGE_CURVE ( 'NONE', #992, #6788, #7409, .T. ) ;
#3488=CYLINDRICAL_SURFACE ( 'NONE', #3494, 24.80000000000000071 ) ;
#3489=ORIENTED_EDGE ( 'NONE', *, *, #669, .T. ) ;
#3490=CARTESIAN_POINT ( 'NONE',  ( -10.00000000000000000, 0.000000000000000000, 0.000000000000000000 ) ) ;
#3491=DIRECTION ( 'NONE',  ( -1.000000000000000000, -0.000000000000000000, -0.000000000000000000 ) ) ;
#3493=DIRECTION ( 'NONE',  ( 1.000000000000000000, 0.000000000000000000, 0.000000000000000000 ) ) ;
#3494=AXIS2_PLACEMENT_3D ( 'NONE', #7197, #2565, #1647 ) ;
#3496=VERTEX_POINT ( 'NONE', #2648 ) ;
#3499=ORIENTED_EDGE ( 'NONE', *, *, #4122, .T. ) ;
#3500=FACE_OUTER_BOUND ( 'NONE', #9093, .T. ) ;
#3501=ORIENTED_EDGE ( 'NONE', *, *, #4499, .F. ) ;
#3502=CIRCLE ( 'NONE', #10332, 22.99899999999999878 ) ;
#3503=DIRECTION ( 'NONE',  ( -1.000000000000000000, -0.000000000000000000, 0.000000000000000000 ) ) ;
#3504=AXIS2_PLACEMENT_3D ( 'NONE', #10801, #5533, #1794 ) ;
#3505=CARTESIAN_POINT ( 'NONE',  ( -10.00000000000000000, 0.000000000000000000, 0.000000000000000000 ) ) ;
#3507=DIRECTION ( 'NONE',  ( 0.000000000000000000, 0.000000000000000000, 1.000000000000000000 ) ) ;
#3508=CARTESIAN_POINT ( 'NONE',  ( 3.000000000000000888, 17.35216073792440739, 17.71842311621536226 ) ) ;
#3509=VERTEX_POINT ( 'NONE', #3572 ) ;
#3510=ORIENTED_EDGE ( 'NONE', *, *, #6940, .T. ) ;
#3511=DIRECTION ( 'NONE',  ( 0.000000000000000000, -0.1045284632676605485, 0.9945218953682725127 ) ) ;
#3513=AXIS2_PLACEMENT_3D ( 'NONE', #2561, #1645, #9109 ) ;
#3516=VERTEX_POINT ( 'NONE', #1970 ) ;
#3517=CARTESIAN_POINT ( 'NONE',  ( 0.000000000000000000, 0.000000000000000000, 0.000000000000000000 ) ) ;
#3518=EDGE_CURVE ( 'NONE', #7676, #11174, #9589, .T. ) ;
#3522=DIRECTION ( 'NONE',  ( 0.000000000000000000, 0.9135454576425990902, 0.4067366430758041496 ) ) ;
#3523=EDGE_CURVE ( 'NONE', #9646, #6735, #5456, .T. ) ;
#3524=CARTESIAN_POINT ( 'NONE',  ( 3.000000000000000888, 4.240409074144097623, 22.15038895030650679 ) ) ;
#3525=ORIENTED_EDGE ( 'NONE', *, *, #330, .T. ) ;
#3526=ORIENTED_EDGE ( 'NONE', *, *, #11141, .F. ) ;
#3527=CIRCLE ( 'NONE', #10978, 9.599999999999997868 ) ;
#3529=CIRCLE ( 'NONE', #10160, 9.599999999999997868 ) ;
#3530=EDGE_CURVE ( 'NONE', #3286, #4143, #7830, .T. ) ;
#3531=DIRECTION ( 'NONE',  ( -1.000000000000000000, -0.000000000000000000, 0.000000000000000000 ) ) ;
#3532=CARTESIAN_POINT ( 'NONE',  ( 3.000000000000000888, 0.000000000000000000, 0.000000000000000000 ) ) ;
#3534=VECTOR ( 'NONE', #4858, 1000.000000000000000 ) ;
#3535=CARTESIAN_POINT ( 'NONE',  ( 3.000000000000000000, 0.000000000000000000, 0.000000000000000000 ) ) ;
#3536=ORIENTED_EDGE ( 'NONE', *, *, #10780, .F. ) ;
#3537=AXIS2_PLACEMENT_3D ( 'NONE', #4530, #11019, #2748 ) ;
#3538=CYLINDRICAL_SURFACE ( 'NONE', #1960, 24.80000000000000071 ) ;
#3539=EDGE_LOOP ( 'NONE', ( #356, #6886, #7903, #1472 ) ) ;
#3540=EDGE_CURVE ( 'NONE', #8199, #8745, #1762, .T. ) ;
#3541=VERTEX_POINT ( 'NONE', #6382 ) ;
#3542=CARTESIAN_POINT ( 'NONE',  ( 3.000000000000000888, 0.000000000000000000, 0.000000000000000000 ) ) ;
#3544=EDGE_CURVE ( 'NONE', #10492, #1145, #10372, .T. ) ;
#3545=AXIS2_PLACEMENT_3D ( 'NONE', #7651, #3014, #6734 ) ;
#3548=DIRECTION ( 'NONE',  ( 0.000000000000000000, 0.000000000000000000, -1.000000000000000000 ) ) ;
#3549=DIRECTION ( 'NONE',  ( 0.000000000000000000, 0.000000000000000000, 1.000000000000000000 ) ) ;
#3551=LINE ( 'NONE', #9299, #793 ) ;
#3552=ORIENTED_EDGE ( 'NONE', *, *, #1649, .F. ) ;
#3553=CIRCLE ( 'NONE', #387, 9.599999999999996092 ) ;
#3554=DIRECTION ( 'NONE',  ( -1.000000000000000000, -0.000000000000000000, 0.000000000000000000 ) ) ;
#3555=VECTOR ( 'NONE', #4435, 1000.000000000000000 ) ;
#3556=VERTEX_POINT ( 'NONE', #7284 ) ;
#3557=ORIENTED_EDGE ( 'NONE', *, *, #2263, .F. ) ;
#3559=EDGE_CURVE ( 'NONE', #5600, #9959, #7619, .T. ) ;
#3561=CARTESIAN_POINT ( 'NONE',  ( 3.000000000000000888, 6.532525787310969001, 21.58580335785678983 ) ) ;
#3562=VERTEX_POINT ( 'NONE', #7346 ) ;
#3563=MECHANICAL_DESIGN_GEOMETRIC_PRESENTATION_REPRESENTATION('',(#7661),#8844);
#3565=DIRECTION ( 'NONE',  ( 0.000000000000000000, 0.000000000000000000, 1.000000000000000000 ) ) ;
#3566=DIRECTION ( 'NONE',  ( -1.000000000000000000, 0.000000000000000000, -0.000000000000000000 ) ) ;
#3568=DIRECTION ( 'NONE',  ( 0.000000000000000000, 0.9945218953682737340, -0.1045284632676502651 ) ) ;
#3569=EDGE_CURVE ( 'NONE', #7896, #11364, #11090, .T. ) ;
#3570=CARTESIAN_POINT ( 'NONE',  ( 3.000000000000000888, -22.56530478845651544, 4.445336973060782348 ) ) ;
#3571=ORIENTED_EDGE ( 'NONE', *, *, #7802, .F. ) ;
#3572=CARTESIAN_POINT ( 'NONE',  ( 0.000000000000000000, -15.40502424595132247, -19.43515443678418819 ) ) ;
#3573=ORIENTED_EDGE ( 'NONE', *, *, #1964, .F. ) ;
#3576=AXIS2_PLACEMENT_3D ( 'NONE', #6768, #7690, #7810 ) ;
#3577=DIRECTION ( 'NONE',  ( 0.000000000000000000, 0.000000000000000000, 1.000000000000000000 ) ) ;
#3578=DIRECTION ( 'NONE',  ( 0.000000000000000000, 0.000000000000000000, 1.000000000000000000 ) ) ;
#3579=CARTESIAN_POINT ( 'NONE',  ( 3.000000000000000888, -13.62355943574006645, -17.97274125076088680 ) ) ;
#3581=AXIS2_PLACEMENT_3D ( 'NONE', #11872, #3503, #2642 ) ;
#3583=CARTESIAN_POINT ( 'NONE',  ( 0.000000000000000000, 19.74380051311539930, 11.79560690673879186 ) ) ;
#3584=DIRECTION ( 'NONE',  ( -1.000000000000000000, 0.000000000000000000, -0.000000000000000000 ) ) ;
#3585=AXIS2_PLACEMENT_3D ( 'NONE', #11853, #10942, #535 ) ;
#3586=CIRCLE ( 'NONE', #7276, 9.599999999999996092 ) ;
#3587=ORIENTED_EDGE ( 'NONE', *, *, #8008, .F. ) ;
#3588=ORIENTED_EDGE ( 'NONE', *, *, #3569, .T. ) ;
#3589=VECTOR ( 'NONE', #11859, 1000.000000000000000 ) ;
#3591=ADVANCED_FACE ( 'NONE', ( #6501 ), #6439, .T. ) ;
#3592=CARTESIAN_POINT ( 'NONE',  ( 3.000000000000000888, 0.000000000000000000, 0.000000000000000000 ) ) ;
#3593=CARTESIAN_POINT ( 'NONE',  ( -10.00000000000000000, 0.000000000000000000, 0.000000000000000000 ) ) ;
#3594=EDGE_CURVE ( 'NONE', #2892, #1098, #4670, .T. ) ;
#3598=EDGE_CURVE ( 'NONE', #1833, #9333, #9002, .T. ) ;
#3599=DIRECTION ( 'NONE',  ( 0.000000000000000000, 0.000000000000000000, 1.000000000000000000 ) ) ;
#3600=VERTEX_POINT ( 'NONE', #2 ) ;
#3601=ORIENTED_EDGE ( 'NONE', *, *, #72, .T. ) ;
#3602=ADVANCED_FACE ( 'NONE', ( #3752 ), #5645, .T. ) ;
#3605=EDGE_CURVE ( 'NONE', #5315, #4337, #2894, .T. ) ;
#3606=DIRECTION ( 'NONE',  ( -1.000000000000000000, 0.000000000000000000, 0.000000000000000000 ) ) ;
#3607=CIRCLE ( 'NONE', #275, 22.99899999999999878 ) ;
#3608=CARTESIAN_POINT ( 'NONE',  ( 3.000000000000000888, -0.3433949777330061459, -22.99643626497957172 ) ) ;
#3609=CARTESIAN_POINT ( 'NONE',  ( 3.000000000000000888, -23.24434456306330787, 8.645255683528924706 ) ) ;
#3610=FACE_OUTER_BOUND ( 'NONE', #11502, .T. ) ;
#3611=DIRECTION ( 'NONE',  ( -1.000000000000000000, 0.000000000000000000, 0.000000000000000000 ) ) ;
#3612=DIRECTION ( 'NONE',  ( -1.000000000000000000, -0.000000000000000000, 0.000000000000000000 ) ) ;
#3613=DIRECTION ( 'NONE',  ( 0.000000000000000000, 0.1045284632676538872, -0.9945218953682732899 ) ) ;
#3614=AXIS2_PLACEMENT_3D ( 'NONE', #3505, #1717, #5451 ) ;
#3616=CARTESIAN_POINT ( 'NONE',  ( 3.000000000000000888, -11.67026512804534022, -19.29833442572371638 ) ) ;
#3617=ORIENTED_EDGE ( 'NONE', *, *, #5534, .T. ) ;
#3619=ORIENTED_EDGE ( 'NONE', *, *, #10045, .F. ) ;
#3620=CARTESIAN_POINT ( 'NONE',  ( 1.499999999999999556, 20.93895013827599882, -13.28910708463105905 ) ) ;
#3622=FACE_OUTER_BOUND ( 'NONE', #7926, .T. ) ;
#3623=DIRECTION ( 'NONE',  ( -1.000000000000000000, -0.000000000000000000, 0.000000000000000000 ) ) ;
#3625=DIRECTION ( 'NONE',  ( -1.000000000000000000, 0.000000000000000000, -0.000000000000000000 ) ) ;
#3626=ADVANCED_FACE ( 'NONE', ( #11941 ), #2211, .T. ) ;
#3627=DIRECTION ( 'NONE',  ( 0.000000000000000000, 0.000000000000000000, 1.000000000000000000 ) ) ;
#3628=ORIENTED_EDGE ( 'NONE', *, *, #2645, .F. ) ;
#3629=DIRECTION ( 'NONE',  ( -1.000000000000000000, -0.000000000000000000, 0.000000000000000000 ) ) ;
#3630=VERTEX_POINT ( 'NONE', #9621 ) ;
#3631=AXIS2_PLACEMENT_3D ( 'NONE', #10369, #1992, #3886 ) ;
#3633=DIRECTION ( 'NONE',  ( -1.000000000000000000, -0.000000000000000000, 0.000000000000000000 ) ) ;
#3634=( LENGTH_UNIT ( ) NAMED_UNIT ( * ) SI_UNIT ( .MILLI., .METRE. ) );
#3635=ADVANCED_FACE ( 'NONE', ( #8586 ), #7720, .T. ) ;
#3636=CYLINDRICAL_SURFACE ( 'NONE', #1317, 24.80000000000000071 ) ;
#3637=CARTESIAN_POINT ( 'NONE',  ( 0.000000000000000000, 18.51065745848395849, -12.88318129270159673 ) ) ;
#3638=CARTESIAN_POINT ( 'NONE',  ( 3.000000000000000888, -22.15038895030646060, -4.240409074144325885 ) ) ;
#3640=CIRCLE ( 'NONE', #4220, 24.80000000000000071 ) ;
#3642=DIRECTION ( 'NONE',  ( -1.000000000000000000, -0.000000000000000000, 0.000000000000000000 ) ) ;
#3644=VERTEX_POINT ( 'NONE', #4909 ) ;
#3645=ORIENTED_EDGE ( 'NONE', *, *, #10819, .T. ) ;
#3646=VECTOR ( 'NONE', #2316, 1000.000000000000000 ) ;
#3647=DIRECTION ( 'NONE',  ( 0.000000000000000000, 0.7431448254773954654, -0.6691306063588569053 ) ) ;
#3649=CARTESIAN_POINT ( 'NONE',  ( 0.000000000000000000, -0.3433949777330061459, -22.99643626497957172 ) ) ;
#3653=DIRECTION ( 'NONE',  ( 0.000000000000000000, -0.4067366430758070917, 0.9135454576425978690 ) ) ;
#3654=EDGE_LOOP ( 'NONE', ( #1516, #11152, #7871, #2286 ) ) ;
#3655=ORIENTED_EDGE ( 'NONE', *, *, #8462, .T. ) ;
#3657=EDGE_CURVE ( 'NONE', #3187, #1049, #1171, .T. ) ;
#3658=DIRECTION ( 'NONE',  ( 0.000000000000000000, -0.8660254037844432595, 0.4999999999999919509 ) ) ;
#3659=DIRECTION ( 'NONE',  ( 0.000000000000000000, -0.4999999999999887867, -0.8660254037844452579 ) ) ;
#3660=CARTESIAN_POINT ( 'NONE',  ( 0.000000000000000000, 22.37663021667340146, 2.811977935938166695 ) ) ;
#3661=CYLINDRICAL_SURFACE ( 'NONE', #6520, 22.99899999999999878 ) ;
#3662=EDGE_CURVE ( 'NONE', #9763, #8613, #9978, .T. ) ;
#3665=EDGE_CURVE ( 'NONE', #4817, #10068, #1236, .T. ) ;
#3666=DIRECTION ( 'NONE',  ( -1.000000000000000000, 0.000000000000000000, -0.000000000000000000 ) ) ;
#3668=ORIENTED_EDGE ( 'NONE', *, *, #4723, .F. ) ;
#3669=DIRECTION ( 'NONE',  ( 0.000000000000000000, -0.8090169943749526693, 0.5877852522924660317 ) ) ;
#3670=ORIENTED_EDGE ( 'NONE', *, *, #4237, .F. ) ;
#3671=AXIS2_PLACEMENT_3D ( 'NONE', #5152, #6800, #2219 ) ;
#3674=ORIENTED_EDGE ( 'NONE', *, *, #2220, .F. ) ;
#3675=CARTESIAN_POINT ( 'NONE',  ( 3.000000000000000888, -15.64281154287608722, 16.85990652506894705 ) ) ;
#3676=ORIENTED_EDGE ( 'NONE', *, *, #1800, .T. ) ;
#3677=EDGE_CURVE ( 'NONE', #2252, #9316, #3920, .T. ) ;
#3678=DIRECTION ( 'NONE',  ( -1.000000000000000000, 0.000000000000000000, 0.000000000000000000 ) ) ;
#3679=FACE_OUTER_BOUND ( 'NONE', #7043, .T. ) ;
#3681=AXIS2_PLACEMENT_3D ( 'NONE', #1521, #8131, #10831 ) ;
#3682=AXIS2_PLACEMENT_3D ( 'NONE', #9836, #1386, #3279 ) ;
#3683=CARTESIAN_POINT ( 'NONE',  ( 0.000000000000000000, -19.43515443678392529, -15.40502424595165110 ) ) ;
#3684=DIRECTION ( 'NONE',  ( -1.000000000000000000, -0.000000000000000000, -0.000000000000000000 ) ) ;
#3685=ORIENTED_EDGE ( 'NONE', *, *, #10130, .T. ) ;
#3686=ORIENTED_EDGE ( 'NONE', *, *, #6441, .T. ) ;
#3687=DIRECTION ( 'NONE',  ( 0.000000000000000000, 0.9945218953682737340, -0.1045284632676502373 ) ) ;
#3688=EDGE_LOOP ( 'NONE', ( #8294, #3501, #10227, #5318 ) ) ;
#3689=EDGE_CURVE ( 'NONE', #5192, #10351, #11155, .T. ) ;
#3691=AXIS2_PLACEMENT_3D ( 'NONE', #5134, #10646, #10518 ) ;
#3693=CARTESIAN_POINT ( 'NONE',  ( 3.000000000000000888, 8.645255683529311952, -23.24434456306316577 ) ) ;
#3694=EDGE_CURVE ( 'NONE', #1936, #3509, #1292, .T. ) ;
#3695=DIRECTION ( 'NONE',  ( 0.000000000000000000, 0.000000000000000000, -1.000000000000000000 ) ) ;
#3698=LINE ( 'NONE', #132, #2763 ) ;
#3699=DIRECTION ( 'NONE',  ( -1.000000000000000000, 0.000000000000000000, 0.000000000000000000 ) ) ;
#3700=CIRCLE ( 'NONE', #9948, 9.599999999999996092 ) ;
#3702=ORIENTED_EDGE ( 'NONE', *, *, #6580, .F. ) ;
#3703=EDGE_CURVE ( 'NONE', #7676, #2929, #3994, .T. ) ;
#3704=ORIENTED_EDGE ( 'NONE', *, *, #9712, .F. ) ;
#3705=FACE_OUTER_BOUND ( 'NONE', #9244, .T. ) ;
#3707=VECTOR ( 'NONE', #6302, 1000.000000000000000 ) ;
#3708=CIRCLE ( 'NONE', #4689, 24.80000000000000071 ) ;
#3709=DIRECTION ( 'NONE',  ( -1.000000000000000000, 0.000000000000000000, 0.000000000000000000 ) ) ;
#3711=DIRECTION ( 'NONE',  ( 0.000000000000000000, -6.982962677686266711E-15, 1.000000000000000000 ) ) ;
#3712=CIRCLE ( 'NONE', #8407, 9.599999999999996092 ) ;
#3714=CARTESIAN_POINT ( 'NONE',  ( 3.000000000000000888, -20.93895013827572171, -13.28910708463150492 ) ) ;
#3716=ORIENTED_EDGE ( 'NONE', *, *, #5841, .F. ) ;
#3717=AXIS2_PLACEMENT_3D ( 'NONE', #11765, #2342, #3511 ) ;
#3718=VERTEX_POINT ( 'NONE', #8708 ) ;
#3719=DIRECTION ( 'NONE',  ( -1.000000000000000000, 0.000000000000000000, 0.000000000000000000 ) ) ;
#3720=CARTESIAN_POINT ( 'NONE',  ( 1.500000000000000444, -24.45282072769603587, 4.135161237383498722 ) ) ;
#3722=LINE ( 'NONE', #6536, #545 ) ;
#3723=AXIS2_PLACEMENT_3D ( 'NONE', #1183, #9509, #11467 ) ;
#3725=VECTOR ( 'NONE', #3815, 1000.000000000000000 ) ;
#3729=DIRECTION ( 'NONE',  ( 0.000000000000000000, 0.6691306063588593478, -0.7431448254773931339 ) ) ;
#3730=ORIENTED_EDGE ( 'NONE', *, *, #973, .T. ) ;
#3731=ORIENTED_EDGE ( 'NONE', *, *, #4086, .T. ) ;
#3732=CARTESIAN_POINT ( 'NONE',  ( 1.500000000000000444, 19.43515443678402832, 15.40502424595151787 ) ) ;
#3733=EDGE_LOOP ( 'NONE', ( #4737, #1879, #5475, #540 ) ) ;
#3734=AXIS2_PLACEMENT_3D ( 'NONE', #7248, #10934, #8244 ) ;
#3735=ORIENTED_EDGE ( 'NONE', *, *, #1989, .T. ) ;
#3736=CARTESIAN_POINT ( 'NONE',  ( 0.000000000000000000, 0.000000000000000000, 0.000000000000000000 ) ) ;
#3737=AXIS2_PLACEMENT_3D ( 'NONE', #9733, #3131, #7592 ) ;
#3738=CARTESIAN_POINT ( 'NONE',  ( 3.000000000000000888, -5.135568396240178579, 21.96011696265489377 ) ) ;
#3739=EDGE_CURVE ( 'NONE', #8566, #4413, #2270, .T. ) ;
#3740=ORIENTED_EDGE ( 'NONE', *, *, #6602, .T. ) ;
#3741=ADVANCED_FACE ( 'NONE', ( #7840 ), #125, .T. ) ;
#3742=CARTESIAN_POINT ( 'NONE',  ( 0.000000000000000000, 11.67026512804572924, -19.29833442572348190 ) ) ;
#3743=LINE ( 'NONE', #4903, #6301 ) ;
#3745=CIRCLE ( 'NONE', #4106, 9.599999999999997868 ) ;
#3746=DIRECTION ( 'NONE',  ( 0.000000000000000000, 0.000000000000000000, 1.000000000000000000 ) ) ;
#3747=CIRCLE ( 'NONE', #10189, 22.99899999999999523 ) ;
#3748=CIRCLE ( 'NONE', #5310, 9.599999999999996092 ) ;
#3749=DIRECTION ( 'NONE',  ( -1.000000000000000000, 0.000000000000000000, 0.000000000000000000 ) ) ;
#3750=VERTEX_POINT ( 'NONE', #309 ) ;
#3751=ORIENTED_EDGE ( 'NONE', *, *, #10417, .T. ) ;
#3752=FACE_OUTER_BOUND ( 'NONE', #7373, .T. ) ;
#3756=EDGE_CURVE ( 'NONE', #8232, #845, #1182, .T. ) ;
#3758=CARTESIAN_POINT ( 'NONE',  ( 3.000000000000000888, -22.47229024614976112, -1.901833551798492561 ) ) ;
#3759=ORIENTED_EDGE ( 'NONE', *, *, #4122, .F. ) ;
#3761=DIRECTION ( 'NONE',  ( 0.000000000000000000, 0.000000000000000000, 1.000000000000000000 ) ) ;
#3762=CYLINDRICAL_SURFACE ( 'NONE', #10837, 22.99899999999999878 ) ;
#3765=CYLINDRICAL_SURFACE ( 'NONE', #9443, 22.99899999999999878 ) ;
#3766=VECTOR ( 'NONE', #6787, 1000.000000000000000 ) ;
#3769=ORIENTED_EDGE ( 'NONE', *, *, #2550, .F. ) ;
#3770=ORIENTED_EDGE ( 'NONE', *, *, #7618, .T. ) ;
#3771=EDGE_CURVE ( 'NONE', #11767, #9480, #10764, .T. ) ;
#3772=ORIENTED_EDGE ( 'NONE', *, *, #7122, .T. ) ;
#3773=CARTESIAN_POINT ( 'NONE',  ( 0.000000000000000000, 15.42759117534385993, 16.45023496161670451 ) ) ;
#3775=CARTESIAN_POINT ( 'NONE',  ( 3.000000000000000888, 21.96011696265491153, -5.135568396240103084 ) ) ;
#3777=DIRECTION ( 'NONE',  ( 0.000000000000000000, 0.000000000000000000, 1.000000000000000000 ) ) ;
#3778=FACE_OUTER_BOUND ( 'NONE', #5365, .T. ) ;
#3780=AXIS2_PLACEMENT_3D ( 'NONE', #2969, #13, #1011 ) ;
#3781=CARTESIAN_POINT ( 'NONE',  ( 3.000000000000000888, 11.20082935824103387, -20.08719549084852929 ) ) ;
#3782=DIRECTION ( 'NONE',  ( -1.000000000000000000, -0.000000000000000000, 0.000000000000000000 ) ) ;
#3783=ORIENTED_EDGE ( 'NONE', *, *, #7362, .F. ) ;
#3784=EDGE_CURVE ( 'NONE', #1833, #11632, #5772, .T. ) ;
#3785=ORIENTED_EDGE ( 'NONE', *, *, #5734, .F. ) ;
#3786=CIRCLE ( 'NONE', #10617, 9.599999999999997868 ) ;
#3787=VERTEX_POINT ( 'NONE', #10597 ) ;
#3788=ORIENTED_EDGE ( 'NONE', *, *, #10467, .T. ) ;
#3789=DIRECTION ( 'NONE',  ( 0.000000000000000000, -0.7431448254773999063, 0.6691306063588520203 ) ) ;
#3790=CARTESIAN_POINT ( 'NONE',  ( 3.000000000000000888, -15.64281154287608722, 16.85990652506894705 ) ) ;
#3793=EDGE_CURVE ( 'NONE', #6911, #3296, #5699, .T. ) ;
#3794=CIRCLE ( 'NONE', #9458, 22.99899999999999878 ) ;
#3795=CARTESIAN_POINT ( 'NONE',  ( 3.000000000000000888, 0.000000000000000000, 0.000000000000000000 ) ) ;
#3797=CARTESIAN_POINT ( 'NONE',  ( 0.000000000000000000, -10.87771529938174808, 19.75591328264882662 ) ) ;
#3798=DIRECTION ( 'NONE',  ( 0.000000000000000000, 0.000000000000000000, 1.000000000000000000 ) ) ;
#3799=ORIENTED_EDGE ( 'NONE', *, *, #1950, .F. ) ;
#3800=ORIENTED_EDGE ( 'NONE', *, *, #1943, .T. ) ;
#3801=DIRECTION ( 'NONE',  ( 0.000000000000000000, 0.3090169943749416781, 0.9510565162951555296 ) ) ;
#3802=ORIENTED_EDGE ( 'NONE', *, *, #8349, .T. ) ;
#3803=CIRCLE ( 'NONE', #4382, 9.599999999999996092 ) ;
#3804=DIRECTION ( 'NONE',  ( -1.000000000000000000, 0.000000000000000000, 0.000000000000000000 ) ) ;
#3805=CARTESIAN_POINT ( 'NONE',  ( 3.000000000000000888, 0.000000000000000000, 0.000000000000000000 ) ) ;
#3806=ORIENTED_EDGE ( 'NONE', *, *, #8383, .T. ) ;
#3807=DIRECTION ( 'NONE',  ( -1.000000000000000000, -0.000000000000000000, 0.000000000000000000 ) ) ;
#3808=DIRECTION ( 'NONE',  ( -1.000000000000000000, 0.000000000000000000, 0.000000000000000000 ) ) ;
#3810=CIRCLE ( 'NONE', #7303, 9.599999999999996092 ) ;
#3813=ORIENTED_EDGE ( 'NONE', *, *, #837, .F. ) ;
#3814=ORIENTED_EDGE ( 'NONE', *, *, #242, .F. ) ;
#3815=DIRECTION ( 'NONE',  ( 1.000000000000000000, -0.000000000000000000, 0.000000000000000000 ) ) ;
#3816=EDGE_LOOP ( 'NONE', ( #306, #4188, #5544, #8713 ) ) ;
#3819=ORIENTED_EDGE ( 'NONE', *, *, #7152, .T. ) ;
#3820=DIRECTION ( 'NONE',  ( -1.000000000000000000, -0.000000000000000000, 0.000000000000000000 ) ) ;
#3821=DIRECTION ( 'NONE',  ( -1.000000000000000000, -0.000000000000000000, 0.000000000000000000 ) ) ;
#3824=CARTESIAN_POINT ( 'NONE',  ( 0.000000000000000000, 0.000000000000000000, 0.000000000000000000 ) ) ;
#3825=DIRECTION ( 'NONE',  ( 0.000000000000000000, 0.9781476007338049117, 0.2079116908177629230 ) ) ;
#3826=ADVANCED_FACE ( 'NONE', ( #6677 ), #1112, .T. ) ;
#3827=CYLINDRICAL_SURFACE ( 'NONE', #7446, 22.99899999999999878 ) ;
#3828=ORIENTED_EDGE ( 'NONE', *, *, #8724, .F. ) ;
#3829=AXIS2_PLACEMENT_3D ( 'NONE', #4426, #1673, #10979 ) ;
#3832=ORIENTED_EDGE ( 'NONE', *, *, #4942, .T. ) ;
#3835=DIRECTION ( 'NONE',  ( -1.000000000000000000, -0.000000000000000000, -0.000000000000000000 ) ) ;
#3836=AXIS2_PLACEMENT_3D ( 'NONE', #8018, #6069, #493 ) ;
#3839=DIRECTION ( 'NONE',  ( 0.000000000000000000, 0.000000000000000000, 1.000000000000000000 ) ) ;
#3840=ORIENTED_EDGE ( 'NONE', *, *, #10173, .T. ) ;
#3841=EDGE_LOOP ( 'NONE', ( #6346, #4911, #10708, #564 ) ) ;
#3843=ORIENTED_EDGE ( 'NONE', *, *, #11376, .F. ) ;
#3845=ADVANCED_FACE ( 'NONE', ( #5080 ), #7145, .T. ) ;
#3846=DIRECTION ( 'NONE',  ( -1.000000000000000000, 0.000000000000000000, 0.000000000000000000 ) ) ;
#3847=CARTESIAN_POINT ( 'NONE',  ( 3.000000000000000888, -22.90635393027944744, -2.062268319295799568 ) ) ;
#3848=DIRECTION ( 'NONE',  ( -1.000000000000000000, 0.000000000000000000, 0.000000000000000000 ) ) ;
#3849=EDGE_CURVE ( 'NONE', #4270, #10729, #2389, .T. ) ;
#3850=DIRECTION ( 'NONE',  ( 1.000000000000000000, 0.000000000000000000, 0.000000000000000000 ) ) ;
#3852=CARTESIAN_POINT ( 'NONE',  ( 8.000000000000000000, 0.000000000000000000, 19.99999999999999645 ) ) ;
#3853=ORIENTED_EDGE ( 'NONE', *, *, #9086, .F. ) ;
#3854=ORIENTED_EDGE ( 'NONE', *, *, #442, .F. ) ;
#3855=CYLINDRICAL_SURFACE ( 'NONE', #11566, 24.80000000000000071 ) ;
#3856=EDGE_CURVE ( 'NONE', #11027, #3033, #1006, .T. ) ;
#3857=EDGE_LOOP ( 'NONE', ( #10674, #1620, #1188, #2691 ) ) ;
#3858=DIRECTION ( 'NONE',  ( 0.000000000000000000, 0.000000000000000000, -1.000000000000000000 ) ) ;
#3859=DIRECTION ( 'NONE',  ( 0.000000000000000000, 0.000000000000000000, 1.000000000000000000 ) ) ;
#3860=ORIENTED_EDGE ( 'NONE', *, *, #7341, .T. ) ;
#3861=DIRECTION ( 'NONE',  ( -1.000000000000000000, 0.000000000000000000, 0.000000000000000000 ) ) ;
#3862=CARTESIAN_POINT ( 'NONE',  ( 0.000000000000000000, 13.28910708463128287, 20.93895013827586382 ) ) ;
#3864=CARTESIAN_POINT ( 'NONE',  ( 0.000000000000000000, 0.000000000000000000, 0.000000000000000000 ) ) ;
#3865=DIRECTION ( 'NONE',  ( 0.000000000000000000, 0.000000000000000000, 1.000000000000000000 ) ) ;
#3866=CIRCLE ( 'NONE', #1932, 24.80000000000000071 ) ;
#3867=ORIENTED_EDGE ( 'NONE', *, *, #11999, .F. ) ;
#3868=ORIENTED_EDGE ( 'NONE', *, *, #7012, .F. ) ;
#3869=DIRECTION ( 'NONE',  ( -1.000000000000000000, -0.000000000000000000, -0.000000000000000000 ) ) ;
#3875=CIRCLE ( 'NONE', #2899, 24.80000000000000071 ) ;
#3876=DIRECTION ( 'NONE',  ( -1.000000000000000000, -0.000000000000000000, -0.000000000000000000 ) ) ;
#3877=DIRECTION ( 'NONE',  ( 0.000000000000000000, -0.9781476007338077983, 0.2079116908177493783 ) ) ;
#3879=DIRECTION ( 'NONE',  ( -1.000000000000000000, -0.000000000000000000, 0.000000000000000000 ) ) ;
#3881=VERTEX_POINT ( 'NONE', #11631 ) ;
#3882=LINE ( 'NONE', #1639, #6262 ) ;
#3883=VECTOR ( 'NONE', #5060, 1000.000000000000000 ) ;
#3884=CIRCLE ( 'NONE', #158, 22.99899999999999523 ) ;
#3885=EDGE_LOOP ( 'NONE', ( #6021, #9486, #3375, #11038 ) ) ;
#3886=DIRECTION ( 'NONE',  ( 0.000000000000000000, 0.000000000000000000, 1.000000000000000000 ) ) ;
#3888=EDGE_CURVE ( 'NONE', #7388, #9445, #6855, .T. ) ;
#3889=DIRECTION ( 'NONE',  ( 0.000000000000000000, 0.000000000000000000, 1.000000000000000000 ) ) ;
#3890=EDGE_CURVE ( 'NONE', #3469, #2524, #1349, .T. ) ;
#3894=CARTESIAN_POINT ( 'NONE',  ( 1.499999999999999556, 23.88662356770115380, 6.668524164681708832 ) ) ;
#3895=VERTEX_POINT ( 'NONE', #8940 ) ;
#3896=VERTEX_POINT ( 'NONE', #6128 ) ;
#3897=CIRCLE ( 'NONE', #5459, 22.99899999999999878 ) ;
#3898=EDGE_CURVE ( 'NONE', #5856, #2132, #4282, .T. ) ;
#3899=DIRECTION ( 'NONE',  ( -1.000000000000000000, -0.000000000000000000, 0.000000000000000000 ) ) ;
#3900=AXIS2_PLACEMENT_3D ( 'NONE', #11672, #12081, #1459 ) ;
#3901=DIRECTION ( 'NONE',  ( -1.000000000000000000, 0.000000000000000000, -0.000000000000000000 ) ) ;
#3903=CARTESIAN_POINT ( 'NONE',  ( 3.000000000000000888, -13.72351598154883412, -20.65684170206505144 ) ) ;
#3904=FACE_OUTER_BOUND ( 'NONE', #182, .T. ) ;
#3905=CARTESIAN_POINT ( 'NONE',  ( 3.000000000000000888, 0.000000000000000000, 0.000000000000000000 ) ) ;
#3907=AXIS2_PLACEMENT_3D ( 'NONE', #4821, #3846, #3658 ) ;
#3908=EDGE_CURVE ( 'NONE', #7759, #9316, #10380, .T. ) ;
#3909=AXIS2_PLACEMENT_3D ( 'NONE', #774, #11970, #11059 ) ;
#3912=EDGE_LOOP ( 'NONE', ( #10953, #2566, #4128, #3645 ) ) ;
#3913=DIRECTION ( 'NONE',  ( -1.000000000000000000, -0.000000000000000000, -0.000000000000000000 ) ) ;
#3914=ORIENTED_EDGE ( 'NONE', *, *, #10856, .F. ) ;
#3915=ADVANCED_FACE ( 'NONE', ( #1595 ), #4172, .T. ) ;
#3918=DIRECTION ( 'NONE',  ( 0.000000000000000000, 0.9781476007338062439, -0.2079116908177564282 ) ) ;
#3919=ORIENTED_EDGE ( 'NONE', *, *, #4936, .F. ) ;
#3920=CIRCLE ( 'NONE', #4900, 24.80000000000000071 ) ;
#3921=DIRECTION ( 'NONE',  ( 0.000000000000000000, 0.000000000000000000, 1.000000000000000000 ) ) ;
#3926=CIRCLE ( 'NONE', #6267, 22.99899999999999523 ) ;
#3927=FACE_OUTER_BOUND ( 'NONE', #12030, .T. ) ;
#3928=ORIENTED_EDGE ( 'NONE', *, *, #8349, .F. ) ;
#3929=CIRCLE ( 'NONE', #1381, 9.599999999999994316 ) ;
#3930=ORIENTED_EDGE ( 'NONE', *, *, #7237, .T. ) ;
#3931=DIRECTION ( 'NONE',  ( 0.000000000000000000, 0.000000000000000000, 1.000000000000000000 ) ) ;
#3932=VERTEX_POINT ( 'NONE', #8997 ) ;
#3933=ADVANCED_FACE ( 'NONE', ( #9971 ), #5333, .T. ) ;
#3936=DIRECTION ( 'NONE',  ( -1.000000000000000000, 0.000000000000000000, 0.000000000000000000 ) ) ;
#3937=( NAMED_UNIT ( * ) PLANE_ANGLE_UNIT ( ) SI_UNIT ( $, .RADIAN. ) );
#3938=AXIS2_PLACEMENT_3D ( 'NONE', #4608, #3684, #929 ) ;
#3939=DIRECTION ( 'NONE',  ( 0.000000000000000000, 0.9945218953682729568, 0.1045284632676571068 ) ) ;
#3940=AXIS2_PLACEMENT_3D ( 'NONE', #3864, #7587, #11328 ) ;
#3941=ADVANCED_FACE ( 'NONE', ( #488 ), #4405, .T. ) ;
#3942=AXIS2_PLACEMENT_3D ( 'NONE', #6626, #4491, #6448 ) ;
#3943=FACE_OUTER_BOUND ( 'NONE', #4640, .T. ) ;
#3945=DIRECTION ( 'NONE',  ( 0.000000000000000000, 0.000000000000000000, 1.000000000000000000 ) ) ;
#3946=CARTESIAN_POINT ( 'NONE',  ( 3.000000000000000888, -18.80635025205160815, -13.23915371906974592 ) ) ;
#3947=CARTESIAN_POINT ( 'NONE',  ( 3.000000000000002665, 0.000000000000000000, 4.000000000000000000 ) ) ;
#3948=DIRECTION ( 'NONE',  ( 0.000000000000000000, 0.000000000000000000, -1.000000000000000000 ) ) ;
#3949=CLOSED_SHELL ( 'NONE', ( #7768, #1676, #489, #3382, #1308, #2501, #1540, #10342, #8766, #1651, #10012, #8717, #3970, #6099, #7160, #1897, #6384, #7665, #3626, #4163, #4562, #6517, #7725, #6022, #8619, #11565, #7488, #4433, #4746, #2245, #2800, #8026, #6056, #5576, #11092, #3915, #3027, #4591, #9234, #2068, #5911, #6943, #678, #3046, #9696, #9385, #6443, #5171, #11445, #7510, #6428, #9574, #3477, #4009, #8309, #9062, #11598, #3741, #405, #11187, #5636, #3081, #9049, #9324, #10405, #1732, #2106, #3591, #2243, #10313, #6365, #8978, #1874, #4907, #527, #11000, #9308, #2857, #6280, #5539, #11468, #247, #12115, #287, #10723, #3635, #3284, #1277, #285, #8222, #8339, #7617, #10161, #4295, #4573, #928, #4638, #7106, #1513, #8184, #7501, #7545, #7579, #11160, #7612, #11657, #1014, #4303, #9883, #11736, #9391, #11251, #4050, #11666, #1868, #10480, #1610, #445, #4457, #2200, #6725, #2697, #6083, #1750, #10099, #3826, #6387, #7324, #5806, #6244, #10542, #138, #11472, #6877, #11143, #8146, #397, #10194, #7177, #3278, #9206, #7925, #106, #1891, #5115, #9724, #69, #3317, #3398, #6537, #11858, #7473, #2916, #9671, #10500, #5652, #3368, #10634, #10944, #9851, #4380, #373, #780, #1363, #10017, #6840, #11083, #6361, #7623, #7654, #5424, #8300, #7524, #7382, #9014, #9581, #5123, #1384, #7088, #1136, #1192, #9464, #735, #3377, #2036, #3310, #4449, #907, #2392, #5910, #5985, #9968, #3941, #2093, #7996, #7476, #10929, #8089, #6965, #1949, #1461, #10731, #1339, #6596, #7776, #6220, #93, #10858, #8875, #5392, #24, #6793, #5021, #517, #4789, #3197, #3845, #4041, #9156, #9940, #5085, #1083, #6961, #3960, #1296, #9311, #2208, #10421, #2889, #6694, #986, #521, #8900, #3602, #1196, #1504, #1805, #4495, #10545, #11827, #3933, #2682, #8570, #5776, #4751, #11834, #8633, #8437, #8608, #11069, #5864, #2170, #2135, #7892, #5006 ) ) ;
#3950=ORIENTED_EDGE ( 'NONE', *, *, #8120, .T. ) ;
#3951=EDGE_LOOP ( 'NONE', ( #3588, #10076, #11009, #2877 ) ) ;
#3952=DIRECTION ( 'NONE',  ( -1.000000000000000000, 0.000000000000000000, -0.000000000000000000 ) ) ;
#3954=CYLINDRICAL_SURFACE ( 'NONE', #9553, 9.599999999999997868 ) ;
#3956=AXIS2_PLACEMENT_3D ( 'NONE', #3298, #6962, #5140 ) ;
#3958=LINE ( 'NONE', #5974, #1988 ) ;
#3959=VERTEX_POINT ( 'NONE', #9913 ) ;
#3960=ADVANCED_FACE ( 'NONE', ( #7899 ), #6968, .T. ) ;
#3961=ORIENTED_EDGE ( 'NONE', *, *, #7874, .F. ) ;
#3963=CARTESIAN_POINT ( 'NONE',  ( 3.000000000000000888, -9.039786367038983528, 21.14796121233193560 ) ) ;
#3964=VERTEX_POINT ( 'NONE', #8139 ) ;
#3965=EDGE_CURVE ( 'NONE', #2073, #6153, #7439, .T. ) ;
#3966=DIRECTION ( 'NONE',  ( 0.000000000000000000, 0.000000000000000000, 1.000000000000000000 ) ) ;
#3967=CARTESIAN_POINT ( 'NONE',  ( 3.000000000000000888, 7.432877647175206270, 21.76479567747243848 ) ) ;
#3968=CARTESIAN_POINT ( 'NONE',  ( 1.499999999999999556, 24.02068490260621303, -6.168200451485523317 ) ) ;
#3970=ADVANCED_FACE ( 'NONE', ( #2575 ), #6312, .T. ) ;
#3971=AXIS2_PLACEMENT_3D ( 'NONE', #4167, #3189, #10590 ) ;
#3972=EDGE_CURVE ( 'NONE', #3644, #4775, #10775, .T. ) ;
#3973=DIRECTION ( 'NONE',  ( 0.000000000000000000, -0.1045284632676401482, -0.9945218953682747332 ) ) ;
#3974=ORIENTED_EDGE ( 'NONE', *, *, #4108, .F. ) ;
#3975=VECTOR ( 'NONE', #7999, 1000.000000000000000 ) ;
#3977=AXIS2_PLACEMENT_3D ( 'NONE', #193, #7670, #441 ) ;
#3978=EDGE_CURVE ( 'NONE', #1804, #5933, #2634, .T. ) ;
#3980=ORIENTED_EDGE ( 'NONE', *, *, #2664, .T. ) ;
#3981=DIRECTION ( 'NONE',  ( -1.000000000000000000, 0.000000000000000000, 0.000000000000000000 ) ) ;
#3982=CARTESIAN_POINT ( 'NONE',  ( 1.500000000000000444, -24.02068490260608868, -6.168200451486004710 ) ) ;
#3983=AXIS2_PLACEMENT_3D ( 'NONE', #4588, #968, #8256 ) ;
#3986=DIRECTION ( 'NONE',  ( -1.000000000000000000, -0.000000000000000000, 0.000000000000000000 ) ) ;
#3987=DIRECTION ( 'NONE',  ( -1.000000000000000000, -0.000000000000000000, 0.000000000000000000 ) ) ;
#3989=DIRECTION ( 'NONE',  ( 0.000000000000000000, 0.000000000000000000, 1.000000000000000000 ) ) ;
#3990=ORIENTED_EDGE ( 'NONE', *, *, #9579, .F. ) ;
#3992=AXIS2_PLACEMENT_3D ( 'NONE', #3905, #11373, #6209 ) ;
#3993=ORIENTED_EDGE ( 'NONE', *, *, #5734, .T. ) ;
#3994=LINE ( 'NONE', #4105, #8614 ) ;
#3995=VERTEX_POINT ( 'NONE', #1656 ) ;
#3997=CYLINDRICAL_SURFACE ( 'NONE', #7537, 22.99899999999999878 ) ;
#3998=CIRCLE ( 'NONE', #4387, 22.99899999999999878 ) ;
#3999=CARTESIAN_POINT ( 'NONE',  ( 0.000000000000000000, 0.000000000000000000, 0.000000000000000000 ) ) ;
#4000=CARTESIAN_POINT ( 'NONE',  ( 0.000000000000000000, 0.000000000000000000, 0.000000000000000000 ) ) ;
#4002=EDGE_CURVE ( 'NONE', #10066, #3234, #3342, .T. ) ;
#4005=ORIENTED_EDGE ( 'NONE', *, *, #8252, .T. ) ;
#4006=CARTESIAN_POINT ( 'NONE',  ( 3.000000000000000888, -2.811977935937640005, -22.37663021667346896 ) ) ;
#4007=AXIS2_PLACEMENT_3D ( 'NONE', #4605, #9180, #5275 ) ;
#4008=ORIENTED_EDGE ( 'NONE', *, *, #8682, .F. ) ;
#4009=ADVANCED_FACE ( 'NONE', ( #4532 ), #8388, .T. ) ;
#4010=ORIENTED_EDGE ( 'NONE', *, *, #9125, .T. ) ;
#4011=CARTESIAN_POINT ( 'NONE',  ( 3.000000000000000888, -2.745295967525840375, -22.83456483164691875 ) ) ;
#4013=CARTESIAN_POINT ( 'NONE',  ( 3.000000000000000888, -22.37663021667341923, -2.811977935938010376 ) ) ;
#4017=LINE ( 'NONE', #7743, #5112 ) ;
#4018=VERTEX_POINT ( 'NONE', #10222 ) ;
#4019=ORIENTED_EDGE ( 'NONE', *, *, #4189, .F. ) ;
#4020=CARTESIAN_POINT ( 'NONE',  ( -10.00000000000000000, 0.000000000000000000, 0.000000000000000000 ) ) ;
#4021=CARTESIAN_POINT ( 'NONE',  ( 0.000000000000000000, 22.90635393027949007, -2.062268319295327057 ) ) ;
#4022=DIRECTION ( 'NONE',  ( -1.000000000000000000, -0.000000000000000000, -0.000000000000000000 ) ) ;
#4023=FACE_OUTER_BOUND ( 'NONE', #3432, .T. ) ;
#4025=AXIS2_PLACEMENT_3D ( 'NONE', #1914, #10297, #11337 ) ;
#4026=DIRECTION ( 'NONE',  ( -1.000000000000000000, 0.000000000000000000, 0.000000000000000000 ) ) ;
#4027=ORIENTED_EDGE ( 'NONE', *, *, #4857, .T. ) ;
#4028=ORIENTED_EDGE ( 'NONE', *, *, #4414, .F. ) ;
#4031=ORIENTED_EDGE ( 'NONE', *, *, #9751, .T. ) ;
#4032=LINE ( 'NONE', #7760, #10922 ) ;
#4033=CARTESIAN_POINT ( 'NONE',  ( 0.000000000000000000, -24.02068490260608868, -6.168200451486004710 ) ) ;
#4034=EDGE_CURVE ( 'NONE', #4410, #11830, #10089, .T. ) ;
#4035=DIRECTION ( 'NONE',  ( 0.000000000000000000, -0.9135454576426046414, 0.4067366430757919926 ) ) ;
#4036=AXIS2_PLACEMENT_3D ( 'NONE', #9070, #5515, #2581 ) ;
#4037=EDGE_LOOP ( 'NONE', ( #7398, #6407, #4578, #5492 ) ) ;
#4038=EDGE_CURVE ( 'NONE', #5213, #712, #4523, .T. ) ;
#4039=DIRECTION ( 'NONE',  ( 0.000000000000000000, -0.3090169943749349613, -0.9510565162951576390 ) ) ;
#4040=EDGE_CURVE ( 'NONE', #4720, #2635, #9197, .T. ) ;
#4041=ADVANCED_FACE ( 'NONE', ( #11076 ), #5572, .T. ) ;
#4042=CARTESIAN_POINT ( 'NONE',  ( 3.000000000000000888, 0.000000000000000000, 0.000000000000000000 ) ) ;
#4044=ORIENTED_EDGE ( 'NONE', *, *, #5951, .T. ) ;
#4045=CARTESIAN_POINT ( 'NONE',  ( -10.00000000000000000, 0.000000000000000000, 0.000000000000000000 ) ) ;
#4046=ORIENTED_EDGE ( 'NONE', *, *, #11629, .F. ) ;
#4047=DIRECTION ( 'NONE',  ( -1.000000000000000000, -0.000000000000000000, -0.000000000000000000 ) ) ;
#4050=ADVANCED_FACE ( 'NONE', ( #6544 ), #10277, .T. ) ;
#4052=ORIENTED_EDGE ( 'NONE', *, *, #5614, .T. ) ;
#4053=CARTESIAN_POINT ( 'NONE',  ( 0.000000000000000000, 0.000000000000000000, 0.000000000000000000 ) ) ;
#4054=DIRECTION ( 'NONE',  ( 0.000000000000000000, 0.000000000000000000, 1.000000000000000000 ) ) ;
#4056=CIRCLE ( 'NONE', #11899, 9.599999999999997868 ) ;
#4057=FACE_OUTER_BOUND ( 'NONE', #6546, .T. ) ;
#4059=FACE_BOUND ( 'NONE', #9392, .T. ) ;
#4062=ORIENTED_EDGE ( 'NONE', *, *, #1352, .T. ) ;
#4063=EDGE_LOOP ( 'NONE', ( #8283, #9171, #3423, #11613 ) ) ;
#4064=ORIENTED_EDGE ( 'NONE', *, *, #2759, .F. ) ;
#4065=EDGE_CURVE ( 'NONE', #5179, #994, #6424, .T. ) ;
#4066=CIRCLE ( 'NONE', #11300, 9.599999999999997868 ) ;
#4067=CYLINDRICAL_SURFACE ( 'NONE', #7921, 9.599999999999997868 ) ;
#4069=DIRECTION ( 'NONE',  ( -1.000000000000000000, 0.000000000000000000, -0.000000000000000000 ) ) ;
#4070=CARTESIAN_POINT ( 'NONE',  ( 3.000000000000000888, -18.51065745848368849, -12.88318129270198042 ) ) ;
#4074=EDGE_CURVE ( 'NONE', #6153, #5028, #11354, .T. ) ;
#4075=AXIS2_PLACEMENT_3D ( 'NONE', #10071, #10876, #3346 ) ;
#4076=DIRECTION ( 'NONE',  ( -1.000000000000000000, 0.000000000000000000, 0.000000000000000000 ) ) ;
#4077=VERTEX_POINT ( 'NONE', #979 ) ;
#4078=AXIS2_PLACEMENT_3D ( 'NONE', #4505, #2668, #10193 ) ;
#4080=FACE_OUTER_BOUND ( 'NONE', #7329, .T. ) ;
#4081=CARTESIAN_POINT ( 'NONE',  ( 3.000000000000000888, -21.14796121233190362, -9.039786367039052806 ) ) ;
#4082=AXIS2_PLACEMENT_3D ( 'NONE', #3593, #4572, #6400 ) ;
#4083=DIRECTION ( 'NONE',  ( -1.000000000000000000, 0.000000000000000000, -0.000000000000000000 ) ) ;
#4085=CIRCLE ( 'NONE', #5649, 9.599999999999996092 ) ;
#4086=EDGE_CURVE ( 'NONE', #4836, #679, #9013, .T. ) ;
#4088=CARTESIAN_POINT ( 'NONE',  ( 0.000000000000000000, 0.000000000000000000, 0.000000000000000000 ) ) ;
#4089=ORIENTED_EDGE ( 'NONE', *, *, #6921, .T. ) ;
#4090=VERTEX_POINT ( 'NONE', #4596 ) ;
#4093=ORIENTED_EDGE ( 'NONE', *, *, #2993, .T. ) ;
#4094=CYLINDRICAL_SURFACE ( 'NONE', #8385, 9.599999999999997868 ) ;
#4095=CYLINDRICAL_SURFACE ( 'NONE', #4285, 9.599999999999997868 ) ;
#4096=CARTESIAN_POINT ( 'NONE',  ( 1.500000000000000444, -23.24434456306330787, 8.645255683528924706 ) ) ;
#4097=ORIENTED_EDGE ( 'NONE', *, *, #2550, .T. ) ;
#4098=LINE ( 'NONE', #3067, #2213 ) ;
#4099=AXIS2_PLACEMENT_3D ( 'NONE', #2997, #6832, #7700 ) ;
#4100=DIRECTION ( 'NONE',  ( -1.000000000000000000, 0.000000000000000000, 0.000000000000000000 ) ) ;
#4102=EDGE_LOOP ( 'NONE', ( #648, #2307, #11940, #11990 ) ) ;
#4103=DIRECTION ( 'NONE',  ( -1.000000000000000000, -0.000000000000000000, -0.000000000000000000 ) ) ;
#4104=EDGE_LOOP ( 'NONE', ( #5234, #8691 ) ) ;
#4105=CARTESIAN_POINT ( 'NONE',  ( 3.000000000000000888, 7.432877647175206270, 21.76479567747243848 ) ) ;
#4106=AXIS2_PLACEMENT_3D ( 'NONE', #3524, #7236, #1559 ) ;
#4107=ORIENTED_EDGE ( 'NONE', *, *, #3112, .T. ) ;
#4108=EDGE_CURVE ( 'NONE', #8051, #1936, #1390, .T. ) ;
#4110=AXIS2_PLACEMENT_3D ( 'NONE', #9511, #2227, #2105 ) ;
#4111=CARTESIAN_POINT ( 'NONE',  ( 0.000000000000000000, 0.000000000000000000, 0.000000000000000000 ) ) ;
#4113=EDGE_CURVE ( 'NONE', #1752, #1491, #8235, .T. ) ;
#4114=DIRECTION ( 'NONE',  ( -1.000000000000000000, 0.000000000000000000, 0.000000000000000000 ) ) ;
#4115=DIRECTION ( 'NONE',  ( 0.000000000000000000, 0.4067366430758009299, -0.9135454576426005335 ) ) ;
#4117=AXIS2_PLACEMENT_3D ( 'NONE', #7221, #687, #4359 ) ;
#4118=DIRECTION ( 'NONE',  ( 0.000000000000000000, 0.000000000000000000, 1.000000000000000000 ) ) ;
#4119=CIRCLE ( 'NONE', #7230, 22.99899999999999523 ) ;
#4121=AXIS2_PLACEMENT_3D ( 'NONE', #2770, #10106, #68 ) ;
#4122=EDGE_CURVE ( 'NONE', #2635, #6096, #918, .T. ) ;
#4125=LINE ( 'NONE', #8600, #11917 ) ;
#4126=EDGE_CURVE ( 'NONE', #9529, #11898, #6087, .T. ) ;
#4127=ORIENTED_EDGE ( 'NONE', *, *, #11043, .F. ) ;
#4128=ORIENTED_EDGE ( 'NONE', *, *, #11678, .F. ) ;
#4129=ORIENTED_EDGE ( 'NONE', *, *, #8084, .T. ) ;
#4130=AXIS2_PLACEMENT_3D ( 'NONE', #1785, #2647, #6555 ) ;
#4131=VECTOR ( 'NONE', #276, 1000.000000000000000 ) ;
#4132=CARTESIAN_POINT ( 'NONE',  ( 3.000000000000000888, -24.02068490260617040, 6.168200451485680524 ) ) ;
#4133=AXIS2_PLACEMENT_3D ( 'NONE', #2448, #4227, #6188 ) ;
#4134=DIRECTION ( 'NONE',  ( 0.000000000000000000, 0.000000000000000000, 1.000000000000000000 ) ) ;
#4135=DIRECTION ( 'NONE',  ( -1.000000000000000000, 0.000000000000000000, 0.000000000000000000 ) ) ;
#4138=DIRECTION ( 'NONE',  ( -1.000000000000000000, -0.000000000000000000, -0.000000000000000000 ) ) ;
#4140=CIRCLE ( 'NONE', #6861, 24.80000000000000071 ) ;
#4141=ORIENTED_EDGE ( 'NONE', *, *, #3174, .T. ) ;
#4142=AXIS2_PLACEMENT_3D ( 'NONE', #11100, #4558, #4619 ) ;
#4143=VERTEX_POINT ( 'NONE', #7520 ) ;
#4144=ORIENTED_EDGE ( 'NONE', *, *, #392, .T. ) ;
#4145=FACE_OUTER_BOUND ( 'NONE', #11381, .T. ) ;
#4146=AXIS2_PLACEMENT_3D ( 'NONE', #2646, #805, #3507 ) ;
#4148=VECTOR ( 'NONE', #3987, 1000.000000000000000 ) ;
#4149=FACE_BOUND ( 'NONE', #10153, .T. ) ;
#4150=DIRECTION ( 'NONE',  ( 1.000000000000000000, -0.000000000000000000, 0.000000000000000000 ) ) ;
#4151=CIRCLE ( 'NONE', #4335, 9.599999999999997868 ) ;
#4152=DIRECTION ( 'NONE',  ( -1.000000000000000000, -0.000000000000000000, 0.000000000000000000 ) ) ;
#4154=EDGE_CURVE ( 'NONE', #10713, #5976, #11264, .T. ) ;
#4155=CARTESIAN_POINT ( 'NONE',  ( 3.000000000000000888, 0.000000000000000000, 0.000000000000000000 ) ) ;
#4156=ORIENTED_EDGE ( 'NONE', *, *, #368, .T. ) ;
#4157=ORIENTED_EDGE ( 'NONE', *, *, #2355, .T. ) ;
#4160=ORIENTED_EDGE ( 'NONE', *, *, #5987, .F. ) ;
#4161=CYLINDRICAL_SURFACE ( 'NONE', #2516, 9.599999999999997868 ) ;
#4162=LINE ( 'NONE', #5135, #2808 ) ;
#4163=ADVANCED_FACE ( 'NONE', ( #11495 ), #3855, .T. ) ;
#4164=CARTESIAN_POINT ( 'NONE',  ( 0.000000000000000000, 15.40502424595145037, 19.43515443678408516 ) ) ;
#4166=CIRCLE ( 'NONE', #3199, 22.99900000000000588 ) ;
#4167=CARTESIAN_POINT ( 'NONE',  ( 3.000000000000000888, 0.000000000000000000, 0.000000000000000000 ) ) ;
#4168=DIRECTION ( 'NONE',  ( 0.000000000000000000, 0.5000000000000011102, -0.8660254037844381525 ) ) ;
#4170=ORIENTED_EDGE ( 'NONE', *, *, #10915, .T. ) ;
#4171=CARTESIAN_POINT ( 'NONE',  ( 3.000000000000000888, -24.45282072769598258, -4.135161237383832677 ) ) ;
#4172=CYLINDRICAL_SURFACE ( 'NONE', #5889, 24.80000000000000071 ) ;
#4173=VERTEX_POINT ( 'NONE', #11438 ) ;
#4174=AXIS2_PLACEMENT_3D ( 'NONE', #3742, #7465, #174 ) ;
#4176=CIRCLE ( 'NONE', #10030, 22.99899999999999523 ) ;
#4177=DIRECTION ( 'NONE',  ( -1.000000000000000000, 0.000000000000000000, -0.000000000000000000 ) ) ;
#4178=ORIENTED_EDGE ( 'NONE', *, *, #10819, .F. ) ;
#4180=DIRECTION ( 'NONE',  ( 0.000000000000000000, 0.1045284632676536929, -0.9945218953682732899 ) ) ;
#4182=AXIS2_PLACEMENT_3D ( 'NONE', #5139, #1702, #3297 ) ;
#4185=FACE_OUTER_BOUND ( 'NONE', #5491, .T. ) ;
#4186=VERTEX_POINT ( 'NONE', #10514 ) ;
#4187=DIRECTION ( 'NONE',  ( -1.000000000000000000, -0.000000000000000000, 0.000000000000000000 ) ) ;
#4188=ORIENTED_EDGE ( 'NONE', *, *, #9521, .T. ) ;
#4189=EDGE_CURVE ( 'NONE', #5168, #4720, #6600, .T. ) ;
#4190=FACE_OUTER_BOUND ( 'NONE', #7330, .T. ) ;
#4191=DIRECTION ( 'NONE',  ( 0.000000000000000000, 0.000000000000000000, 1.000000000000000000 ) ) ;
#4192=EDGE_CURVE ( 'NONE', #5574, #5856, #7849, .T. ) ;
#4193=CARTESIAN_POINT ( 'NONE',  ( 0.000000000000000000, -1.556492618230806535, 24.75110766671651774 ) ) ;
#4197=EDGE_CURVE ( 'NONE', #6189, #11027, #8636, .T. ) ;
#4198=CIRCLE ( 'NONE', #12003, 22.99899999999999523 ) ;
#4199=CARTESIAN_POINT ( 'NONE',  ( 3.000000000000000888, 22.37663021667344054, 6.788022064062137595 ) ) ;
#4200=ORIENTED_EDGE ( 'NONE', *, *, #5714, .F. ) ;
#4201=ORIENTED_EDGE ( 'NONE', *, *, #2172, .F. ) ;
#4202=VERTEX_POINT ( 'NONE', #5694 ) ;
#4203=DIRECTION ( 'NONE',  ( 0.000000000000000000, -0.4067366430758072582, 0.9135454576425977580 ) ) ;
#4204=DIRECTION ( 'NONE',  ( -1.000000000000000000, 0.000000000000000000, 0.000000000000000000 ) ) ;
#4205=CARTESIAN_POINT ( 'NONE',  ( 0.000000000000000000, -20.78471918669866270, 8.753070780933086326 ) ) ;
#4207=CARTESIAN_POINT ( 'NONE',  ( 3.000000000000000888, -20.86861857134741172, 9.667200211209745930 ) ) ;
#4208=DIRECTION ( 'NONE',  ( -1.000000000000000000, -0.000000000000000000, 0.000000000000000000 ) ) ;
#4213=ORIENTED_EDGE ( 'NONE', *, *, #3677, .T. ) ;
#4214=DIRECTION ( 'NONE',  ( -1.000000000000000000, 0.000000000000000000, 0.000000000000000000 ) ) ;
#4216=EDGE_CURVE ( 'NONE', #9404, #1587, #8447, .T. ) ;
#4217=DIRECTION ( 'NONE',  ( 0.000000000000000000, 1.000000000000000000, 3.491481338843133355E-15 ) ) ;
#4218=ORIENTED_EDGE ( 'NONE', *, *, #1943, .F. ) ;
#4219=CARTESIAN_POINT ( 'NONE',  ( 0.000000000000000000, 20.08719549084880640, -11.20082935824054182 ) ) ;
#4220=AXIS2_PLACEMENT_3D ( 'NONE', #1533, #11996, #7093 ) ;
#4221=DIRECTION ( 'NONE',  ( 0.000000000000000000, 0.000000000000000000, 1.000000000000000000 ) ) ;
#4223=ORIENTED_EDGE ( 'NONE', *, *, #7185, .T. ) ;
#4224=EDGE_CURVE ( 'NONE', #5646, #6550, #3333, .T. ) ;
#4225=CARTESIAN_POINT ( 'NONE',  ( 1.499999999999999556, -11.48910920600668284, -21.97817939804051690 ) ) ;
#4226=VERTEX_POINT ( 'NONE', #5228 ) ;
#4227=DIRECTION ( 'NONE',  ( -1.000000000000000000, 0.000000000000000000, 0.000000000000000000 ) ) ;
#4228=ORIENTED_EDGE ( 'NONE', *, *, #2268, .F. ) ;
#4230=ORIENTED_EDGE ( 'NONE', *, *, #8102, .T. ) ;
#4232=DIRECTION ( 'NONE',  ( -1.000000000000000000, 0.000000000000000000, 0.000000000000000000 ) ) ;
#4233=ORIENTED_EDGE ( 'NONE', *, *, #4814, .T. ) ;
#4235=DIRECTION ( 'NONE',  ( -1.000000000000000000, -0.000000000000000000, 0.000000000000000000 ) ) ;
#4237=EDGE_CURVE ( 'NONE', #3881, #1864, #8961, .T. ) ;
#4238=CARTESIAN_POINT ( 'NONE',  ( 0.000000000000000000, -15.80756504416703656, 19.10918332567953115 ) ) ;
#4240=FACE_OUTER_BOUND ( 'NONE', #1280, .T. ) ;
#4241=DIRECTION ( 'NONE',  ( 0.000000000000000000, 0.000000000000000000, 1.000000000000000000 ) ) ;
#4242=VERTEX_POINT ( 'NONE', #7113 ) ;
#4243=CYLINDRICAL_SURFACE ( 'NONE', #2849, 9.599999999999997868 ) ;
#4244=ORIENTED_EDGE ( 'NONE', *, *, #2275, .T. ) ;
#4245=DIRECTION ( 'NONE',  ( 1.000000000000000000, 0.000000000000000000, 0.000000000000000000 ) ) ;
#4246=CYLINDRICAL_SURFACE ( 'NONE', #1780, 9.599999999999997868 ) ;
#4250=DIRECTION ( 'NONE',  ( -1.000000000000000000, 0.000000000000000000, -0.000000000000000000 ) ) ;
#4251=LINE ( 'NONE', #1441, #2940 ) ;
#4252=ORIENTED_EDGE ( 'NONE', *, *, #8693, .F. ) ;
#4253=AXIS2_PLACEMENT_3D ( 'NONE', #6071, #7907, #1357 ) ;
#4254=VERTEX_POINT ( 'NONE', #10865 ) ;
#4255=EDGE_CURVE ( 'NONE', #2419, #6911, #2476, .T. ) ;
#4256=VERTEX_POINT ( 'NONE', #10358 ) ;
#4258=EDGE_CURVE ( 'NONE', #4254, #10458, #614, .T. ) ;
#4262=LINE ( 'NONE', #4389, #3154 ) ;
#4263=EDGE_CURVE ( 'NONE', #8927, #4549, #9414, .T. ) ;
#4264=CARTESIAN_POINT ( 'NONE',  ( 0.000000000000000000, 0.000000000000000000, 0.000000000000000000 ) ) ;
#4265=EDGE_LOOP ( 'NONE', ( #7460, #6887, #3853, #10777 ) ) ;
#4266=EDGE_LOOP ( 'NONE', ( #11277, #534, #7070, #8913 ) ) ;
#4269=EDGE_CURVE ( 'NONE', #5364, #3541, #4534, .T. ) ;
#4270=VERTEX_POINT ( 'NONE', #9326 ) ;
#4272=AXIS2_PLACEMENT_3D ( 'NONE', #1134, #3835, #4869 ) ;
#4273=FACE_OUTER_BOUND ( 'NONE', #10488, .T. ) ;
#4274=DIRECTION ( 'NONE',  ( -1.000000000000000000, -0.000000000000000000, 0.000000000000000000 ) ) ;
#4275=FACE_OUTER_BOUND ( 'NONE', #398, .T. ) ;
#4276=ORIENTED_EDGE ( 'NONE', *, *, #3448, .T. ) ;
#4277=CARTESIAN_POINT ( 'NONE',  ( 0.000000000000000000, -6.668524164681463695, -23.88662356770121775 ) ) ;
#4278=DIRECTION ( 'NONE',  ( -1.000000000000000000, 0.000000000000000000, 0.000000000000000000 ) ) ;
#4280=CIRCLE ( 'NONE', #2527, 22.99900000000000233 ) ;
#4281=CARTESIAN_POINT ( 'NONE',  ( 0.000000000000000000, 0.000000000000000000, 0.000000000000000000 ) ) ;
#4282=LINE ( 'NONE', #10712, #2965 ) ;
#4283=ORIENTED_EDGE ( 'NONE', *, *, #9289, .T. ) ;
#4285=AXIS2_PLACEMENT_3D ( 'NONE', #7825, #8874, #6051 ) ;
#4286=AXIS2_PLACEMENT_3D ( 'NONE', #4704, #2930, #1037 ) ;
#4287=LINE ( 'NONE', #10782, #12033 ) ;
#4288=CARTESIAN_POINT ( 'NONE',  ( 1.500000000000000444, -1.039229259764318680, -24.77821629063823394 ) ) ;
#4289=CIRCLE ( 'NONE', #1366, 9.599999999999999645 ) ;
#4290=CARTESIAN_POINT ( 'NONE',  ( 3.000000000000000888, -6.532525787310825116, -21.58580335785683246 ) ) ;
#4291=CARTESIAN_POINT ( 'NONE',  ( 1.500000000000000444, 23.24434456306337182, -8.645255683528766610 ) ) ;
#4295=ADVANCED_FACE ( 'NONE', ( #821 ), #8290, .T. ) ;
#4296=DIRECTION ( 'NONE',  ( 0.000000000000000000, 0.000000000000000000, 1.000000000000000000 ) ) ;
#4297=ORIENTED_EDGE ( 'NONE', *, *, #10763, .T. ) ;
#4298=DIRECTION ( 'NONE',  ( 0.000000000000000000, 0.000000000000000000, 1.000000000000000000 ) ) ;
#4299=VERTEX_POINT ( 'NONE', #12016 ) ;
#4300=DIRECTION ( 'NONE',  ( -1.000000000000000000, -0.000000000000000000, 0.000000000000000000 ) ) ;
#4301=CARTESIAN_POINT ( 'NONE',  ( 3.000000000000000888, -19.74380051311548456, 11.79560690673865331 ) ) ;
#4302=ORIENTED_EDGE ( 'NONE', *, *, #11233, .F. ) ;
#4303=ADVANCED_FACE ( 'NONE', ( #12071 ), #2717, .T. ) ;
#4304=CIRCLE ( 'NONE', #11150, 18.49999999999999645 ) ;
#4305=FACE_OUTER_BOUND ( 'NONE', #7639, .T. ) ;
#4306=VECTOR ( 'NONE', #5027, 1000.000000000000000 ) ;
#4307=CYLINDRICAL_SURFACE ( 'NONE', #2030, 9.599999999999997868 ) ;
#4308=DIRECTION ( 'NONE',  ( 0.000000000000000000, -0.2079116908177468526, -0.9781476007338083534 ) ) ;
#4310=CYLINDRICAL_SURFACE ( 'NONE', #8067, 22.99899999999999878 ) ;
#4311=LINE ( 'NONE', #11780, #9384 ) ;
#4312=ORIENTED_EDGE ( 'NONE', *, *, #4792, .F. ) ;
#4313=AXIS2_PLACEMENT_3D ( 'NONE', #6851, #4908, #7719 ) ;
#4314=ORIENTED_EDGE ( 'NONE', *, *, #256, .T. ) ;
#4315=AXIS2_PLACEMENT_3D ( 'NONE', #11864, #4347, #10954 ) ;
#4316=ORIENTED_EDGE ( 'NONE', *, *, #6137, .T. ) ;
#4317=AXIS2_PLACEMENT_3D ( 'NONE', #4703, #9291, #2809 ) ;
#4321=DIRECTION ( 'NONE',  ( 0.000000000000000000, 0.000000000000000000, -1.000000000000000000 ) ) ;
#4322=AXIS2_PLACEMENT_3D ( 'NONE', #1055, #7003, #4784 ) ;
#4323=CIRCLE ( 'NONE', #1018, 9.599999999999996092 ) ;
#4325=DIRECTION ( 'NONE',  ( 0.000000000000000000, 0.000000000000000000, 1.000000000000000000 ) ) ;
#4326=LINE ( 'NONE', #3285, #5272 ) ;
#4327=ORIENTED_EDGE ( 'NONE', *, *, #7498, .F. ) ;
#4328=ORIENTED_EDGE ( 'NONE', *, *, #7237, .F. ) ;
#4329=AXIS2_PLACEMENT_3D ( 'NONE', #9809, #4357, #2400 ) ;
#4330=ORIENTED_EDGE ( 'NONE', *, *, #10248, .F. ) ;
#4333=DIRECTION ( 'NONE',  ( 0.000000000000000000, 0.000000000000000000, -1.000000000000000000 ) ) ;
#4334=DIRECTION ( 'NONE',  ( 0.000000000000000000, 0.7431448254773909134, 0.6691306063588620123 ) ) ;
#4335=AXIS2_PLACEMENT_3D ( 'NONE', #3193, #9912, #6127 ) ;
#4336=CYLINDRICAL_SURFACE ( 'NONE', #5412, 9.599999999999997868 ) ;
#4337=VERTEX_POINT ( 'NONE', #1704 ) ;
#4339=DIRECTION ( 'NONE',  ( -1.000000000000000000, 0.000000000000000000, 0.000000000000000000 ) ) ;
#4340=EDGE_CURVE ( 'NONE', #1307, #5268, #10776, .T. ) ;
#4341=LINE ( 'NONE', #5436, #1409 ) ;
#4343=CIRCLE ( 'NONE', #2190, 22.99900000000000233 ) ;
#4344=CIRCLE ( 'NONE', #11581, 24.80000000000000071 ) ;
#4345=EDGE_CURVE ( 'NONE', #6529, #7759, #4528, .T. ) ;
#4346=LINE ( 'NONE', #11630, #7828 ) ;
#4347=DIRECTION ( 'NONE',  ( -1.000000000000000000, 0.000000000000000000, 0.000000000000000000 ) ) ;
#4348=EDGE_LOOP ( 'NONE', ( #10105, #7581, #5410, #3251 ) ) ;
#4351=ORIENTED_EDGE ( 'NONE', *, *, #2420, .T. ) ;
#4352=DIRECTION ( 'NONE',  ( -1.000000000000000000, -0.000000000000000000, -0.000000000000000000 ) ) ;
#4354=FACE_OUTER_BOUND ( 'NONE', #9944, .T. ) ;
#4355=DIRECTION ( 'NONE',  ( 0.000000000000000000, 1.000000000000000000, 3.614007241618349165E-15 ) ) ;
#4357=DIRECTION ( 'NONE',  ( 1.000000000000000000, 0.000000000000000000, 0.000000000000000000 ) ) ;
#4359=DIRECTION ( 'NONE',  ( 0.000000000000000000, 0.4067366430758009299, -0.9135454576426005335 ) ) ;
#4361=ORIENTED_EDGE ( 'NONE', *, *, #669, .F. ) ;
#4362=FACE_OUTER_BOUND ( 'NONE', #7993, .T. ) ;
#4363=ORIENTED_EDGE ( 'NONE', *, *, #4977, .F. ) ;
#4364=AXIS2_PLACEMENT_3D ( 'NONE', #11564, #1335, #9607 ) ;
#4366=CARTESIAN_POINT ( 'NONE',  ( 0.000000000000000000, 20.41249101028211754, -9.589108953447965433 ) ) ;
#4368=ORIENTED_EDGE ( 'NONE', *, *, #3665, .F. ) ;
#4369=EDGE_CURVE ( 'NONE', #10077, #7105, #11071, .T. ) ;
#4370=AXIS2_PLACEMENT_3D ( 'NONE', #1650, #5384, #9111 ) ;
#4372=FACE_OUTER_BOUND ( 'NONE', #7214, .T. ) ;
#4373=DIRECTION ( 'NONE',  ( 1.000000000000000000, 0.000000000000000000, 0.000000000000000000 ) ) ;
#4378=LINE ( 'NONE', #4199, #3165 ) ;
#4379=ORIENTED_EDGE ( 'NONE', *, *, #851, .F. ) ;
#4380=ADVANCED_FACE ( 'NONE', ( #6818 ), #274, .T. ) ;
#4381=ORIENTED_EDGE ( 'NONE', *, *, #11063, .F. ) ;
#4382=AXIS2_PLACEMENT_3D ( 'NONE', #6155, #159, #2069 ) ;
#4385=DIRECTION ( 'NONE',  ( 0.000000000000000000, 0.000000000000000000, -1.000000000000000000 ) ) ;
#4386=CARTESIAN_POINT ( 'NONE',  ( 3.000000000000000888, 0.000000000000000000, 0.000000000000000000 ) ) ;
#4387=AXIS2_PLACEMENT_3D ( 'NONE', #8091, #8276, #2457 ) ;
#4389=CARTESIAN_POINT ( 'NONE',  ( 1.500000000000000444, 20.65684170206509762, -13.72351598154876129 ) ) ;
#4392=VERTEX_POINT ( 'NONE', #5973 ) ;
#4394=ORIENTED_EDGE ( 'NONE', *, *, #11265, .F. ) ;
#4395=CARTESIAN_POINT ( 'NONE',  ( 0.000000000000000000, -22.21333432029556221, -11.02759168516767474 ) ) ;
#4396=CYLINDRICAL_SURFACE ( 'NONE', #5858, 24.80000000000000071 ) ;
#4397=CYLINDRICAL_SURFACE ( 'NONE', #3681, 22.99899999999999878 ) ;
#4398=EDGE_LOOP ( 'NONE', ( #4363, #10890, #11810, #11623 ) ) ;
#4399=DIRECTION ( 'NONE',  ( -1.000000000000000000, 0.000000000000000000, 0.000000000000000000 ) ) ;
#4400=DIRECTION ( 'NONE',  ( 0.000000000000000000, 0.000000000000000000, 1.000000000000000000 ) ) ;
#4402=VECTOR ( 'NONE', #3458, 1000.000000000000000 ) ;
#4403=DIRECTION ( 'NONE',  ( -1.000000000000000000, -0.000000000000000000, -0.000000000000000000 ) ) ;
#4404=VERTEX_POINT ( 'NONE', #11259 ) ;
#4405=CYLINDRICAL_SURFACE ( 'NONE', #1774, 9.599999999999999645 ) ;
#4406=ORIENTED_EDGE ( 'NONE', *, *, #1797, .F. ) ;
#4407=ORIENTED_EDGE ( 'NONE', *, *, #4636, .T. ) ;
#4409=EDGE_CURVE ( 'NONE', #1752, #8897, #3747, .T. ) ;
#4410=VERTEX_POINT ( 'NONE', #5050 ) ;
#4411=LINE ( 'NONE', #8145, #5595 ) ;
#4412=AXIS2_PLACEMENT_3D ( 'NONE', #6373, #5269, #11081 ) ;
#4413=VERTEX_POINT ( 'NONE', #2873 ) ;
#4414=EDGE_CURVE ( 'NONE', #12055, #4735, #2366, .T. ) ;
#4415=DIRECTION ( 'NONE',  ( 1.000000000000000000, 0.000000000000000000, 0.000000000000000000 ) ) ;
#4416=CARTESIAN_POINT ( 'NONE',  ( 0.000000000000000000, -22.90635393027947941, 2.062268319295487817 ) ) ;
#4418=CARTESIAN_POINT ( 'NONE',  ( 0.000000000000000000, 0.000000000000000000, 0.000000000000000000 ) ) ;
#4419=EDGE_LOOP ( 'NONE', ( #6632, #1029, #51, #716 ) ) ;
#4420=AXIS2_PLACEMENT_3D ( 'NONE', #8829, #4177, #6972 ) ;
#4421=ORIENTED_EDGE ( 'NONE', *, *, #6981, .T. ) ;
#4422=CYLINDRICAL_SURFACE ( 'NONE', #1753, 9.599999999999997868 ) ;
#4423=ORIENTED_EDGE ( 'NONE', *, *, #6179, .T. ) ;
#4424=EDGE_CURVE ( 'NONE', #2739, #8206, #6289, .T. ) ;
#4426=CARTESIAN_POINT ( 'NONE',  ( 3.000000000000000888, 0.000000000000000000, 0.000000000000000000 ) ) ;
#4428=ORIENTED_EDGE ( 'NONE', *, *, #3022, .F. ) ;
#4429=DIRECTION ( 'NONE',  ( 0.000000000000000000, 0.000000000000000000, 1.000000000000000000 ) ) ;
#4431=DIRECTION ( 'NONE',  ( 0.000000000000000000, 0.000000000000000000, -1.000000000000000000 ) ) ;
#4433=ADVANCED_FACE ( 'NONE', ( #3218 ), #4995, .T. ) ;
#4435=DIRECTION ( 'NONE',  ( -1.000000000000000000, -0.000000000000000000, 0.000000000000000000 ) ) ;
#4436=DIRECTION ( 'NONE',  ( 0.000000000000000000, 0.000000000000000000, 1.000000000000000000 ) ) ;
#4437=EDGE_LOOP ( 'NONE', ( #6068, #11579, #9747, #1434 ) ) ;
#4441=DIRECTION ( 'NONE',  ( -1.000000000000000000, 0.000000000000000000, 0.000000000000000000 ) ) ;
#4442=DIRECTION ( 'NONE',  ( -1.000000000000000000, -0.000000000000000000, -0.000000000000000000 ) ) ;
#4443=EDGE_CURVE ( 'NONE', #5009, #4610, #7742, .T. ) ;
#4445=AXIS2_PLACEMENT_3D ( 'NONE', #2531, #754, #6388 ) ;
#4446=CARTESIAN_POINT ( 'NONE',  ( 0.000000000000000000, 22.99643626497956816, 0.3433949777332492848 ) ) ;
#4447=EDGE_LOOP ( 'NONE', ( #11237, #5545, #8370, #1894 ) ) ;
#4448=FACE_OUTER_BOUND ( 'NONE', #3654, .T. ) ;
#4449=ADVANCED_FACE ( 'NONE', ( #7923 ), #3271, .T. ) ;
#4451=SHAPE_DEFINITION_REPRESENTATION ( #325, #842 ) ;
#4452=ORIENTED_EDGE ( 'NONE', *, *, #8969, .F. ) ;
#4455=CIRCLE ( 'NONE', #538, 24.80000000000000071 ) ;
#4457=ADVANCED_FACE ( 'NONE', ( #6936 ), #6093, .T. ) ;
#4458=CARTESIAN_POINT ( 'NONE',  ( 3.000000000000000888, 0.000000000000000000, 0.000000000000000000 ) ) ;
#4459=CARTESIAN_POINT ( 'NONE',  ( 0.000000000000000000, -21.76479567747246691, 7.432877647175128999 ) ) ;
#4461=DIRECTION ( 'NONE',  ( 0.000000000000000000, 0.000000000000000000, -1.000000000000000000 ) ) ;
#4462=CIRCLE ( 'NONE', #555, 24.80000000000000071 ) ;
#4463=CARTESIAN_POINT ( 'NONE',  ( 0.000000000000000000, 10.87771529938162196, 19.75591328264889768 ) ) ;
#4464=VERTEX_POINT ( 'NONE', #10557 ) ;
#4465=ORIENTED_EDGE ( 'NONE', *, *, #510, .F. ) ;
#4467=VERTEX_POINT ( 'NONE', #6883 ) ;
#4468=CARTESIAN_POINT ( 'NONE',  ( 1.500000000000000444, -8.645255683528844770, -23.24434456306333985 ) ) ;
#4469=ORIENTED_EDGE ( 'NONE', *, *, #214, .T. ) ;
#4470=CIRCLE ( 'NONE', #5845, 9.599999999999996092 ) ;
#4471=DIRECTION ( 'NONE',  ( 0.000000000000000000, -0.7431448254773862505, -0.6691306063588672304 ) ) ;
#4473=CARTESIAN_POINT ( 'NONE',  ( 3.000000000000000888, 0.000000000000000000, 0.000000000000000000 ) ) ;
#4475=LINE ( 'NONE', #11032, #9038 ) ;
#4477=ORIENTED_EDGE ( 'NONE', *, *, #7960, .T. ) ;
#4478=EDGE_CURVE ( 'NONE', #5773, #6788, #4323, .T. ) ;
#4479=DIRECTION ( 'NONE',  ( -1.000000000000000000, 0.000000000000000000, 0.000000000000000000 ) ) ;
#4481=CIRCLE ( 'NONE', #8403, 24.80000000000000071 ) ;
#4482=CIRCLE ( 'NONE', #11903, 24.80000000000000071 ) ;
#4484=CIRCLE ( 'NONE', #2538, 22.99900000000000233 ) ;
#4485=EDGE_CURVE ( 'NONE', #11794, #9479, #10920, .T. ) ;
#4486=DIRECTION ( 'NONE',  ( -1.000000000000000000, -0.000000000000000000, 0.000000000000000000 ) ) ;
#4487=PRESENTATION_STYLE_ASSIGNMENT (( #7109 ) ) ;
#4488=ORIENTED_EDGE ( 'NONE', *, *, #11415, .F. ) ;
#4489=CARTESIAN_POINT ( 'NONE',  ( 3.000000000000000888, 0.000000000000000000, 0.000000000000000000 ) ) ;
#4491=DIRECTION ( 'NONE',  ( -1.000000000000000000, -0.000000000000000000, 0.000000000000000000 ) ) ;
#4492=EDGE_CURVE ( 'NONE', #3221, #5933, #1204, .T. ) ;
#4494=CARTESIAN_POINT ( 'NONE',  ( -10.00000000000000000, 0.000000000000000000, 0.000000000000000000 ) ) ;
#4495=ADVANCED_FACE ( 'NONE', ( #8166 ), #2417, .T. ) ;
#4496=AXIS2_PLACEMENT_3D ( 'NONE', #6019, #11413, #3948 ) ;
#4498=EDGE_LOOP ( 'NONE', ( #2013, #7796 ) ) ;
#4499=EDGE_CURVE ( 'NONE', #11993, #7265, #5114, .T. ) ;
#4500=ORIENTED_EDGE ( 'NONE', *, *, #4857, .F. ) ;
#4501=EDGE_LOOP ( 'NONE', ( #11997, #7492, #11772, #11202 ) ) ;
#4504=AXIS2_PLACEMENT_3D ( 'NONE', #8954, #630, #11825 ) ;
#4505=CARTESIAN_POINT ( 'NONE',  ( 0.000000000000000000, 12.88318129270179035, 18.51065745848382349 ) ) ;
#4506=DIRECTION ( 'NONE',  ( 0.000000000000000000, 0.9510565162951544194, -0.3090169943749449533 ) ) ;
#4508=AXIS2_PLACEMENT_3D ( 'NONE', #9570, #3145, #8775 ) ;
#4509=CARTESIAN_POINT ( 'NONE',  ( 3.000000000000000888, -17.31945870441157354, 15.13242714128113775 ) ) ;
#4510=CIRCLE ( 'NONE', #5094, 9.599999999999997868 ) ;
#4511=AXIS2_PLACEMENT_3D ( 'NONE', #4551, #1788, #8344 ) ;
#4512=CYLINDRICAL_SURFACE ( 'NONE', #9965, 24.80000000000000071 ) ;
#4514=ORIENTED_EDGE ( 'NONE', *, *, #6325, .T. ) ;
#4516=VERTEX_POINT ( 'NONE', #10000 ) ;
#4517=CARTESIAN_POINT ( 'NONE',  ( 0.000000000000000000, -20.93895013827572171, -13.28910708463150492 ) ) ;
#4519=AXIS2_PLACEMENT_3D ( 'NONE', #2088, #11395, #1967 ) ;
#4520=AXIS2_PLACEMENT_3D ( 'NONE', #11907, #6226, #2552 ) ;
#4521=PRODUCT_DEFINITION_CONTEXT ( 'detailed design', #9271, 'design' ) ;
#4523=CIRCLE ( 'NONE', #10179, 9.599999999999996092 ) ;
#4524=AXIS2_PLACEMENT_3D ( 'NONE', #11608, #10503, #4203 ) ;
#4525=EDGE_CURVE ( 'NONE', #1487, #8295, #8039, .T. ) ;
#4526=DIRECTION ( 'NONE',  ( 0.000000000000000000, 0.000000000000000000, -1.000000000000000000 ) ) ;
#4527=CARTESIAN_POINT ( 'NONE',  ( 3.000000000000000888, 17.06259499759964271, -14.74749645579993995 ) ) ;
#4528=LINE ( 'NONE', #10145, #11372 ) ;
#4530=CARTESIAN_POINT ( 'NONE',  ( 3.000000000000000888, -0.4575788569253416149, 22.54798042742717712 ) ) ;
#4531=ORIENTED_EDGE ( 'NONE', *, *, #7268, .F. ) ;
#4532=FACE_OUTER_BOUND ( 'NONE', #6394, .T. ) ;
#4534=CIRCLE ( 'NONE', #10982, 19.99999999999999645 ) ;
#4535=ORIENTED_EDGE ( 'NONE', *, *, #8438, .F. ) ;
#4536=VERTEX_POINT ( 'NONE', #5230 ) ;
#4539=ORIENTED_EDGE ( 'NONE', *, *, #4002, .T. ) ;
#4540=CYLINDRICAL_SURFACE ( 'NONE', #3054, 24.80000000000000071 ) ;
#4541=VERTEX_POINT ( 'NONE', #3583 ) ;
#4542=AXIS2_PLACEMENT_3D ( 'NONE', #11288, #7788, #1251 ) ;
#4543=AXIS2_PLACEMENT_3D ( 'NONE', #5945, #5882, #5075 ) ;
#4544=FACE_OUTER_BOUND ( 'NONE', #4266, .T. ) ;
#4545=DIRECTION ( 'NONE',  ( 0.000000000000000000, 0.9781476007338048007, 0.2079116908177630618 ) ) ;
#4547=DIRECTION ( 'NONE',  ( 0.000000000000000000, 0.000000000000000000, 1.000000000000000000 ) ) ;
#4548=DIRECTION ( 'NONE',  ( 0.000000000000000000, 0.000000000000000000, 1.000000000000000000 ) ) ;
#4549=VERTEX_POINT ( 'NONE', #6158 ) ;
#4550=VERTEX_POINT ( 'NONE', #7235 ) ;
#4551=CARTESIAN_POINT ( 'NONE',  ( 0.000000000000000000, 18.51065745848377730, 12.88318129270185430 ) ) ;
#4552=ORIENTED_EDGE ( 'NONE', *, *, #2115, .F. ) ;
#4555=DIRECTION ( 'NONE',  ( -1.000000000000000000, -0.000000000000000000, -0.000000000000000000 ) ) ;
#4556=DIRECTION ( 'NONE',  ( -1.000000000000000000, -0.000000000000000000, -0.000000000000000000 ) ) ;
#4557=CARTESIAN_POINT ( 'NONE',  ( 0.000000000000000000, 19.74380051311556628, -11.79560690673851475 ) ) ;
#4558=DIRECTION ( 'NONE',  ( -1.000000000000000000, -0.000000000000000000, -0.000000000000000000 ) ) ;
#4560=CARTESIAN_POINT ( 'NONE',  ( 1.500000000000000444, -20.65684170206481696, -13.72351598154918406 ) ) ;
#4562=ADVANCED_FACE ( 'NONE', ( #7977 ), #8909, .T. ) ;
#4563=CIRCLE ( 'NONE', #11584, 9.599999999999997868 ) ;
#4564=AXIS2_PLACEMENT_3D ( 'NONE', #4494, #6212, #5295 ) ;
#4565=ORIENTED_EDGE ( 'NONE', *, *, #2546, .T. ) ;
#4566=ORIENTED_EDGE ( 'NONE', *, *, #4966, .F. ) ;
#4567=AXIS2_PLACEMENT_3D ( 'NONE', #9909, #8991, #10026 ) ;
#4568=DIRECTION ( 'NONE',  ( 1.000000000000000000, -0.000000000000000000, -0.000000000000000000 ) ) ;
#4570=EDGE_CURVE ( 'NONE', #3056, #8295, #806, .T. ) ;
#4571=DIRECTION ( 'NONE',  ( 0.000000000000000000, 0.000000000000000000, 1.000000000000000000 ) ) ;
#4572=DIRECTION ( 'NONE',  ( -1.000000000000000000, -0.000000000000000000, -0.000000000000000000 ) ) ;
#4573=ADVANCED_FACE ( 'NONE', ( #2606 ), #4310, .T. ) ;
#4575=CYLINDRICAL_SURFACE ( 'NONE', #10609, 22.99899999999999878 ) ;
#4576=CIRCLE ( 'NONE', #5155, 9.599999999999997868 ) ;
#4577=DIRECTION ( 'NONE',  ( -1.000000000000000000, 0.000000000000000000, -0.000000000000000000 ) ) ;
#4578=ORIENTED_EDGE ( 'NONE', *, *, #2619, .F. ) ;
#4579=ORIENTED_EDGE ( 'NONE', *, *, #6948, .T. ) ;
#4581=VERTEX_POINT ( 'NONE', #700 ) ;
#4582=EDGE_CURVE ( 'NONE', #9364, #10168, #6341, .T. ) ;
#4583=CYLINDRICAL_SURFACE ( 'NONE', #9249, 9.599999999999997868 ) ;
#4585=CIRCLE ( 'NONE', #8697, 24.80000000000000071 ) ;
#4586=CARTESIAN_POINT ( 'NONE',  ( 0.000000000000000000, 19.29833442572375546, -11.67026512804527272 ) ) ;
#4587=FACE_OUTER_BOUND ( 'NONE', #4829, .T. ) ;
#4588=CARTESIAN_POINT ( 'NONE',  ( 3.000000000000000888, 0.000000000000000000, 0.000000000000000000 ) ) ;
#4591=ADVANCED_FACE ( 'NONE', ( #11713 ), #5416, .T. ) ;
#4593=VECTOR ( 'NONE', #6196, 1000.000000000000000 ) ;
#4594=VERTEX_POINT ( 'NONE', #11953 ) ;
#4595=EDGE_LOOP ( 'NONE', ( #7940, #4107, #1110, #7254 ) ) ;
#4596=CARTESIAN_POINT ( 'NONE',  ( 3.000000000000000888, -18.40266524480579236, -13.79477846460815194 ) ) ;
#4598=EDGE_CURVE ( 'NONE', #8541, #6939, #2798, .T. ) ;
#4600=ORIENTED_EDGE ( 'NONE', *, *, #11256, .F. ) ;
#4601=CARTESIAN_POINT ( 'NONE',  ( 0.000000000000000000, 0.000000000000000000, 0.000000000000000000 ) ) ;
#4602=ORIENTED_EDGE ( 'NONE', *, *, #8757, .F. ) ;
#4605=CARTESIAN_POINT ( 'NONE',  ( 3.000000000000000888, -10.87771529938148518, -19.75591328264897228 ) ) ;
#4607=CARTESIAN_POINT ( 'NONE',  ( 3.000000000000000888, 21.30300407174362576, -7.402892494506364329 ) ) ;
#4608=CARTESIAN_POINT ( 'NONE',  ( 0.000000000000000000, 0.000000000000000000, 0.000000000000000000 ) ) ;
#4609=VERTEX_POINT ( 'NONE', #1440 ) ;
#4610=VERTEX_POINT ( 'NONE', #11837 ) ;
#4611=DIRECTION ( 'NONE',  ( -1.000000000000000000, 0.000000000000000000, 0.000000000000000000 ) ) ;
#4612=ORIENTED_EDGE ( 'NONE', *, *, #7713, .F. ) ;
#4613=AXIS2_PLACEMENT_3D ( 'NONE', #882, #4555, #3577 ) ;
#4615=DIRECTION ( 'NONE',  ( -1.000000000000000000, -0.000000000000000000, -0.000000000000000000 ) ) ;
#4617=DIRECTION ( 'NONE',  ( 0.000000000000000000, 0.000000000000000000, 1.000000000000000000 ) ) ;
#4618=DIRECTION ( 'NONE',  ( 0.000000000000000000, 0.000000000000000000, 1.000000000000000000 ) ) ;
#4619=DIRECTION ( 'NONE',  ( 0.000000000000000000, 0.000000000000000000, 1.000000000000000000 ) ) ;
#4620=VECTOR ( 'NONE', #2037, 1000.000000000000000 ) ;
#4623=DIRECTION ( 'NONE',  ( 0.000000000000000000, 0.000000000000000000, 1.000000000000000000 ) ) ;
#4624=CARTESIAN_POINT ( 'NONE',  ( 3.000000000000000888, -22.37663021667341923, -2.811977935938010376 ) ) ;
#4625=ORIENTED_EDGE ( 'NONE', *, *, #3474, .F. ) ;
#4626=EDGE_LOOP ( 'NONE', ( #3325, #6065, #4828, #9068 ) ) ;
#4627=VECTOR ( 'NONE', #11501, 1000.000000000000000 ) ;
#4628=DIRECTION ( 'NONE',  ( -1.000000000000000000, 0.000000000000000000, -0.000000000000000000 ) ) ;
#4630=LINE ( 'NONE', #8173, #948 ) ;
#4634=LINE ( 'NONE', #7372, #9985 ) ;
#4635=ORIENTED_EDGE ( 'NONE', *, *, #134, .F. ) ;
#4636=EDGE_CURVE ( 'NONE', #662, #3166, #1431, .T. ) ;
#4637=ORIENTED_EDGE ( 'NONE', *, *, #1063, .T. ) ;
#4638=ADVANCED_FACE ( 'NONE', ( #6451 ), #5597, .T. ) ;
#4639=EDGE_CURVE ( 'NONE', #531, #11364, #449, .T. ) ;
#4640=EDGE_LOOP ( 'NONE', ( #791, #2239, #11508, #9729 ) ) ;
#4641=CARTESIAN_POINT ( 'NONE',  ( 3.000000000000000888, -22.37663021667346186, 2.811977935937707063 ) ) ;
#4642=CARTESIAN_POINT ( 'NONE',  ( 3.000000000000000888, -15.64281154287585807, -16.85990652506916021 ) ) ;
#4643=DIRECTION ( 'NONE',  ( -1.000000000000000000, -0.000000000000000000, 0.000000000000000000 ) ) ;
#4644=CARTESIAN_POINT ( 'NONE',  ( 3.000000000000000888, -13.62355943574031869, 17.97274125076070206 ) ) ;
#4645=DIRECTION ( 'NONE',  ( 0.000000000000000000, 0.000000000000000000, 1.000000000000000000 ) ) ;
#4648=EDGE_CURVE ( 'NONE', #4226, #5406, #7684, .T. ) ;
#4649=EDGE_CURVE ( 'NONE', #10066, #11319, #5470, .T. ) ;
#4650=CARTESIAN_POINT ( 'NONE',  ( 3.000000000000000888, 0.000000000000000000, 0.000000000000000000 ) ) ;
#4651=EDGE_LOOP ( 'NONE', ( #10157, #11839, #8085, #11614 ) ) ;
#4652=VECTOR ( 'NONE', #7678, 1000.000000000000000 ) ;
#4653=VERTEX_POINT ( 'NONE', #8292 ) ;
#4654=CARTESIAN_POINT ( 'NONE',  ( 3.000000000000000888, -21.97702544527753332, -6.779701584702958250 ) ) ;
#4655=ORIENTED_EDGE ( 'NONE', *, *, #11376, .T. ) ;
#4656=AXIS2_PLACEMENT_3D ( 'NONE', #554, #9920, #7216 ) ;
#4661=DIRECTION ( 'NONE',  ( 0.000000000000000000, 0.8090169943749445647, 0.5877852522924771339 ) ) ;
#4662=DIRECTION ( 'NONE',  ( -1.000000000000000000, 0.000000000000000000, 0.000000000000000000 ) ) ;
#4664=CIRCLE ( 'NONE', #2908, 9.599999999999997868 ) ;
#4665=AXIS2_PLACEMENT_3D ( 'NONE', #464, #2300, #11788 ) ;
#4666=CARTESIAN_POINT ( 'NONE',  ( 50.00005079999999680, 0.000000000000000000, 0.000000000000000000 ) ) ;
#4667=DIRECTION ( 'NONE',  ( 0.000000000000000000, 0.000000000000000000, 1.000000000000000000 ) ) ;
#4668=DIRECTION ( 'NONE',  ( -1.000000000000000000, -0.000000000000000000, -0.000000000000000000 ) ) ;
#4669=ORIENTED_EDGE ( 'NONE', *, *, #771, .T. ) ;
#4670=LINE ( 'NONE', #7472, #1971 ) ;
#4671=EDGE_LOOP ( 'NONE', ( #4725, #3238, #7526, #9497 ) ) ;
#4674=( NAMED_UNIT ( * ) SI_UNIT ( $, .STERADIAN. ) SOLID_ANGLE_UNIT ( ) );
#4675=DIRECTION ( 'NONE',  ( 1.000000000000000000, 0.000000000000000000, 0.000000000000000000 ) ) ;
#4676=CARTESIAN_POINT ( 'NONE',  ( 1.500000000000000444, 15.40502424595171149, -19.43515443678387200 ) ) ;
#4678=EDGE_CURVE ( 'NONE', #11323, #1657, #10361, .T. ) ;
#4681=CIRCLE ( 'NONE', #9562, 22.99899999999999878 ) ;
#4682=CARTESIAN_POINT ( 'NONE',  ( 3.000000000000000888, 1.901833551798570721, -22.47229024614975401 ) ) ;
#4683=ORIENTED_EDGE ( 'NONE', *, *, #12031, .T. ) ;
#4684=VERTEX_POINT ( 'NONE', #8415 ) ;
#4685=EDGE_CURVE ( 'NONE', #8902, #5976, #6505, .T. ) ;
#4686=VERTEX_POINT ( 'NONE', #2719 ) ;
#4687=DIRECTION ( 'NONE',  ( -1.000000000000000000, 0.000000000000000000, -0.000000000000000000 ) ) ;
#4689=AXIS2_PLACEMENT_3D ( 'NONE', #8621, #221, #3966 ) ;
#4690=CARTESIAN_POINT ( 'NONE',  ( 3.000000000000000888, -6.779701584702581663, -21.97702544527764701 ) ) ;
#4691=LINE ( 'NONE', #12085, #8964 ) ;
#4692=AXIS2_PLACEMENT_3D ( 'NONE', #10822, #1274, #5245 ) ;
#4694=DIRECTION ( 'NONE',  ( 0.000000000000000000, -0.1045284632676607012, 0.9945218953682726237 ) ) ;
#4695=DIRECTION ( 'NONE',  ( -1.000000000000000000, -0.000000000000000000, 0.000000000000000000 ) ) ;
#4696=ORIENTED_EDGE ( 'NONE', *, *, #2962, .T. ) ;
#4697=AXIS2_PLACEMENT_3D ( 'NONE', #6276, #2353, #5231 ) ;
#4699=EDGE_LOOP ( 'NONE', ( #4790, #6783, #10293, #8981 ) ) ;
#4700=AXIS2_PLACEMENT_3D ( 'NONE', #7308, #7249, #4805 ) ;
#4701=ORIENTED_EDGE ( 'NONE', *, *, #1157, .F. ) ;
#4702=CARTESIAN_POINT ( 'NONE',  ( 0.000000000000000000, 22.37663021667344054, -2.811977935937859385 ) ) ;
#4703=CARTESIAN_POINT ( 'NONE',  ( 0.000000000000000000, 0.000000000000000000, 0.000000000000000000 ) ) ;
#4704=CARTESIAN_POINT ( 'NONE',  ( 8.000000000000000000, 0.000000000000000000, 0.000000000000000000 ) ) ;
#4705=DIRECTION ( 'NONE',  ( 0.000000000000000000, 0.000000000000000000, 1.000000000000000000 ) ) ;
#4706=VECTOR ( 'NONE', #8599, 1000.000000000000000 ) ;
#4707=CARTESIAN_POINT ( 'NONE',  ( 0.000000000000000000, 14.74749645580034496, -17.06259499759930165 ) ) ;
#4708=AXIS2_PLACEMENT_3D ( 'NONE', #4281, #10709, #3373 ) ;
#4709=VECTOR ( 'NONE', #5281, 1000.000000000000000 ) ;
#4711=CARTESIAN_POINT ( 'NONE',  ( 3.000000000000000888, -22.54798042742717357, -0.4575788569254196636 ) ) ;
#4714=EDGE_CURVE ( 'NONE', #3630, #3600, #6322, .T. ) ;
#4715=ORIENTED_EDGE ( 'NONE', *, *, #5957, .T. ) ;
#4717=DIRECTION ( 'NONE',  ( 1.000000000000000000, -0.000000000000000000, -0.000000000000000000 ) ) ;
#4718=ORIENTED_EDGE ( 'NONE', *, *, #11621, .F. ) ;
#4719=AXIS2_PLACEMENT_3D ( 'NONE', #5487, #5610, #3653 ) ;
#4720=VERTEX_POINT ( 'NONE', #1921 ) ;
#4721=CARTESIAN_POINT ( 'NONE',  ( 3.000000000000000888, 0.000000000000000000, 0.000000000000000000 ) ) ;
#4722=AXIS2_PLACEMENT_3D ( 'NONE', #674, #613, #3246 ) ;
#4723=EDGE_CURVE ( 'NONE', #4242, #3460, #8861, .T. ) ;
#4724=CARTESIAN_POINT ( 'NONE',  ( 0.000000000000000000, -13.79477846460783574, -18.40266524480602683 ) ) ;
#4725=ORIENTED_EDGE ( 'NONE', *, *, #1223, .F. ) ;
#4726=EDGE_CURVE ( 'NONE', #4299, #7424, #3586, .T. ) ;
#4727=CYLINDRICAL_SURFACE ( 'NONE', #5735, 22.99899999999999878 ) ;
#4728=EDGE_CURVE ( 'NONE', #9467, #9480, #9050, .T. ) ;
#4729=CYLINDRICAL_SURFACE ( 'NONE', #1025, 24.80000000000000071 ) ;
#4731=CIRCLE ( 'NONE', #5288, 22.99899999999999523 ) ;
#4733=AXIS2_PLACEMENT_3D ( 'NONE', #4711, #9417, #2352 ) ;
#4734=DIRECTION ( 'NONE',  ( -1.000000000000000000, 0.000000000000000000, -0.000000000000000000 ) ) ;
#4735=VERTEX_POINT ( 'NONE', #9450 ) ;
#4736=DIRECTION ( 'NONE',  ( -1.000000000000000000, 0.000000000000000000, -0.000000000000000000 ) ) ;
#4737=ORIENTED_EDGE ( 'NONE', *, *, #6912, .F. ) ;
#4739=DIRECTION ( 'NONE',  ( 0.000000000000000000, 0.8660254037844363761, 0.5000000000000039968 ) ) ;
#4741=CARTESIAN_POINT ( 'NONE',  ( -10.00000000000000000, 0.000000000000000000, 0.000000000000000000 ) ) ;
#4744=DIRECTION ( 'NONE',  ( 0.000000000000000000, 0.000000000000000000, 1.000000000000000000 ) ) ;
#4745=AXIS2_PLACEMENT_3D ( 'NONE', #9370, #2947, #176 ) ;
#4746=ADVANCED_FACE ( 'NONE', ( #10116 ), #80, .T. ) ;
#4747=ORIENTED_EDGE ( 'NONE', *, *, #11747, .F. ) ;
#4748=DIRECTION ( 'NONE',  ( 0.000000000000000000, 0.000000000000000000, -1.000000000000000000 ) ) ;
#4749=CIRCLE ( 'NONE', #436, 9.599999999999996092 ) ;
#4750=EDGE_LOOP ( 'NONE', ( #6630, #4747, #2137, #5742 ) ) ;
#4751=ADVANCED_FACE ( 'NONE', ( #12074 ), #3765, .T. ) ;
#4754=CIRCLE ( 'NONE', #6691, 4.000000000000000000 ) ;
#4755=DIRECTION ( 'NONE',  ( 0.000000000000000000, 0.000000000000000000, 1.000000000000000000 ) ) ;
#4757=AXIS2_PLACEMENT_3D ( 'NONE', #9937, #9031, #11048 ) ;
#4758=EDGE_CURVE ( 'NONE', #8246, #11319, #10612, .T. ) ;
#4759=CARTESIAN_POINT ( 'NONE',  ( 0.000000000000000000, -20.86861857134728027, -9.667200211210033700 ) ) ;
#4760=ORIENTED_EDGE ( 'NONE', *, *, #11236, .F. ) ;
#4761=ORIENTED_EDGE ( 'NONE', *, *, #10243, .T. ) ;
#4762=AXIS2_PLACEMENT_3D ( 'NONE', #10162, #3678, #4661 ) ;
#4763=ORIENTED_EDGE ( 'NONE', *, *, #90, .T. ) ;
#4764=ORIENTED_EDGE ( 'NONE', *, *, #7122, .F. ) ;
#4765=DIRECTION ( 'NONE',  ( -1.000000000000000000, 0.000000000000000000, 0.000000000000000000 ) ) ;
#4766=CARTESIAN_POINT ( 'NONE',  ( 3.000000000000000888, 0.000000000000000000, 0.000000000000000000 ) ) ;
#4767=DIRECTION ( 'NONE',  ( 0.000000000000000000, 0.1045284632676471287, 0.9945218953682740670 ) ) ;
#4768=FACE_OUTER_BOUND ( 'NONE', #6833, .T. ) ;
#4772=ORIENTED_EDGE ( 'NONE', *, *, #6882, .F. ) ;
#4773=ORIENTED_EDGE ( 'NONE', *, *, #11442, .F. ) ;
#4775=VERTEX_POINT ( 'NONE', #11521 ) ;
#4776=AXIS2_PLACEMENT_3D ( 'NONE', #3638, #7354, #7417 ) ;
#4777=CARTESIAN_POINT ( 'NONE',  ( 0.000000000000000000, 0.000000000000000000, 0.000000000000000000 ) ) ;
#4780=DIRECTION ( 'NONE',  ( 0.000000000000000000, 0.000000000000000000, 1.000000000000000000 ) ) ;
#4781=DIRECTION ( 'NONE',  ( -1.000000000000000000, 0.000000000000000000, 0.000000000000000000 ) ) ;
#4784=DIRECTION ( 'NONE',  ( 0.000000000000000000, 0.000000000000000000, 1.000000000000000000 ) ) ;
#4785=CYLINDRICAL_SURFACE ( 'NONE', #5511, 24.80000000000000071 ) ;
#4786=ORIENTED_EDGE ( 'NONE', *, *, #8969, .T. ) ;
#4787=EDGE_LOOP ( 'NONE', ( #6187, #6468, #50, #11235 ) ) ;
#4788=CARTESIAN_POINT ( 'NONE',  ( 3.000000000000000888, -2.062268319295719632, 22.90635393027945454 ) ) ;
#4789=ADVANCED_FACE ( 'NONE', ( #6865 ), #6925, .T. ) ;
#4790=ORIENTED_EDGE ( 'NONE', *, *, #6608, .T. ) ;
#4791=EDGE_CURVE ( 'NONE', #1383, #4254, #8596, .T. ) ;
#4792=EDGE_CURVE ( 'NONE', #6834, #7011, #3206, .T. ) ;
#4794=DIRECTION ( 'NONE',  ( 0.000000000000000000, 0.000000000000000000, -1.000000000000000000 ) ) ;
#4796=LINE ( 'NONE', #8592, #8762 ) ;
#4797=FACE_OUTER_BOUND ( 'NONE', #83, .T. ) ;
#4799=CARTESIAN_POINT ( 'NONE',  ( 3.000000000000000888, 21.58580335785685378, -6.532525787310757615 ) ) ;
#4800=DIRECTION ( 'NONE',  ( 0.000000000000000000, -0.8660254037844328234, -0.5000000000000099920 ) ) ;
#4802=EDGE_CURVE ( 'NONE', #10265, #8647, #3384, .T. ) ;
#4803=DIRECTION ( 'NONE',  ( -1.000000000000000000, 0.000000000000000000, 0.000000000000000000 ) ) ;
#4804=ORIENTED_EDGE ( 'NONE', *, *, #748, .T. ) ;
#4805=DIRECTION ( 'NONE',  ( 0.000000000000000000, 0.000000000000000000, 1.000000000000000000 ) ) ;
#4806=ORIENTED_EDGE ( 'NONE', *, *, #6144, .T. ) ;
#4807=DIRECTION ( 'NONE',  ( -1.000000000000000000, 0.000000000000000000, 0.000000000000000000 ) ) ;
#4810=EDGE_CURVE ( 'NONE', #7795, #2848, #1303, .T. ) ;
#4811=AXIS2_PLACEMENT_3D ( 'NONE', #7777, #3135, #5150 ) ;
#4814=EDGE_CURVE ( 'NONE', #518, #1487, #5143, .T. ) ;
#4815=CARTESIAN_POINT ( 'NONE',  ( 3.000000000000000888, 9.589108953448178596, -20.41249101028201451 ) ) ;
#4816=ORIENTED_EDGE ( 'NONE', *, *, #4113, .F. ) ;
#4817=VERTEX_POINT ( 'NONE', #3946 ) ;
#4818=CIRCLE ( 'NONE', #3064, 9.599999999999996092 ) ;
#4819=EDGE_LOOP ( 'NONE', ( #5524, #5943, #8943, #6929 ) ) ;
#4820=FACE_OUTER_BOUND ( 'NONE', #10088, .T. ) ;
#4821=CARTESIAN_POINT ( 'NONE',  ( 0.000000000000000000, -18.51065745848368849, -12.88318129270198042 ) ) ;
#4822=DIRECTION ( 'NONE',  ( -1.000000000000000000, 0.000000000000000000, 0.000000000000000000 ) ) ;
#4823=CARTESIAN_POINT ( 'NONE',  ( 0.000000000000000000, 22.99643626497956816, -0.3433949777332470088 ) ) ;
#4824=CARTESIAN_POINT ( 'NONE',  ( 0.000000000000000000, -22.56530478845645860, -4.445336973061090546 ) ) ;
#4827=CARTESIAN_POINT ( 'NONE',  ( 3.000000000000000888, -6.668524164681794097, 23.88662356770113249 ) ) ;
#4828=ORIENTED_EDGE ( 'NONE', *, *, #11375, .F. ) ;
#4829=EDGE_LOOP ( 'NONE', ( #7035, #6097, #11492, #9437 ) ) ;
#4831=CARTESIAN_POINT ( 'NONE',  ( 3.000000000000000888, 18.40266524480588473, 13.79477846460802226 ) ) ;
#4832=EDGE_LOOP ( 'NONE', ( #2207, #6692, #695, #3047 ) ) ;
#4833=DIRECTION ( 'NONE',  ( 0.000000000000000000, 0.2079116908177598144, -0.9781476007338055778 ) ) ;
#4834=EDGE_CURVE ( 'NONE', #9694, #518, #10817, .T. ) ;
#4835=CARTESIAN_POINT ( 'NONE',  ( -10.00000000000000000, 0.000000000000000000, 0.000000000000000000 ) ) ;
#4836=VERTEX_POINT ( 'NONE', #1956 ) ;
#4838=DIRECTION ( 'NONE',  ( -1.000000000000000000, 0.000000000000000000, 0.000000000000000000 ) ) ;
#4841=DIRECTION ( 'NONE',  ( -1.000000000000000000, -0.000000000000000000, -0.000000000000000000 ) ) ;
#4842=AXIS2_PLACEMENT_3D ( 'NONE', #6684, #5592, #5836 ) ;
#4843=ORIENTED_EDGE ( 'NONE', *, *, #6870, .F. ) ;
#4844=ORIENTED_EDGE ( 'NONE', *, *, #4038, .F. ) ;
#4845=CARTESIAN_POINT ( 'NONE',  ( 3.000000000000000888, -21.96011696265495061, 5.135568396239952982 ) ) ;
#4846=VERTEX_POINT ( 'NONE', #1160 ) ;
#4848=CARTESIAN_POINT ( 'NONE',  ( 3.000000000000000888, 0.000000000000000000, 0.000000000000000000 ) ) ;
#4851=AXIS2_PLACEMENT_3D ( 'NONE', #6359, #5255, #8989 ) ;
#4853=CARTESIAN_POINT ( 'NONE',  ( 3.000000000000000888, 0.000000000000000000, 0.000000000000000000 ) ) ;
#4855=DIRECTION ( 'NONE',  ( -1.000000000000000000, 0.000000000000000000, 0.000000000000000000 ) ) ;
#4857=EDGE_CURVE ( 'NONE', #4775, #2104, #1629, .T. ) ;
#4858=DIRECTION ( 'NONE',  ( -1.000000000000000000, 0.000000000000000000, 0.000000000000000000 ) ) ;
#4859=ORIENTED_EDGE ( 'NONE', *, *, #9298, .T. ) ;
#4860=FACE_OUTER_BOUND ( 'NONE', #123, .T. ) ;
#4861=AXIS2_PLACEMENT_3D ( 'NONE', #5372, #6349, #5305 ) ;
#4862=EDGE_CURVE ( 'NONE', #8329, #10038, #3192, .T. ) ;
#4863=VECTOR ( 'NONE', #6459, 1000.000000000000000 ) ;
#4864=ORIENTED_EDGE ( 'NONE', *, *, #2091, .T. ) ;
#4865=EDGE_LOOP ( 'NONE', ( #10925, #7471, #7238, #5052 ) ) ;
#4868=EDGE_CURVE ( 'NONE', #1881, #8050, #9484, .T. ) ;
#4869=DIRECTION ( 'NONE',  ( 0.000000000000000000, 0.000000000000000000, 1.000000000000000000 ) ) ;
#4872=AXIS2_PLACEMENT_3D ( 'NONE', #8974, #584, #4321 ) ;
#4874=EDGE_CURVE ( 'NONE', #8071, #9845, #9837, .T. ) ;
#4875=DIRECTION ( 'NONE',  ( -1.000000000000000000, 0.000000000000000000, 0.000000000000000000 ) ) ;
#4876=ORIENTED_EDGE ( 'NONE', *, *, #4726, .T. ) ;
#4879=FACE_OUTER_BOUND ( 'NONE', #58, .T. ) ;
#4880=AXIS2_PLACEMENT_3D ( 'NONE', #2726, #1518, #11108 ) ;
#4883=ORIENTED_EDGE ( 'NONE', *, *, #5385, .F. ) ;
#4884=CARTESIAN_POINT ( 'NONE',  ( 0.000000000000000000, 17.06259499759964271, -14.74749645579993995 ) ) ;
#4885=CARTESIAN_POINT ( 'NONE',  ( 0.000000000000000000, 22.21333432029578603, -11.02759168516723065 ) ) ;
#4886=DIRECTION ( 'NONE',  ( -1.000000000000000000, 0.000000000000000000, 0.000000000000000000 ) ) ;
#4888=AXIS2_PLACEMENT_3D ( 'NONE', #11469, #1186, #3149 ) ;
#4889=FACE_OUTER_BOUND ( 'NONE', #524, .T. ) ;
#4890=EDGE_LOOP ( 'NONE', ( #9703, #2879, #4351, #860 ) ) ;
#4891=ORIENTED_EDGE ( 'NONE', *, *, #134, .T. ) ;
#4893=ORIENTED_EDGE ( 'NONE', *, *, #973, .F. ) ;
#4894=CARTESIAN_POINT ( 'NONE',  ( 3.000000000000000888, 21.97817939804055598, -11.48910920600660646 ) ) ;
#4895=LINE ( 'NONE', #3982, #11600 ) ;
#4897=EDGE_CURVE ( 'NONE', #9669, #8183, #113, .T. ) ;
#4898=DIRECTION ( 'NONE',  ( 0.000000000000000000, 0.000000000000000000, 1.000000000000000000 ) ) ;
#4899=ORIENTED_EDGE ( 'NONE', *, *, #9824, .F. ) ;
#4900=AXIS2_PLACEMENT_3D ( 'NONE', #8648, #3869, #8763 ) ;
#4901=DIRECTION ( 'NONE',  ( 0.000000000000000000, 0.000000000000000000, -1.000000000000000000 ) ) ;
#4903=CARTESIAN_POINT ( 'NONE',  ( 1.500000000000000444, -13.28910708463142498, 20.93895013827577145 ) ) ;
#4906=ORIENTED_EDGE ( 'NONE', *, *, #3849, .T. ) ;
#4907=ADVANCED_FACE ( 'NONE', ( #8390 ), #982, .T. ) ;
#4908=DIRECTION ( 'NONE',  ( -1.000000000000000000, 0.000000000000000000, 0.000000000000000000 ) ) ;
#4909=CARTESIAN_POINT ( 'NONE',  ( 3.000000000000000888, -22.83456483164687256, -2.745295967526231173 ) ) ;
#4910=AXIS2_PLACEMENT_3D ( 'NONE', #8011, #7206, #8824 ) ;
#4911=ORIENTED_EDGE ( 'NONE', *, *, #2466, .F. ) ;
#4912=VECTOR ( 'NONE', #5802, 1000.000000000000000 ) ;
#4914=DIRECTION ( 'NONE',  ( -1.000000000000000000, 0.000000000000000000, -0.000000000000000000 ) ) ;
#4915=AXIS2_PLACEMENT_3D ( 'NONE', #2874, #5690, #9419 ) ;
#4916=CYLINDRICAL_SURFACE ( 'NONE', #3671, 9.599999999999997868 ) ;
#4917=AXIS2_PLACEMENT_3D ( 'NONE', #3535, #6107, #9043 ) ;
#4918=AXIS2_PLACEMENT_3D ( 'NONE', #11602, #7804, #11539 ) ;
#4921=CYLINDRICAL_SURFACE ( 'NONE', #10395, 9.599999999999997868 ) ;
#4923=CARTESIAN_POINT ( 'NONE',  ( 8.000000000000000000, 0.000000000000000000, 0.000000000000000000 ) ) ;
#4924=EDGE_LOOP ( 'NONE', ( #5696, #5611, #2722, #4488 ) ) ;
#4925=DIRECTION ( 'NONE',  ( -1.000000000000000000, -0.000000000000000000, -0.000000000000000000 ) ) ;
#4927=ORIENTED_EDGE ( 'NONE', *, *, #10436, .T. ) ;
#4928=AXIS2_PLACEMENT_3D ( 'NONE', #6366, #7385, #915 ) ;
#4929=VERTEX_POINT ( 'NONE', #10280 ) ;
#4930=CARTESIAN_POINT ( 'NONE',  ( 0.000000000000000000, 9.128825345753341480, -23.05871956130112821 ) ) ;
#4933=DIRECTION ( 'NONE',  ( -1.000000000000000000, 0.000000000000000000, 0.000000000000000000 ) ) ;
#4936=EDGE_CURVE ( 'NONE', #5220, #219, #653, .T. ) ;
#4938=DIRECTION ( 'NONE',  ( -1.000000000000000000, -0.000000000000000000, 0.000000000000000000 ) ) ;
#4939=AXIS2_PLACEMENT_3D ( 'NONE', #4999, #3168, #7107 ) ;
#4940=DIRECTION ( 'NONE',  ( -1.000000000000000000, 0.000000000000000000, 0.000000000000000000 ) ) ;
#4941=ORIENTED_EDGE ( 'NONE', *, *, #7024, .F. ) ;
#4942=EDGE_CURVE ( 'NONE', #9445, #10348, #1102, .T. ) ;
#4943=EDGE_CURVE ( 'NONE', #6369, #8696, #4176, .T. ) ;
#4944=VERTEX_POINT ( 'NONE', #8573 ) ;
#4945=DIRECTION ( 'NONE',  ( 0.000000000000000000, 0.000000000000000000, 1.000000000000000000 ) ) ;
#4946=AXIS2_PLACEMENT_3D ( 'NONE', #4527, #6362, #5258 ) ;
#4947=DIRECTION ( 'NONE',  ( -1.000000000000000000, -0.000000000000000000, 0.000000000000000000 ) ) ;
#4948=EDGE_CURVE ( 'NONE', #5148, #6070, #7641, .T. ) ;
#4949=LINE ( 'NONE', #102, #8980 ) ;
#4950=DIRECTION ( 'NONE',  ( 1.000000000000000000, 0.000000000000000000, 0.000000000000000000 ) ) ;
#4952=AXIS2_PLACEMENT_3D ( 'NONE', #5214, #7275, #8022 ) ;
#4953=EDGE_CURVE ( 'NONE', #8886, #10656, #2079, .T. ) ;
#4954=DIRECTION ( 'NONE',  ( -1.000000000000000000, 0.000000000000000000, 0.000000000000000000 ) ) ;
#4956=AXIS2_PLACEMENT_3D ( 'NONE', #4641, #11120, #7376 ) ;
#4957=ORIENTED_EDGE ( 'NONE', *, *, #3605, .F. ) ;
#4959=ORIENTED_EDGE ( 'NONE', *, *, #3414, .F. ) ;
#4960=LINE ( 'NONE', #8699, #5460 ) ;
#4961=CARTESIAN_POINT ( 'NONE',  ( 3.000000000000000888, 22.37663021667344054, -2.811977935937859385 ) ) ;
#4962=AXIS2_PLACEMENT_3D ( 'NONE', #10390, #10328, #8508 ) ;
#4964=ORIENTED_EDGE ( 'NONE', *, *, #11879, .F. ) ;
#4965=CARTESIAN_POINT ( 'NONE',  ( 3.000000000000000888, 0.000000000000000000, 0.000000000000000000 ) ) ;
#4966=EDGE_CURVE ( 'NONE', #5082, #11972, #4895, .T. ) ;
#4967=CARTESIAN_POINT ( 'NONE',  ( 0.000000000000000000, 11.48910920600714647, -21.97817939804027176 ) ) ;
#4969=ORIENTED_EDGE ( 'NONE', *, *, #5549, .T. ) ;
#4970=EDGE_CURVE ( 'NONE', #4404, #2419, #2024, .T. ) ;
#4971=CARTESIAN_POINT ( 'NONE',  ( 3.000000000000000888, 19.29833442572375546, -11.67026512804527272 ) ) ;
#4972=AXIS2_PLACEMENT_3D ( 'NONE', #2602, #884, #12070 ) ;
#4973=DIRECTION ( 'NONE',  ( 0.000000000000000000, 0.000000000000000000, 1.000000000000000000 ) ) ;
#4974=ORIENTED_EDGE ( 'NONE', *, *, #10184, .F. ) ;
#4976=LINE ( 'NONE', #8944, #6183 ) ;
#4977=EDGE_CURVE ( 'NONE', #9866, #7518, #6781, .T. ) ;
#4979=AXIS2_PLACEMENT_3D ( 'NONE', #1480, #9868, #5215 ) ;
#4981=CARTESIAN_POINT ( 'NONE',  ( 3.000000000000000888, 0.000000000000000000, 0.000000000000000000 ) ) ;
#4983=DIRECTION ( 'NONE',  ( 0.000000000000000000, 0.000000000000000000, 1.000000000000000000 ) ) ;
#4985=CYLINDRICAL_SURFACE ( 'NONE', #9194, 9.599999999999997868 ) ;
#4986=CARTESIAN_POINT ( 'NONE',  ( 3.000000000000000888, -3.623565124517270419, 24.53384959170456270 ) ) ;
#4987=VERTEX_POINT ( 'NONE', #3293 ) ;
#4988=ORIENTED_EDGE ( 'NONE', *, *, #9648, .T. ) ;
#4989=CARTESIAN_POINT ( 'NONE',  ( 3.000000000000000888, 24.02068490260620948, -6.168200451485520652 ) ) ;
#4992=DIRECTION ( 'NONE',  ( -1.000000000000000000, 0.000000000000000000, 0.000000000000000000 ) ) ;
#4995=CYLINDRICAL_SURFACE ( 'NONE', #9995, 24.80000000000000071 ) ;
#4996=CARTESIAN_POINT ( 'NONE',  ( 3.000000000000000888, 15.42759117534407309, -16.45023496161649845 ) ) ;
#4997=ORIENTED_EDGE ( 'NONE', *, *, #3289, .T. ) ;
#4998=ORIENTED_EDGE ( 'NONE', *, *, #11961, .T. ) ;
#4999=CARTESIAN_POINT ( 'NONE',  ( 3.000000000000000888, 0.000000000000000000, 0.000000000000000000 ) ) ;
#5001=CYLINDRICAL_SURFACE ( 'NONE', #7450, 24.80000000000000071 ) ;
#5003=LINE ( 'NONE', #6037, #8374 ) ;
#5005=AXIS2_PLACEMENT_3D ( 'NONE', #7033, #6918, #10661 ) ;
#5006=ADVANCED_FACE ( 'NONE', ( #6903 ), #7014, .F. ) ;
#5008=CARTESIAN_POINT ( 'NONE',  ( 3.000000000000000888, -9.589108953447752270, -20.41249101028221702 ) ) ;
#5009=VERTEX_POINT ( 'NONE', #9778 ) ;
#5013=ORIENTED_EDGE ( 'NONE', *, *, #11305, .F. ) ;
#5014=DIRECTION ( 'NONE',  ( 0.000000000000000000, 0.000000000000000000, 1.000000000000000000 ) ) ;
#5015=DIRECTION ( 'NONE',  ( -1.000000000000000000, -0.000000000000000000, -0.000000000000000000 ) ) ;
#5016=CARTESIAN_POINT ( 'NONE',  ( 3.000000000000000888, -1.901833551798098876, -22.47229024614979309 ) ) ;
#5017=AXIS2_PLACEMENT_3D ( 'NONE', #3738, #2020, #984 ) ;
#5018=ORIENTED_EDGE ( 'NONE', *, *, #3022, .T. ) ;
#5019=EDGE_CURVE ( 'NONE', #9635, #5247, #9720, .T. ) ;
#5020=CARTESIAN_POINT ( 'NONE',  ( 3.000000000000000888, -4.240409074143949297, -22.15038895030653521 ) ) ;
#5021=ADVANCED_FACE ( 'NONE', ( #1402 ), #10647, .T. ) ;
#5022=CARTESIAN_POINT ( 'NONE',  ( 3.000000000000000888, -23.24434456306319419, -8.645255683529244450 ) ) ;
#5025=ORIENTED_EDGE ( 'NONE', *, *, #9191, .F. ) ;
#5026=CYLINDRICAL_SURFACE ( 'NONE', #5101, 24.80000000000000071 ) ;
#5027=DIRECTION ( 'NONE',  ( -1.000000000000000000, 0.000000000000000000, 0.000000000000000000 ) ) ;
#5028=VERTEX_POINT ( 'NONE', #9850 ) ;
#5030=DIRECTION ( 'NONE',  ( 0.000000000000000000, 0.000000000000000000, -1.000000000000000000 ) ) ;
#5032=EDGE_CURVE ( 'NONE', #8778, #9064, #4162, .T. ) ;
#5033=CARTESIAN_POINT ( 'NONE',  ( 0.000000000000000000, 0.000000000000000000, 0.000000000000000000 ) ) ;
#5034=DIRECTION ( 'NONE',  ( -1.000000000000000000, 0.000000000000000000, 0.000000000000000000 ) ) ;
#5037=( NAMED_UNIT ( * ) SI_UNIT ( $, .STERADIAN. ) SOLID_ANGLE_UNIT ( ) );
#5039=LINE ( 'NONE', #2047, #3534 ) ;
#5040=ORIENTED_EDGE ( 'NONE', *, *, #1149, .F. ) ;
#5041=CARTESIAN_POINT ( 'NONE',  ( 3.000000000000000888, 22.54798042742718067, -0.4575788569252652871 ) ) ;
#5042=VERTEX_POINT ( 'NONE', #6117 ) ;
#5045=CARTESIAN_POINT ( 'NONE',  ( 0.000000000000000000, 22.42251312757879234, 5.117118920208566735 ) ) ;
#5046=EDGE_CURVE ( 'NONE', #3562, #11246, #9061, .T. ) ;
#5050=CARTESIAN_POINT ( 'NONE',  ( 3.000000000000000888, -21.97702544527753332, -6.779701584702958250 ) ) ;
#5051=DIRECTION ( 'NONE',  ( -1.000000000000000000, 0.000000000000000000, 0.000000000000000000 ) ) ;
#5052=ORIENTED_EDGE ( 'NONE', *, *, #2759, .T. ) ;
#5054=ORIENTED_EDGE ( 'NONE', *, *, #1964, .T. ) ;
#5055=VERTEX_POINT ( 'NONE', #8700 ) ;
#5056=FACE_OUTER_BOUND ( 'NONE', #9131, .T. ) ;
#5057=DIRECTION ( 'NONE',  ( -1.000000000000000000, -0.000000000000000000, -0.000000000000000000 ) ) ;
#5058=CIRCLE ( 'NONE', #10138, 24.80000000000000071 ) ;
#5060=DIRECTION ( 'NONE',  ( 1.000000000000000000, -0.000000000000000000, -0.000000000000000000 ) ) ;
#5063=CARTESIAN_POINT ( 'NONE',  ( 3.000000000000000888, -17.06259499759935139, -14.74749645580028101 ) ) ;
#5065=VERTEX_POINT ( 'NONE', #3121 ) ;
#5068=VERTEX_POINT ( 'NONE', #1460 ) ;
#5069=CARTESIAN_POINT ( 'NONE',  ( 3.000000000000000888, 9.667200211209818761, 20.86861857134737264 ) ) ;
#5070=DIRECTION ( 'NONE',  ( -1.000000000000000000, 0.000000000000000000, 0.000000000000000000 ) ) ;
#5071=CARTESIAN_POINT ( 'NONE',  ( 0.000000000000000000, -6.779701584702887196, 21.97702544527755464 ) ) ;
#5072=VERTEX_POINT ( 'NONE', #296 ) ;
#5073=DIRECTION ( 'NONE',  ( -1.000000000000000000, -0.000000000000000000, 0.000000000000000000 ) ) ;
#5074=CIRCLE ( 'NONE', #4692, 9.599999999999997868 ) ;
#5075=DIRECTION ( 'NONE',  ( 0.000000000000000000, 0.9781476007338062439, -0.2079116908177564282 ) ) ;
#5078=DIRECTION ( 'NONE',  ( -1.000000000000000000, 0.000000000000000000, 0.000000000000000000 ) ) ;
#5079=EDGE_LOOP ( 'NONE', ( #1332, #5947, #10444, #618 ) ) ;
#5080=FACE_OUTER_BOUND ( 'NONE', #421, .T. ) ;
#5081=AXIS2_PLACEMENT_3D ( 'NONE', #11540, #4076, #10626 ) ;
#5082=VERTEX_POINT ( 'NONE', #4033 ) ;
#5083=EDGE_CURVE ( 'NONE', #10038, #8212, #1634, .T. ) ;
#5085=ADVANCED_FACE ( 'NONE', ( #11620 ), #8001, .T. ) ;
#5086=CIRCLE ( 'NONE', #11721, 9.599999999999997868 ) ;
#5087=ORIENTED_EDGE ( 'NONE', *, *, #11480, .F. ) ;
#5088=DIRECTION ( 'NONE',  ( 0.000000000000000000, 0.000000000000000000, 1.000000000000000000 ) ) ;
#5089=CARTESIAN_POINT ( 'NONE',  ( 0.000000000000000000, -21.14796121233203152, 9.039786367038763260 ) ) ;
#5090=DIRECTION ( 'NONE',  ( -1.000000000000000000, -0.000000000000000000, -0.000000000000000000 ) ) ;
#5092=AXIS2_PLACEMENT_3D ( 'NONE', #7855, #5962, #1125 ) ;
#5093=DIRECTION ( 'NONE',  ( 0.000000000000000000, 0.000000000000000000, 1.000000000000000000 ) ) ;
#5094=AXIS2_PLACEMENT_3D ( 'NONE', #725, #3493, #4461 ) ;
#5096=CIRCLE ( 'NONE', #4511, 9.599999999999997868 ) ;
#5097=DIRECTION ( 'NONE',  ( 0.000000000000000000, 0.000000000000000000, 1.000000000000000000 ) ) ;
#5099=CARTESIAN_POINT ( 'NONE',  ( 0.000000000000000000, -18.51065745848386968, 12.88318129270172818 ) ) ;
#5100=ORIENTED_EDGE ( 'NONE', *, *, #10281, .T. ) ;
#5101=AXIS2_PLACEMENT_3D ( 'NONE', #4045, #4103, #1234 ) ;
#5102=AXIS2_PLACEMENT_3D ( 'NONE', #2369, #11725, #9953 ) ;
#5103=DIRECTION ( 'NONE',  ( 0.000000000000000000, 0.000000000000000000, 1.000000000000000000 ) ) ;
#5104=CYLINDRICAL_SURFACE ( 'NONE', #140, 9.599999999999997868 ) ;
#5105=CARTESIAN_POINT ( 'NONE',  ( 0.000000000000000000, 1.556492618230966851, -24.75110766671650708 ) ) ;
#5107=EDGE_CURVE ( 'NONE', #4686, #5213, #4481, .T. ) ;
#5109=CARTESIAN_POINT ( 'NONE',  ( 3.000000000000000888, 21.76479567747241717, 7.432877647175279101 ) ) ;
#5110=CIRCLE ( 'NONE', #6671, 9.599999999999996092 ) ;
#5111=DIRECTION ( 'NONE',  ( 1.000000000000000000, 0.000000000000000000, 0.000000000000000000 ) ) ;
#5112=VECTOR ( 'NONE', #7614, 1000.000000000000000 ) ;
#5114=CIRCLE ( 'NONE', #9806, 9.599999999999999645 ) ;
#5115=ADVANCED_FACE ( 'NONE', ( #354 ), #4095, .T. ) ;
#5116=ORIENTED_EDGE ( 'NONE', *, *, #7174, .F. ) ;
#5117=ORIENTED_EDGE ( 'NONE', *, *, #3849, .F. ) ;
#5119=CARTESIAN_POINT ( 'NONE',  ( 0.000000000000000000, 11.20082935824075321, 20.08719549084868561 ) ) ;
#5120=AXIS2_PLACEMENT_3D ( 'NONE', #4799, #11520, #10426 ) ;
#5122=CARTESIAN_POINT ( 'NONE',  ( 0.000000000000000000, -19.75591328264893676, 10.87771529938155268 ) ) ;
#5123=ADVANCED_FACE ( 'NONE', ( #3486 ), #5496, .T. ) ;
#5124=APPLICATION_CONTEXT ( 'automotive_design' ) ;
#5126=CARTESIAN_POINT ( 'NONE',  ( 1.499999999999999556, 24.53384959170457336, 3.623565124517186931 ) ) ;
#5128=DIRECTION ( 'NONE',  ( 0.000000000000000000, 0.000000000000000000, 1.000000000000000000 ) ) ;
#5130=ORIENTED_EDGE ( 'NONE', *, *, #819, .T. ) ;
#5133=ORIENTED_EDGE ( 'NONE', *, *, #1938, .F. ) ;
#5134=CARTESIAN_POINT ( 'NONE',  ( 0.000000000000000000, -19.75591328264879110, -10.87771529938182091 ) ) ;
#5135=CARTESIAN_POINT ( 'NONE',  ( 1.499999999999999556, 11.02759168516744737, 22.21333432029567589 ) ) ;
#5136=CARTESIAN_POINT ( 'NONE',  ( 3.000000000000000888, -12.88318129270165890, -18.51065745848391586 ) ) ;
#5137=EDGE_LOOP ( 'NONE', ( #7914, #2375, #9691, #4141 ) ) ;
#5138=CIRCLE ( 'NONE', #8670, 9.599999999999999645 ) ;
#5139=CARTESIAN_POINT ( 'NONE',  ( 3.000000000000000888, 0.000000000000000000, 0.000000000000000000 ) ) ;
#5140=DIRECTION ( 'NONE',  ( 0.000000000000000000, 0.000000000000000000, 1.000000000000000000 ) ) ;
#5142=CIRCLE ( 'NONE', #1822, 22.99899999999999878 ) ;
#5143=CIRCLE ( 'NONE', #3396, 9.599999999999996092 ) ;
#5144=ORIENTED_EDGE ( 'NONE', *, *, #3070, .T. ) ;
#5145=DIRECTION ( 'NONE',  ( 0.000000000000000000, 0.000000000000000000, 1.000000000000000000 ) ) ;
#5146=ORIENTED_EDGE ( 'NONE', *, *, #5486, .F. ) ;
#5147=DIRECTION ( 'NONE',  ( -1.000000000000000000, -0.000000000000000000, -0.000000000000000000 ) ) ;
#5148=VERTEX_POINT ( 'NONE', #779 ) ;
#5150=DIRECTION ( 'NONE',  ( 0.000000000000000000, 0.000000000000000000, -1.000000000000000000 ) ) ;
#5152=CARTESIAN_POINT ( 'NONE',  ( 3.000000000000000888, 0.4575788569254873317, -22.54798042742717712 ) ) ;
#5153=DIRECTION ( 'NONE',  ( 0.000000000000000000, -1.000000000000000000, -1.048062100069321321E-14 ) ) ;
#5155=AXIS2_PLACEMENT_3D ( 'NONE', #8289, #4373, #4431 ) ;
#5156=DIRECTION ( 'NONE',  ( -1.000000000000000000, 0.000000000000000000, 0.000000000000000000 ) ) ;
#5158=EDGE_CURVE ( 'NONE', #505, #3056, #8253, .T. ) ;
#5159=CYLINDRICAL_SURFACE ( 'NONE', #2356, 9.599999999999997868 ) ;
#5160=EDGE_CURVE ( 'NONE', #5042, #5965, #2728, .T. ) ;
#5161=EDGE_CURVE ( 'NONE', #5009, #8199, #11128, .T. ) ;
#5162=CYLINDRICAL_SURFACE ( 'NONE', #2162, 9.599999999999997868 ) ;
#5163=ORIENTED_EDGE ( 'NONE', *, *, #819, .F. ) ;
#5164=CIRCLE ( 'NONE', #475, 9.599999999999996092 ) ;
#5165=DIRECTION ( 'NONE',  ( -1.000000000000000000, 0.000000000000000000, -0.000000000000000000 ) ) ;
#5166=ORIENTED_EDGE ( 'NONE', *, *, #2693, .T. ) ;
#5167=CYLINDRICAL_SURFACE ( 'NONE', #7569, 9.599999999999997868 ) ;
#5168=VERTEX_POINT ( 'NONE', #10887 ) ;
#5169=CYLINDRICAL_SURFACE ( 'NONE', #3412, 9.599999999999997868 ) ;
#5171=ADVANCED_FACE ( 'NONE', ( #2677 ), #4396, .T. ) ;
#5174=EDGE_CURVE ( 'NONE', #8841, #6834, #3307, .T. ) ;
#5175=CIRCLE ( 'NONE', #10845, 9.599999999999997868 ) ;
#5176=DIRECTION ( 'NONE',  ( -1.000000000000000000, 0.000000000000000000, 0.000000000000000000 ) ) ;
#5177=ORIENTED_EDGE ( 'NONE', *, *, #7333, .T. ) ;
#5178=ORIENTED_EDGE ( 'NONE', *, *, #8312, .F. ) ;
#5179=VERTEX_POINT ( 'NONE', #9231 ) ;
#5183=DIRECTION ( 'NONE',  ( -1.000000000000000000, 0.000000000000000000, 0.000000000000000000 ) ) ;
#5184=EDGE_CURVE ( 'NONE', #10794, #2327, #2138, .T. ) ;
#5186=DIRECTION ( 'NONE',  ( 0.000000000000000000, 0.000000000000000000, 1.000000000000000000 ) ) ;
#5187=DIRECTION ( 'NONE',  ( 0.000000000000000000, 0.000000000000000000, -1.000000000000000000 ) ) ;
#5189=ORIENTED_EDGE ( 'NONE', *, *, #11625, .F. ) ;
#5190=AXIS2_PLACEMENT_3D ( 'NONE', #9444, #5777, #187 ) ;
#5192=VERTEX_POINT ( 'NONE', #7075 ) ;
#5194=CARTESIAN_POINT ( 'NONE',  ( -10.00000000000000000, 0.000000000000000000, 0.000000000000000000 ) ) ;
#5196=CARTESIAN_POINT ( 'NONE',  ( 3.000000000000000888, 0.000000000000000000, 0.000000000000000000 ) ) ;
#5197=EDGE_LOOP ( 'NONE', ( #10913, #9560, #112, #977 ) ) ;
#5198=EDGE_CURVE ( 'NONE', #3033, #7795, #11522, .T. ) ;
#5199=DIRECTION ( 'NONE',  ( -1.000000000000000000, -0.000000000000000000, 0.000000000000000000 ) ) ;
#5200=AXIS2_PLACEMENT_3D ( 'NONE', #1775, #1713, #9918 ) ;
#5201=CYLINDRICAL_SURFACE ( 'NONE', #7464, 9.599999999999997868 ) ;
#5203=EDGE_LOOP ( 'NONE', ( #10957, #5950, #978, #350 ) ) ;
#5204=CYLINDRICAL_SURFACE ( 'NONE', #6843, 9.599999999999997868 ) ;
#5206=EDGE_CURVE ( 'NONE', #8295, #5263, #5254, .T. ) ;
#5207=ORIENTED_EDGE ( 'NONE', *, *, #3523, .T. ) ;
#5208=AXIS2_PLACEMENT_3D ( 'NONE', #6118, #9853, #4898 ) ;
#5210=ORIENTED_EDGE ( 'NONE', *, *, #10767, .T. ) ;
#5211=LINE ( 'NONE', #8712, #8333 ) ;
#5213=VERTEX_POINT ( 'NONE', #1700 ) ;
#5214=CARTESIAN_POINT ( 'NONE',  ( 3.000000000000000888, 21.58580335785685378, -6.532525787310757615 ) ) ;
#5215=DIRECTION ( 'NONE',  ( 0.000000000000000000, 0.000000000000000000, 1.000000000000000000 ) ) ;
#5219=FACE_OUTER_BOUND ( 'NONE', #9812, .T. ) ;
#5220=VERTEX_POINT ( 'NONE', #5320 ) ;
#5221=CARTESIAN_POINT ( 'NONE',  ( 0.000000000000000000, -17.06259499759954679, 14.74749645580005364 ) ) ;
#5222=ORIENTED_EDGE ( 'NONE', *, *, #11043, .T. ) ;
#5223=CARTESIAN_POINT ( 'NONE',  ( 3.000000000000000888, 9.589108953448178596, -20.41249101028201451 ) ) ;
#5224=ORIENTED_EDGE ( 'NONE', *, *, #3908, .F. ) ;
#5225=CARTESIAN_POINT ( 'NONE',  ( 3.000000000000000888, -4.240409074144249502, 22.15038895030647836 ) ) ;
#5226=EDGE_CURVE ( 'NONE', #9316, #8647, #7257, .T. ) ;
#5228=CARTESIAN_POINT ( 'NONE',  ( 0.000000000000000000, 4.135161237383914390, -24.45282072769597193 ) ) ;
#5230=CARTESIAN_POINT ( 'NONE',  ( 0.000000000000000000, -4.445336973060693531, -22.56530478845653676 ) ) ;
#5231=DIRECTION ( 'NONE',  ( 0.000000000000000000, 0.000000000000000000, 1.000000000000000000 ) ) ;
#5232=EDGE_CURVE ( 'NONE', #2526, #6927, #8977, .T. ) ;
#5234=ORIENTED_EDGE ( 'NONE', *, *, #7915, .F. ) ;
#5236=VERTEX_POINT ( 'NONE', #849 ) ;
#5239=EDGE_CURVE ( 'NONE', #5976, #384, #5266, .T. ) ;
#5240=DIRECTION ( 'NONE',  ( -1.000000000000000000, -0.000000000000000000, -0.000000000000000000 ) ) ;
#5241=EDGE_CURVE ( 'NONE', #8808, #6916, #10146, .T. ) ;
#5242=AXIS2_PLACEMENT_3D ( 'NONE', #8740, #4083, #2247 ) ;
#5244=DIRECTION ( 'NONE',  ( -1.000000000000000000, 0.000000000000000000, 0.000000000000000000 ) ) ;
#5245=DIRECTION ( 'NONE',  ( 0.000000000000000000, 0.3090169943749417336, 0.9510565162951555296 ) ) ;
#5246=EDGE_LOOP ( 'NONE', ( #8461, #9103, #4655, #5297 ) ) ;
#5247=VERTEX_POINT ( 'NONE', #11799 ) ;
#5249=ORIENTED_EDGE ( 'NONE', *, *, #5206, .T. ) ;
#5250=CARTESIAN_POINT ( 'NONE',  ( 3.000000000000000888, 0.000000000000000000, 0.000000000000000000 ) ) ;
#5251=AXIS2_PLACEMENT_3D ( 'NONE', #1448, #7064, #9950 ) ;
#5252=VECTOR ( 'NONE', #1994, 1000.000000000000000 ) ;
#5253=CARTESIAN_POINT ( 'NONE',  ( 0.000000000000000000, 0.000000000000000000, 0.000000000000000000 ) ) ;
#5254=LINE ( 'NONE', #1756, #3707 ) ;
#5255=DIRECTION ( 'NONE',  ( -1.000000000000000000, -0.000000000000000000, -0.000000000000000000 ) ) ;
#5256=ORIENTED_EDGE ( 'NONE', *, *, #6870, .T. ) ;
#5258=DIRECTION ( 'NONE',  ( 0.000000000000000000, -0.9135454576425964257, -0.4067366430758102558 ) ) ;
#5260=CIRCLE ( 'NONE', #371, 9.599999999999999645 ) ;
#5261=CARTESIAN_POINT ( 'NONE',  ( 3.000000000000000888, 22.37663021667344054, -2.811977935937859385 ) ) ;
#5262=DIRECTION ( 'NONE',  ( 0.000000000000000000, -0.1045284632676401482, -0.9945218953682747332 ) ) ;
#5263=VERTEX_POINT ( 'NONE', #9051 ) ;
#5264=EDGE_CURVE ( 'NONE', #9796, #10367, #9377, .T. ) ;
#5266=CIRCLE ( 'NONE', #2535, 9.599999999999997868 ) ;
#5268=VERTEX_POINT ( 'NONE', #11122 ) ;
#5269=DIRECTION ( 'NONE',  ( -1.000000000000000000, 0.000000000000000000, 0.000000000000000000 ) ) ;
#5270=DIRECTION ( 'NONE',  ( 1.000000000000000000, -0.000000000000000000, 0.000000000000000000 ) ) ;
#5271=VERTEX_POINT ( 'NONE', #4642 ) ;
#5272=VECTOR ( 'NONE', #6170, 1000.000000000000000 ) ;
#5273=FACE_OUTER_BOUND ( 'NONE', #8160, .T. ) ;
#5274=EDGE_CURVE ( 'NONE', #7806, #9081, #11902, .T. ) ;
#5275=DIRECTION ( 'NONE',  ( 0.000000000000000000, 0.000000000000000000, 1.000000000000000000 ) ) ;
#5277=CYLINDRICAL_SURFACE ( 'NONE', #226, 9.599999999999997868 ) ;
#5279=DIRECTION ( 'NONE',  ( -1.000000000000000000, 0.000000000000000000, 0.000000000000000000 ) ) ;
#5280=ORIENTED_EDGE ( 'NONE', *, *, #8252, .F. ) ;
#5281=DIRECTION ( 'NONE',  ( -1.000000000000000000, 0.000000000000000000, 0.000000000000000000 ) ) ;
#5282=CIRCLE ( 'NONE', #6270, 9.600000000000001421 ) ;
#5283=ORIENTED_EDGE ( 'NONE', *, *, #9981, .F. ) ;
#5285=FACE_OUTER_BOUND ( 'NONE', #11987, .T. ) ;
#5287=ORIENTED_EDGE ( 'NONE', *, *, #2546, .F. ) ;
#5288=AXIS2_PLACEMENT_3D ( 'NONE', #5598, #1922, #5727 ) ;
#5289=CARTESIAN_POINT ( 'NONE',  ( 3.000000000000000888, 23.88662356770124973, -6.668524164681381095 ) ) ;
#5290=CIRCLE ( 'NONE', #11544, 9.599999999999997868 ) ;
#5291=CARTESIAN_POINT ( 'NONE',  ( 3.000000000000000888, -19.10918332567968747, 15.80756504416684649 ) ) ;
#5295=DIRECTION ( 'NONE',  ( 0.000000000000000000, 0.000000000000000000, 1.000000000000000000 ) ) ;
#5296=FACE_OUTER_BOUND ( 'NONE', #1346, .T. ) ;
#5297=ORIENTED_EDGE ( 'NONE', *, *, #10780, .T. ) ;
#5298=AXIS2_PLACEMENT_3D ( 'NONE', #6437, #3749, #4667 ) ;
#5299=ORIENTED_EDGE ( 'NONE', *, *, #145, .T. ) ;
#5300=AXIS2_PLACEMENT_3D ( 'NONE', #5427, #529, #8976 ) ;
#5301=AXIS2_PLACEMENT_3D ( 'NONE', #9065, #547, #5262 ) ;
#5302=EDGE_LOOP ( 'NONE', ( #5975, #2935, #8845, #2051 ) ) ;
#5304=FACE_OUTER_BOUND ( 'NONE', #4447, .T. ) ;
#5305=DIRECTION ( 'NONE',  ( 0.000000000000000000, 0.000000000000000000, 1.000000000000000000 ) ) ;
#5306=AXIS2_PLACEMENT_3D ( 'NONE', #3775, #1810, #1118 ) ;
#5307=AXIS2_PLACEMENT_3D ( 'NONE', #2983, #7686, #11424 ) ;
#5308=VECTOR ( 'NONE', #2937, 1000.000000000000000 ) ;
#5310=AXIS2_PLACEMENT_3D ( 'NONE', #2299, #217, #1268 ) ;
#5311=DIRECTION ( 'NONE',  ( -1.000000000000000000, 0.000000000000000000, -0.000000000000000000 ) ) ;
#5312=EDGE_CURVE ( 'NONE', #2975, #8970, #3897, .T. ) ;
#5313=CARTESIAN_POINT ( 'NONE',  ( 0.000000000000000000, 4.240409074144097623, 22.15038895030650679 ) ) ;
#5314=ORIENTED_EDGE ( 'NONE', *, *, #4648, .F. ) ;
#5315=VERTEX_POINT ( 'NONE', #5678 ) ;
#5317=CIRCLE ( 'NONE', #7253, 9.599999999999997868 ) ;
#5318=ORIENTED_EDGE ( 'NONE', *, *, #556, .T. ) ;
#5320=CARTESIAN_POINT ( 'NONE',  ( 3.000000000000000888, 13.79477846460820700, -18.40266524480574972 ) ) ;
#5321=AXIS2_PLACEMENT_3D ( 'NONE', #11509, #3130, #3865 ) ;
#5322=DIRECTION ( 'NONE',  ( -1.000000000000000000, -0.000000000000000000, 0.000000000000000000 ) ) ;
#5323=ORIENTED_EDGE ( 'NONE', *, *, #1865, .T. ) ;
#5324=CARTESIAN_POINT ( 'NONE',  ( 0.000000000000000000, -13.23915371906968375, 18.80635025205165434 ) ) ;
#5325=CARTESIAN_POINT ( 'NONE',  ( 3.000000000000000888, -6.532525787310825116, -21.58580335785683246 ) ) ;
#5327=CIRCLE ( 'NONE', #8053, 9.599999999999997868 ) ;
#5328=EDGE_CURVE ( 'NONE', #3995, #2252, #8203, .T. ) ;
#5329=CIRCLE ( 'NONE', #10207, 24.80000000000000071 ) ;
#5330=CIRCLE ( 'NONE', #11770, 22.99900000000000233 ) ;
#5331=CARTESIAN_POINT ( 'NONE',  ( 3.000000000000000888, 0.000000000000000000, 0.000000000000000000 ) ) ;
#5332=ORIENTED_EDGE ( 'NONE', *, *, #5226, .T. ) ;
#5333=CYLINDRICAL_SURFACE ( 'NONE', #4722, 9.599999999999997868 ) ;
#5334=EDGE_LOOP ( 'NONE', ( #9303, #7309, #2442, #11266 ) ) ;
#5335=ORIENTED_EDGE ( 'NONE', *, *, #3756, .T. ) ;
#5337=AXIS2_PLACEMENT_3D ( 'NONE', #9058, #3611, #3434 ) ;
#5338=EDGE_CURVE ( 'NONE', #2284, #490, #5665, .T. ) ;
#5340=ORIENTED_EDGE ( 'NONE', *, *, #10053, .T. ) ;
#5341=CARTESIAN_POINT ( 'NONE',  ( 3.000000000000000888, 20.65684170206509762, -13.72351598154876484 ) ) ;
#5342=VECTOR ( 'NONE', #6804, 1000.000000000000000 ) ;
#5343=DIRECTION ( 'NONE',  ( -1.000000000000000000, 0.000000000000000000, -0.000000000000000000 ) ) ;
#5345=EDGE_CURVE ( 'NONE', #9863, #5811, #380, .T. ) ;
#5346=CARTESIAN_POINT ( 'NONE',  ( 3.000000000000000888, 17.97274125076074114, 13.62355943574025652 ) ) ;
#5347=FACE_OUTER_BOUND ( 'NONE', #11074, .T. ) ;
#5348=CIRCLE ( 'NONE', #3581, 9.599999999999997868 ) ;
#5349=ORIENTED_EDGE ( 'NONE', *, *, #2622, .T. ) ;
#5350=FACE_OUTER_BOUND ( 'NONE', #396, .T. ) ;
#5351=ORIENTED_EDGE ( 'NONE', *, *, #8498, .F. ) ;
#5352=VECTOR ( 'NONE', #3804, 1000.000000000000000 ) ;
#5353=EDGE_CURVE ( 'NONE', #1896, #5661, #7017, .T. ) ;
#5355=DIRECTION ( 'NONE',  ( -1.000000000000000000, -0.000000000000000000, 0.000000000000000000 ) ) ;
#5356=ORIENTED_EDGE ( 'NONE', *, *, #8247, .T. ) ;
#5357=AXIS2_PLACEMENT_3D ( 'NONE', #6416, #1039, #911 ) ;
#5358=CARTESIAN_POINT ( 'NONE',  ( 0.000000000000000000, -2.745295967525840375, -22.83456483164691875 ) ) ;
#5359=CARTESIAN_POINT ( 'NONE',  ( 0.000000000000000000, 17.71842311621553279, -17.35216073792423330 ) ) ;
#5362=CARTESIAN_POINT ( 'NONE',  ( 0.000000000000000000, -22.47229024614978599, 1.901833551798177036 ) ) ;
#5363=DIRECTION ( 'NONE',  ( -1.000000000000000000, 0.000000000000000000, -0.000000000000000000 ) ) ;
#5364=VERTEX_POINT ( 'NONE', #10384 ) ;
#5365=EDGE_LOOP ( 'NONE', ( #3930, #11022, #6907, #11007 ) ) ;
#5366=VECTOR ( 'NONE', #4886, 1000.000000000000000 ) ;
#5367=EDGE_CURVE ( 'NONE', #2865, #4186, #7444, .T. ) ;
#5368=EDGE_CURVE ( 'NONE', #7212, #5213, #6589, .T. ) ;
#5369=ORIENTED_EDGE ( 'NONE', *, *, #11033, .F. ) ;
#5372=CARTESIAN_POINT ( 'NONE',  ( 0.000000000000000000, 0.000000000000000000, 0.000000000000000000 ) ) ;
#5373=CIRCLE ( 'NONE', #6919, 22.99900000000000588 ) ;
#5375=DIRECTION ( 'NONE',  ( -1.000000000000000000, 0.000000000000000000, -0.000000000000000000 ) ) ;
#5376=CARTESIAN_POINT ( 'NONE',  ( 3.000000000000000888, 19.74380051311556628, -11.79560690673851475 ) ) ;
#5377=ORIENTED_EDGE ( 'NONE', *, *, #10475, .T. ) ;
#5379=VERTEX_POINT ( 'NONE', #7377 ) ;
#5380=DIRECTION ( 'NONE',  ( -1.000000000000000000, 0.000000000000000000, -0.000000000000000000 ) ) ;
#5383=DIRECTION ( 'NONE',  ( 1.000000000000000000, 0.000000000000000000, -0.000000000000000000 ) ) ;
#5384=DIRECTION ( 'NONE',  ( -1.000000000000000000, 0.000000000000000000, 0.000000000000000000 ) ) ;
#5385=EDGE_CURVE ( 'NONE', #1013, #9776, #12095, .T. ) ;
#5388=DIRECTION ( 'NONE',  ( 0.000000000000000000, 0.000000000000000000, 1.000000000000000000 ) ) ;
#5389=DIRECTION ( 'NONE',  ( 0.000000000000000000, 0.000000000000000000, 1.000000000000000000 ) ) ;
#5390=ORIENTED_EDGE ( 'NONE', *, *, #2220, .T. ) ;
#5392=ADVANCED_FACE ( 'NONE', ( #7622 ), #100, .T. ) ;
#5393=VERTEX_POINT ( 'NONE', #11193 ) ;
#5395=VECTOR ( 'NONE', #11635, 1000.000000000000000 ) ;
#5396=ORIENTED_EDGE ( 'NONE', *, *, #6904, .F. ) ;
#5397=EDGE_CURVE ( 'NONE', #3932, #4536, #2064, .T. ) ;
#5398=DIRECTION ( 'NONE',  ( 0.000000000000000000, 0.000000000000000000, -1.000000000000000000 ) ) ;
#5399=CYLINDRICAL_SURFACE ( 'NONE', #4007, 9.599999999999997868 ) ;
#5401=DIRECTION ( 'NONE',  ( 0.000000000000000000, 0.7431448254773909134, 0.6691306063588620123 ) ) ;
#5402=DIRECTION ( 'NONE',  ( -1.000000000000000000, -0.000000000000000000, -0.000000000000000000 ) ) ;
#5403=VECTOR ( 'NONE', #10226, 1000.000000000000000 ) ;
#5404=VERTEX_POINT ( 'NONE', #6470 ) ;
#5405=CARTESIAN_POINT ( 'NONE',  ( 3.000000000000000888, -14.74749645580022772, 17.06259499759939402 ) ) ;
#5406=VERTEX_POINT ( 'NONE', #8443 ) ;
#5408=DIRECTION ( 'NONE',  ( 0.000000000000000000, 0.000000000000000000, -1.000000000000000000 ) ) ;
#5409=( LENGTH_UNIT ( ) NAMED_UNIT ( * ) SI_UNIT ( .MILLI., .METRE. ) );
#5410=ORIENTED_EDGE ( 'NONE', *, *, #4154, .F. ) ;
#5411=FACE_OUTER_BOUND ( 'NONE', #4924, .T. ) ;
#5412=AXIS2_PLACEMENT_3D ( 'NONE', #9906, #666, #3364 ) ;
#5413=CARTESIAN_POINT ( 'NONE',  ( 3.000000000000000888, 24.77821629063821973, -1.039229259764575364 ) ) ;
#5416=CYLINDRICAL_SURFACE ( 'NONE', #4564, 24.80000000000000071 ) ;
#5419=EDGE_LOOP ( 'NONE', ( #9861, #5874, #327, #960 ) ) ;
#5420=EDGE_CURVE ( 'NONE', #8541, #7251, #796, .T. ) ;
#5422=CARTESIAN_POINT ( 'NONE',  ( 3.000000000000000888, 2.745295967526300451, -22.83456483164686546 ) ) ;
#5423=DIRECTION ( 'NONE',  ( -1.000000000000000000, 0.000000000000000000, -0.000000000000000000 ) ) ;
#5424=ADVANCED_FACE ( 'NONE', ( #6533 ), #1884, .T. ) ;
#5426=AXIS2_PLACEMENT_3D ( 'NONE', #9820, #10618, #7917 ) ;
#5427=CARTESIAN_POINT ( 'NONE',  ( 3.000000000000000888, 1.901833551798570721, -22.47229024614975401 ) ) ;
#5428=CARTESIAN_POINT ( 'NONE',  ( 3.000000000000000888, 0.000000000000000000, 0.000000000000000000 ) ) ;
#5429=ORIENTED_EDGE ( 'NONE', *, *, #8626, .F. ) ;
#5430=VERTEX_POINT ( 'NONE', #3790 ) ;
#5431=CYLINDRICAL_SURFACE ( 'NONE', #6702, 24.80000000000000071 ) ;
#5433=CIRCLE ( 'NONE', #7371, 24.80000000000000071 ) ;
#5434=DIRECTION ( 'NONE',  ( -1.000000000000000000, 0.000000000000000000, 0.000000000000000000 ) ) ;
#5436=CARTESIAN_POINT ( 'NONE',  ( 1.500000000000000444, -8.645255683529168067, 23.24434456306322616 ) ) ;
#5437=CARTESIAN_POINT ( 'NONE',  ( 3.000000000000000888, 19.75591328264886215, 10.87771529938168946 ) ) ;
#5438=CARTESIAN_POINT ( 'NONE',  ( 3.000000000000000888, 20.08719549084865008, 11.20082935824082249 ) ) ;
#5439=CIRCLE ( 'NONE', #2506, 24.80000000000000071 ) ;
#5440=ORIENTED_EDGE ( 'NONE', *, *, #4485, .F. ) ;
#5441=AXIS2_PLACEMENT_3D ( 'NONE', #6285, #7301, #9279 ) ;
#5442=DIRECTION ( 'NONE',  ( 0.000000000000000000, 0.000000000000000000, 1.000000000000000000 ) ) ;
#5443=ORIENTED_EDGE ( 'NONE', *, *, #9185, .F. ) ;
#5444=ORIENTED_EDGE ( 'NONE', *, *, #893, .T. ) ;
#5446=ORIENTED_EDGE ( 'NONE', *, *, #7020, .F. ) ;
#5447=DIRECTION ( 'NONE',  ( 1.000000000000000000, -0.000000000000000000, -0.000000000000000000 ) ) ;
#5448=ORIENTED_EDGE ( 'NONE', *, *, #3040, .F. ) ;
#5449=EDGE_CURVE ( 'NONE', #4594, #4467, #9201, .T. ) ;
#5450=CARTESIAN_POINT ( 'NONE',  ( 0.000000000000000000, -18.80635025205178579, 13.23915371906949012 ) ) ;
#5451=DIRECTION ( 'NONE',  ( 0.000000000000000000, 0.000000000000000000, 1.000000000000000000 ) ) ;
#5453=CYLINDRICAL_SURFACE ( 'NONE', #4146, 9.599999999999994316 ) ;
#5454=DIRECTION ( 'NONE',  ( 0.000000000000000000, 0.000000000000000000, 1.000000000000000000 ) ) ;
#5455=ORIENTED_EDGE ( 'NONE', *, *, #1488, .F. ) ;
#5456=LINE ( 'NONE', #8282, #194 ) ;
#5457=EDGE_CURVE ( 'NONE', #6518, #7873, #1598, .T. ) ;
#5459=AXIS2_PLACEMENT_3D ( 'NONE', #1036, #9471, #8316 ) ;
#5460=VECTOR ( 'NONE', #295, 1000.000000000000000 ) ;
#5461=EDGE_CURVE ( 'NONE', #6550, #7092, #23, .T. ) ;
#5464=CARTESIAN_POINT ( 'NONE',  ( 3.000000000000000888, 4.445336973060856955, 22.56530478845650123 ) ) ;
#5465=DIRECTION ( 'NONE',  ( 0.000000000000000000, 0.8090169943749485615, -0.5877852522924714718 ) ) ;
#5466=DIRECTION ( 'NONE',  ( 0.000000000000000000, 0.000000000000000000, 1.000000000000000000 ) ) ;
#5467=DIRECTION ( 'NONE',  ( 0.000000000000000000, 0.000000000000000000, 1.000000000000000000 ) ) ;
#5468=DIRECTION ( 'NONE',  ( -1.000000000000000000, 0.000000000000000000, -0.000000000000000000 ) ) ;
#5470=LINE ( 'NONE', #2904, #11781 ) ;
#5471=EDGE_CURVE ( 'NONE', #5393, #11133, #7875, .T. ) ;
#5472=CARTESIAN_POINT ( 'NONE',  ( 3.000000000000000888, 0.000000000000000000, 0.000000000000000000 ) ) ;
#5474=EDGE_LOOP ( 'NONE', ( #9773, #6429, #5755, #9988 ) ) ;
#5475=ORIENTED_EDGE ( 'NONE', *, *, #7048, .F. ) ;
#5476=CIRCLE ( 'NONE', #4508, 22.99899999999999523 ) ;
#5477=CARTESIAN_POINT ( 'NONE',  ( 0.000000000000000000, -1.556492618230473468, -24.75110766671653906 ) ) ;
#5479=AXIS2_PLACEMENT_3D ( 'NONE', #8032, #7104, #10855 ) ;
#5480=CARTESIAN_POINT ( 'NONE',  ( 0.000000000000000000, 19.10918332567978695, -15.80756504416672215 ) ) ;
#5481=EDGE_CURVE ( 'NONE', #1256, #1804, #3748, .T. ) ;
#5482=CYLINDRICAL_SURFACE ( 'NONE', #10128, 9.599999999999997868 ) ;
#5485=CARTESIAN_POINT ( 'NONE',  ( 1.500000000000000444, -24.75110766671653195, 1.556492618230556513 ) ) ;
#5486=EDGE_CURVE ( 'NONE', #2776, #10367, #10587, .T. ) ;
#5487=CARTESIAN_POINT ( 'NONE',  ( 0.000000000000000000, 0.000000000000000000, 0.000000000000000000 ) ) ;
#5488=ORIENTED_EDGE ( 'NONE', *, *, #11879, .T. ) ;
#5489=VECTOR ( 'NONE', #11455, 1000.000000000000000 ) ;
#5490=DIRECTION ( 'NONE',  ( -1.000000000000000000, 0.000000000000000000, 0.000000000000000000 ) ) ;
#5491=EDGE_LOOP ( 'NONE', ( #5906, #9390, #10562, #5013 ) ) ;
#5492=ORIENTED_EDGE ( 'NONE', *, *, #5198, .T. ) ;
#5494=ORIENTED_EDGE ( 'NONE', *, *, #7004, .T. ) ;
#5496=CYLINDRICAL_SURFACE ( 'NONE', #7809, 9.599999999999997868 ) ;
#5497=EDGE_CURVE ( 'NONE', #4594, #7105, #8040, .T. ) ;
#5498=AXIS2_PLACEMENT_3D ( 'NONE', #10074, #2490, #5186 ) ;
#5501=FACE_OUTER_BOUND ( 'NONE', #11842, .T. ) ;
#5503=DIRECTION ( 'NONE',  ( -1.000000000000000000, 0.000000000000000000, 0.000000000000000000 ) ) ;
#5506=VECTOR ( 'NONE', #1909, 1000.000000000000000 ) ;
#5507=CARTESIAN_POINT ( 'NONE',  ( 0.000000000000000000, 0.000000000000000000, 0.000000000000000000 ) ) ;
#5508=ORIENTED_EDGE ( 'NONE', *, *, #2420, .F. ) ;
#5509=VERTEX_POINT ( 'NONE', #5861 ) ;
#5510=CARTESIAN_POINT ( 'NONE',  ( 3.000000000000000888, -21.96011696265487600, -5.135568396240250522 ) ) ;
#5511=AXIS2_PLACEMENT_3D ( 'NONE', #2890, #1056, #7589 ) ;
#5512=ORIENTED_EDGE ( 'NONE', *, *, #9512, .T. ) ;
#5513=ORIENTED_EDGE ( 'NONE', *, *, #1143, .T. ) ;
#5515=DIRECTION ( 'NONE',  ( -1.000000000000000000, 0.000000000000000000, -0.000000000000000000 ) ) ;
#5516=VERTEX_POINT ( 'NONE', #10746 ) ;
#5517=CIRCLE ( 'NONE', #9615, 9.599999999999997868 ) ;
#5518=AXIS2_PLACEMENT_3D ( 'NONE', #12057, #7466, #10229 ) ;
#5520=DIRECTION ( 'NONE',  ( -1.000000000000000000, -0.000000000000000000, -0.000000000000000000 ) ) ;
#5522=FACE_OUTER_BOUND ( 'NONE', #8514, .T. ) ;
#5523=DIRECTION ( 'NONE',  ( -1.000000000000000000, -0.000000000000000000, -0.000000000000000000 ) ) ;
#5524=ORIENTED_EDGE ( 'NONE', *, *, #1143, .F. ) ;
#5525=ORIENTED_EDGE ( 'NONE', *, *, #6921, .F. ) ;
#5526=CIRCLE ( 'NONE', #8603, 9.599999999999997868 ) ;
#5527=DIRECTION ( 'NONE',  ( 0.000000000000000000, 0.9945218953682729568, 0.1045284632676570929 ) ) ;
#5528=ORIENTED_EDGE ( 'NONE', *, *, #4525, .T. ) ;
#5531=DIRECTION ( 'NONE',  ( 0.000000000000000000, 0.000000000000000000, 1.000000000000000000 ) ) ;
#5532=VERTEX_POINT ( 'NONE', #3963 ) ;
#5533=DIRECTION ( 'NONE',  ( -1.000000000000000000, 0.000000000000000000, 0.000000000000000000 ) ) ;
#5534=EDGE_CURVE ( 'NONE', #5028, #11239, #6864, .T. ) ;
#5535=DIRECTION ( 'NONE',  ( -1.000000000000000000, -0.000000000000000000, 0.000000000000000000 ) ) ;
#5536=DIRECTION ( 'NONE',  ( 0.000000000000000000, 0.000000000000000000, 1.000000000000000000 ) ) ;
#5538=DIRECTION ( 'NONE',  ( -1.000000000000000000, -0.000000000000000000, 0.000000000000000000 ) ) ;
#5539=ADVANCED_FACE ( 'NONE', ( #4145 ), #7811, .T. ) ;
#5540=DIRECTION ( 'NONE',  ( 0.000000000000000000, 0.000000000000000000, 1.000000000000000000 ) ) ;
#5541=CIRCLE ( 'NONE', #9060, 9.599999999999997868 ) ;
#5542=AXIS2_PLACEMENT_3D ( 'NONE', #3736, #7461, #237 ) ;
#5543=EDGE_LOOP ( 'NONE', ( #8955, #4283, #8016, #8171 ) ) ;
#5544=ORIENTED_EDGE ( 'NONE', *, *, #767, .F. ) ;
#5545=ORIENTED_EDGE ( 'NONE', *, *, #10467, .F. ) ;
#5546=CIRCLE ( 'NONE', #4182, 24.80000000000000071 ) ;
#5547=CYLINDRICAL_SURFACE ( 'NONE', #11711, 9.599999999999997868 ) ;
#5549=EDGE_CURVE ( 'NONE', #2329, #9635, #3351, .T. ) ;
#5551=CARTESIAN_POINT ( 'NONE',  ( 3.000000000000000888, 24.45282072769606430, -4.135161237383341515 ) ) ;
#5552=EDGE_CURVE ( 'NONE', #1145, #5516, #1385, .T. ) ;
#5554=FACE_OUTER_BOUND ( 'NONE', #6606, .T. ) ;
#5555=VECTOR ( 'NONE', #11890, 1000.000000000000000 ) ;
#5557=ORIENTED_EDGE ( 'NONE', *, *, #2509, .T. ) ;
#5558=EDGE_LOOP ( 'NONE', ( #11910, #8655, #7756, #5283 ) ) ;
#5559=ORIENTED_EDGE ( 'NONE', *, *, #11105, .T. ) ;
#5560=CARTESIAN_POINT ( 'NONE',  ( 1.499999999999999556, -6.668524164681463695, -23.88662356770121775 ) ) ;
#5562=CIRCLE ( 'NONE', #2041, 9.599999999999997868 ) ;
#5563=CYLINDRICAL_SURFACE ( 'NONE', #565, 22.99899999999999878 ) ;
#5564=CARTESIAN_POINT ( 'NONE',  ( 3.000000000000000888, 6.532525787311267429, -21.58580335785669746 ) ) ;
#5565=DIRECTION ( 'NONE',  ( 0.000000000000000000, -0.7431448254773861395, -0.6691306063588672304 ) ) ;
#5568=CARTESIAN_POINT ( 'NONE',  ( 3.000000000000000888, 0.000000000000000000, 0.000000000000000000 ) ) ;
#5569=CIRCLE ( 'NONE', #2438, 22.99900000000000588 ) ;
#5570=EDGE_LOOP ( 'NONE', ( #646, #11574, #8830, #3452 ) ) ;
#5571=VERTEX_POINT ( 'NONE', #4021 ) ;
#5572=CYLINDRICAL_SURFACE ( 'NONE', #1193, 22.99899999999999878 ) ;
#5574=VERTEX_POINT ( 'NONE', #5119 ) ;
#5576=ADVANCED_FACE ( 'NONE', ( #3224 ), #5001, .T. ) ;
#5577=CARTESIAN_POINT ( 'NONE',  ( 3.000000000000000888, 0.000000000000000000, 0.000000000000000000 ) ) ;
#5578=EDGE_LOOP ( 'NONE', ( #5429, #7755, #8269, #7982 ) ) ;
#5579=CARTESIAN_POINT ( 'NONE',  ( 3.000000000000000888, -4.135161237383746524, 24.45282072769599679 ) ) ;
#5580=CARTESIAN_POINT ( 'NONE',  ( 0.000000000000000000, -11.67026512804534022, -19.29833442572371638 ) ) ;
#5583=EDGE_CURVE ( 'NONE', #11368, #308, #8859, .T. ) ;
#5586=ORIENTED_EDGE ( 'NONE', *, *, #4189, .T. ) ;
#5587=CARTESIAN_POINT ( 'NONE',  ( -10.00000000000000000, 0.000000000000000000, 0.000000000000000000 ) ) ;
#5588=EDGE_LOOP ( 'NONE', ( #5989, #753, #4804, #11557 ) ) ;
#5589=CIRCLE ( 'NONE', #9488, 9.599999999999997868 ) ;
#5592=DIRECTION ( 'NONE',  ( -1.000000000000000000, -0.000000000000000000, -0.000000000000000000 ) ) ;
#5593=FACE_OUTER_BOUND ( 'NONE', #1901, .T. ) ;
#5595=VECTOR ( 'NONE', #3441, 1000.000000000000000 ) ;
#5597=CYLINDRICAL_SURFACE ( 'NONE', #644, 9.599999999999997868 ) ;
#5598=CARTESIAN_POINT ( 'NONE',  ( 0.000000000000000000, 0.000000000000000000, 0.000000000000000000 ) ) ;
#5599=ORIENTED_EDGE ( 'NONE', *, *, #11296, .T. ) ;
#5600=VERTEX_POINT ( 'NONE', #8681 ) ;
#5602=AXIS2_PLACEMENT_3D ( 'NONE', #7213, #6318, #9247 ) ;
#5603=DIRECTION ( 'NONE',  ( -1.000000000000000000, -0.000000000000000000, -0.000000000000000000 ) ) ;
#5605=FACE_OUTER_BOUND ( 'NONE', #7094, .T. ) ;
#5606=CARTESIAN_POINT ( 'NONE',  ( 1.499999999999999556, 1.556492618230641556, 24.75110766671652485 ) ) ;
#5610=DIRECTION ( 'NONE',  ( -1.000000000000000000, 0.000000000000000000, 0.000000000000000000 ) ) ;
#5611=ORIENTED_EDGE ( 'NONE', *, *, #3530, .T. ) ;
#5613=ORIENTED_EDGE ( 'NONE', *, *, #4038, .T. ) ;
#5614=EDGE_CURVE ( 'NONE', #3056, #1694, #2368, .T. ) ;
#5615=ORIENTED_EDGE ( 'NONE', *, *, #6579, .F. ) ;
#5616=DIRECTION ( 'NONE',  ( 1.000000000000000000, 0.000000000000000000, -0.000000000000000000 ) ) ;
#5617=EDGE_CURVE ( 'NONE', #9078, #117, #2495, .T. ) ;
#5618=DIRECTION ( 'NONE',  ( -1.000000000000000000, 0.000000000000000000, 0.000000000000000000 ) ) ;
#5619=CARTESIAN_POINT ( 'NONE',  ( 1.499999999999999556, 3.623565124517435176, -24.53384959170453783 ) ) ;
#5621=CIRCLE ( 'NONE', #1908, 22.99899999999999878 ) ;
#5622=DIRECTION ( 'NONE',  ( 0.000000000000000000, -0.5877852522924797984, 0.8090169943749426773 ) ) ;
#5625=DIRECTION ( 'NONE',  ( 0.000000000000000000, 0.000000000000000000, 1.000000000000000000 ) ) ;
#5626=ORIENTED_EDGE ( 'NONE', *, *, #3161, .T. ) ;
#5627=ORIENTED_EDGE ( 'NONE', *, *, #10391, .T. ) ;
#5629=ORIENTED_EDGE ( 'NONE', *, *, #8383, .F. ) ;
#5630=AXIS2_PLACEMENT_3D ( 'NONE', #1067, #1916, #8 ) ;
#5631=ORIENTED_EDGE ( 'NONE', *, *, #3414, .T. ) ;
#5632=CARTESIAN_POINT ( 'NONE',  ( 3.000000000000000888, 0.000000000000000000, 0.000000000000000000 ) ) ;
#5633=DIRECTION ( 'NONE',  ( -1.000000000000000000, -0.000000000000000000, 0.000000000000000000 ) ) ;
#5634=ORIENTED_EDGE ( 'NONE', *, *, #4478, .F. ) ;
#5635=DIRECTION ( 'NONE',  ( 0.000000000000000000, 0.000000000000000000, 1.000000000000000000 ) ) ;
#5636=ADVANCED_FACE ( 'NONE', ( #11911 ), #5431, .T. ) ;
#5637=CARTESIAN_POINT ( 'NONE',  ( 0.000000000000000000, -21.58580335785672233, -6.532525787311189269 ) ) ;
#5639=AXIS2_PLACEMENT_3D ( 'NONE', #103, #8319, #7448 ) ;
#5640=AXIS2_PLACEMENT_3D ( 'NONE', #144, #10495, #4755 ) ;
#5641=CARTESIAN_POINT ( 'NONE',  ( 0.000000000000000000, 6.779701584703026640, -21.97702544527751201 ) ) ;
#5642=EDGE_CURVE ( 'NONE', #6844, #1972, #6124, .T. ) ;
#5643=CARTESIAN_POINT ( 'NONE',  ( 3.000000000000000888, -13.23915371906968019, 18.80635025205165078 ) ) ;
#5644=EDGE_LOOP ( 'NONE', ( #1111, #2786, #3536, #5756 ) ) ;
#5645=CYLINDRICAL_SURFACE ( 'NONE', #8223, 9.599999999999999645 ) ;
#5646=VERTEX_POINT ( 'NONE', #4395 ) ;
#5648=CIRCLE ( 'NONE', #4861, 24.80000000000000071 ) ;
#5649=AXIS2_PLACEMENT_3D ( 'NONE', #3329, #4992, #1372 ) ;
#5652=ADVANCED_FACE ( 'NONE', ( #8129 ), #9160, .T. ) ;
#5653=CARTESIAN_POINT ( 'NONE',  ( 0.000000000000000000, 0.000000000000000000, 0.000000000000000000 ) ) ;
#5654=DIRECTION ( 'NONE',  ( 0.000000000000000000, 0.000000000000000000, -1.000000000000000000 ) ) ;
#5657=CARTESIAN_POINT ( 'NONE',  ( 3.000000000000000888, 12.88318129270179035, 18.51065745848382349 ) ) ;
#5658=AXIS2_PLACEMENT_3D ( 'NONE', #2497, #719, #8190 ) ;
#5659=VECTOR ( 'NONE', #5270, 1000.000000000000000 ) ;
#5661=VERTEX_POINT ( 'NONE', #778 ) ;
#5662=EDGE_LOOP ( 'NONE', ( #9174, #4316, #6497, #6410 ) ) ;
#5663=CYLINDRICAL_SURFACE ( 'NONE', #726, 9.599999999999997868 ) ;
#5665=CIRCLE ( 'NONE', #10745, 22.99899999999999523 ) ;
#5666=FACE_OUTER_BOUND ( 'NONE', #3912, .T. ) ;
#5667=CIRCLE ( 'NONE', #175, 22.99900000000000233 ) ;
#5670=DIRECTION ( 'NONE',  ( 0.000000000000000000, 0.000000000000000000, 1.000000000000000000 ) ) ;
#5671=VERTEX_POINT ( 'NONE', #7255 ) ;
#5672=AXIS2_PLACEMENT_3D ( 'NONE', #3101, #4875, #457 ) ;
#5673=ORIENTED_EDGE ( 'NONE', *, *, #2522, .F. ) ;
#5674=VERTEX_POINT ( 'NONE', #4517 ) ;
#5675=CIRCLE ( 'NONE', #4496, 9.599999999999997868 ) ;
#5677=CARTESIAN_POINT ( 'NONE',  ( 1.499999999999999556, -24.77821629063822328, 1.039229259764403501 ) ) ;
#5678=CARTESIAN_POINT ( 'NONE',  ( 3.000000000000000888, -22.54798042742717357, 9.142421143074578538 ) ) ;
#5679=DIRECTION ( 'NONE',  ( 0.000000000000000000, 0.000000000000000000, 1.000000000000000000 ) ) ;
#5680=FACE_OUTER_BOUND ( 'NONE', #632, .T. ) ;
#5681=AXIS2_PLACEMENT_3D ( 'NONE', #4624, #2905, #12075 ) ;
#5682=CARTESIAN_POINT ( 'NONE',  ( 0.000000000000000000, 15.80756504416717334, -19.10918332567941036 ) ) ;
#5683=AXIS2_PLACEMENT_3D ( 'NONE', #8261, #8197, #3613 ) ;
#5684=EDGE_CURVE ( 'NONE', #4987, #4256, #8187, .T. ) ;
#5685=AXIS2_PLACEMENT_3D ( 'NONE', #9186, #7535, #811 ) ;
#5687=CARTESIAN_POINT ( 'NONE',  ( -10.00000000000000000, 0.000000000000000000, 0.000000000000000000 ) ) ;
#5689=EDGE_CURVE ( 'NONE', #845, #7676, #5142, .T. ) ;
#5690=DIRECTION ( 'NONE',  ( -1.000000000000000000, 0.000000000000000000, -0.000000000000000000 ) ) ;
#5692=ORIENTED_EDGE ( 'NONE', *, *, #8230, .F. ) ;
#5693=ORIENTED_EDGE ( 'NONE', *, *, #466, .F. ) ;
#5694=CARTESIAN_POINT ( 'NONE',  ( 0.000000000000000000, -21.76479567747236743, -7.432877647175426539 ) ) ;
#5695=AXIS2_PLACEMENT_3D ( 'NONE', #6736, #11329, #5825 ) ;
#5696=ORIENTED_EDGE ( 'NONE', *, *, #11744, .F. ) ;
#5697=CIRCLE ( 'NONE', #4719, 22.99899999999999878 ) ;
#5698=DIRECTION ( 'NONE',  ( -1.000000000000000000, -0.000000000000000000, 0.000000000000000000 ) ) ;
#5699=CIRCLE ( 'NONE', #2756, 9.599999999999999645 ) ;
#5700=CARTESIAN_POINT ( 'NONE',  ( 3.000000000000000888, -19.74380051311548456, 11.79560690673865331 ) ) ;
#5701=ORIENTED_EDGE ( 'NONE', *, *, #4040, .F. ) ;
#5702=EDGE_CURVE ( 'NONE', #8206, #11050, #7683, .T. ) ;
#5704=CARTESIAN_POINT ( 'NONE',  ( 0.000000000000000000, -2.062268319295719632, 22.90635393027945454 ) ) ;
#5706=CIRCLE ( 'NONE', #17, 22.99899999999999878 ) ;
#5709=AXIS2_PLACEMENT_3D ( 'NONE', #8352, #1731, #1981 ) ;
#5710=CARTESIAN_POINT ( 'NONE',  ( 3.000000000000000888, -9.667200211209964422, 20.86861857134731579 ) ) ;
#5711=ORIENTED_EDGE ( 'NONE', *, *, #6149, .T. ) ;
#5712=DIRECTION ( 'NONE',  ( -1.000000000000000000, -0.000000000000000000, 0.000000000000000000 ) ) ;
#5714=EDGE_CURVE ( 'NONE', #9333, #730, #6515, .T. ) ;
#5716=AXIS2_PLACEMENT_3D ( 'NONE', #874, #1906, #2703 ) ;
#5717=VECTOR ( 'NONE', #8758, 1000.000000000000000 ) ;
#5718=CARTESIAN_POINT ( 'NONE',  ( 1.499999999999999556, 3.623565124517106995, 24.53384959170458757 ) ) ;
#5719=ORIENTED_EDGE ( 'NONE', *, *, #6137, .F. ) ;
#5720=CIRCLE ( 'NONE', #9976, 9.599999999999999645 ) ;
#5721=EDGE_CURVE ( 'NONE', #4653, #9467, #8066, .T. ) ;
#5722=CARTESIAN_POINT ( 'NONE',  ( 0.000000000000000000, 0.000000000000000000, 0.000000000000000000 ) ) ;
#5723=FACE_OUTER_BOUND ( 'NONE', #2267, .T. ) ;
#5725=CARTESIAN_POINT ( 'NONE',  ( 3.000000000000000888, -22.99643626497956461, -0.3433949777334098785 ) ) ;
#5726=DIRECTION ( 'NONE',  ( 0.000000000000000000, 0.5000000000000011102, -0.8660254037844381525 ) ) ;
#5727=DIRECTION ( 'NONE',  ( 0.000000000000000000, -0.8090169943749526693, 0.5877852522924661427 ) ) ;
#5728=MECHANICAL_DESIGN_GEOMETRIC_PRESENTATION_REPRESENTATION('',(#8851),#431);
#5729=EDGE_LOOP ( 'NONE', ( #1817, #11958, #5440, #8358 ) ) ;
#5730=CARTESIAN_POINT ( 'NONE',  ( -10.00000000000000000, 0.000000000000000000, 0.000000000000000000 ) ) ;
#5731=ORIENTED_EDGE ( 'NONE', *, *, #10793, .F. ) ;
#5732=CARTESIAN_POINT ( 'NONE',  ( 3.000000000000000888, -12.88318129270191825, 18.51065745848373822 ) ) ;
#5734=EDGE_CURVE ( 'NONE', #2005, #1648, #10622, .T. ) ;
#5735=AXIS2_PLACEMENT_3D ( 'NONE', #8465, #3807, #482 ) ;
#5738=CIRCLE ( 'NONE', #7490, 9.599999999999997868 ) ;
#5742=ORIENTED_EDGE ( 'NONE', *, *, #7867, .T. ) ;
#5744=CIRCLE ( 'NONE', #9647, 9.599999999999996092 ) ;
#5745=ORIENTED_EDGE ( 'NONE', *, *, #9824, .T. ) ;
#5746=VERTEX_POINT ( 'NONE', #8442 ) ;
#5747=CARTESIAN_POINT ( 'NONE',  ( 0.000000000000000000, -8.645255683528846546, -23.24434456306333985 ) ) ;
#5748=CARTESIAN_POINT ( 'NONE',  ( 3.000000000000000888, 21.96011696265491153, -5.135568396240103084 ) ) ;
#5749=EDGE_LOOP ( 'NONE', ( #9483, #9538, #1046, #11051 ) ) ;
#5750=FACE_OUTER_BOUND ( 'NONE', #4750, .T. ) ;
#5752=CARTESIAN_POINT ( 'NONE',  ( 0.000000000000000000, 0.000000000000000000, 0.000000000000000000 ) ) ;
#5754=CARTESIAN_POINT ( 'NONE',  ( 0.000000000000000000, 0.000000000000000000, 0.000000000000000000 ) ) ;
#5755=ORIENTED_EDGE ( 'NONE', *, *, #11999, .T. ) ;
#5756=ORIENTED_EDGE ( 'NONE', *, *, #851, .T. ) ;
#5758=ORIENTED_EDGE ( 'NONE', *, *, #11915, .F. ) ;
#5761=EDGE_LOOP ( 'NONE', ( #10491, #2107, #11106, #9941 ) ) ;
#5764=CARTESIAN_POINT ( 'NONE',  ( 0.000000000000000000, 0.3433949777331667397, 22.99643626497956816 ) ) ;
#5766=AXIS2_PLACEMENT_3D ( 'NONE', #4000, #7726, #2841 ) ;
#5767=EDGE_CURVE ( 'NONE', #11802, #9240, #6532, .T. ) ;
#5768=CARTESIAN_POINT ( 'NONE',  ( 3.000000000000000888, 7.402892494506579268, -21.30300407174355115 ) ) ;
#5769=FACE_OUTER_BOUND ( 'NONE', #11568, .T. ) ;
#5770=ORIENTED_EDGE ( 'NONE', *, *, #11476, .T. ) ;
#5771=EDGE_LOOP ( 'NONE', ( #7967, #8725, #4899, #11416 ) ) ;
#5772=LINE ( 'NONE', #4788, #5489 ) ;
#5773=VERTEX_POINT ( 'NONE', #10137 ) ;
#5774=EDGE_CURVE ( 'NONE', #3600, #11784, #5541, .T. ) ;
#5776=ADVANCED_FACE ( 'NONE', ( #848 ), #4583, .T. ) ;
#5777=DIRECTION ( 'NONE',  ( -1.000000000000000000, -0.000000000000000000, 0.000000000000000000 ) ) ;
#5780=FACE_OUTER_BOUND ( 'NONE', #10870, .T. ) ;
#5781=CARTESIAN_POINT ( 'NONE',  ( 3.000000000000000888, -9.589108953448036488, 20.41249101028208202 ) ) ;
#5783=CARTESIAN_POINT ( 'NONE',  ( 0.000000000000000000, -4.240409074144249502, 22.15038895030647836 ) ) ;
#5785=CARTESIAN_POINT ( 'NONE',  ( 3.000000000000000888, 2.811977935937781670, 22.37663021667345120 ) ) ;
#5787=CIRCLE ( 'NONE', #5190, 9.599999999999999645 ) ;
#5788=DIRECTION ( 'NONE',  ( -1.000000000000000000, -0.000000000000000000, 0.000000000000000000 ) ) ;
#5789=VERTEX_POINT ( 'NONE', #2807 ) ;
#5790=DIRECTION ( 'NONE',  ( 0.000000000000000000, 0.9510565162951543083, -0.3090169943749450643 ) ) ;
#5792=CARTESIAN_POINT ( 'NONE',  ( 0.000000000000000000, 0.000000000000000000, 0.000000000000000000 ) ) ;
#5793=VECTOR ( 'NONE', #2695, 1000.000000000000000 ) ;
#5796=DIRECTION ( 'NONE',  ( -1.000000000000000000, 0.000000000000000000, 0.000000000000000000 ) ) ;
#5797=ORIENTED_EDGE ( 'NONE', *, *, #8678, .F. ) ;
#5798=EDGE_CURVE ( 'NONE', #7882, #7859, #10266, .T. ) ;
#5799=AXIS2_PLACEMENT_3D ( 'NONE', #2826, #10282, #11268 ) ;
#5800=ORIENTED_EDGE ( 'NONE', *, *, #8268, .F. ) ;
#5801=CARTESIAN_POINT ( 'NONE',  ( 3.000000000000000888, 0.000000000000000000, 0.000000000000000000 ) ) ;
#5802=DIRECTION ( 'NONE',  ( -1.000000000000000000, -0.000000000000000000, 0.000000000000000000 ) ) ;
#5803=EDGE_LOOP ( 'NONE', ( #9732, #8793, #2145, #8999 ) ) ;
#5804=CARTESIAN_POINT ( 'NONE',  ( 0.000000000000000000, 0.000000000000000000, 0.000000000000000000 ) ) ;
#5806=ADVANCED_FACE ( 'NONE', ( #7565 ), #2676, .T. ) ;
#5807=DIRECTION ( 'NONE',  ( 0.000000000000000000, 0.000000000000000000, 1.000000000000000000 ) ) ;
#5809=CYLINDRICAL_SURFACE ( 'NONE', #4099, 22.99899999999999878 ) ;
#5810=ORIENTED_EDGE ( 'NONE', *, *, #1903, .F. ) ;
#5811=VERTEX_POINT ( 'NONE', #152 ) ;
#5815=DIRECTION ( 'NONE',  ( 0.000000000000000000, -0.3090169943749349613, -0.9510565162951576390 ) ) ;
#5816=CARTESIAN_POINT ( 'NONE',  ( 3.000000000000000888, 16.85990652506920995, -15.64281154287580655 ) ) ;
#5817=LINE ( 'NONE', #3675, #5403 ) ;
#5818=VERTEX_POINT ( 'NONE', #12093 ) ;
#5819=CARTESIAN_POINT ( 'NONE',  ( 3.000000000000000000, 0.000000000000000000, 18.49999999999999645 ) ) ;
#5820=DIRECTION ( 'NONE',  ( 0.000000000000000000, 0.000000000000000000, 1.000000000000000000 ) ) ;
#5822=AXIS2_PLACEMENT_3D ( 'NONE', #10550, #8424, #6756 ) ;
#5823=FACE_OUTER_BOUND ( 'NONE', #8440, .T. ) ;
#5824=ORIENTED_EDGE ( 'NONE', *, *, #4258, .T. ) ;
#5825=DIRECTION ( 'NONE',  ( 0.000000000000000000, 0.000000000000000000, 1.000000000000000000 ) ) ;
#5826=VECTOR ( 'NONE', #8532, 1000.000000000000000 ) ;
#5827=ORIENTED_EDGE ( 'NONE', *, *, #3972, .T. ) ;
#5828=VERTEX_POINT ( 'NONE', #11250 ) ;
#5829=CARTESIAN_POINT ( 'NONE',  ( 3.000000000000000888, -22.90635393027944744, -2.062268319295799568 ) ) ;
#5830=ORIENTED_EDGE ( 'NONE', *, *, #7268, .T. ) ;
#5832=EDGE_CURVE ( 'NONE', #622, #8206, #2740, .T. ) ;
#5833=DIRECTION ( 'NONE',  ( -1.000000000000000000, 0.000000000000000000, -0.000000000000000000 ) ) ;
#5836=DIRECTION ( 'NONE',  ( 0.000000000000000000, 0.000000000000000000, 1.000000000000000000 ) ) ;
#5837=DIRECTION ( 'NONE',  ( -1.000000000000000000, -0.000000000000000000, -0.000000000000000000 ) ) ;
#5839=CARTESIAN_POINT ( 'NONE',  ( 0.000000000000000000, 0.000000000000000000, 0.000000000000000000 ) ) ;
#5841=EDGE_CURVE ( 'NONE', #4846, #7440, #5738, .T. ) ;
#5842=DIRECTION ( 'NONE',  ( -1.000000000000000000, -0.000000000000000000, -0.000000000000000000 ) ) ;
#5843=EDGE_CURVE ( 'NONE', #10367, #1329, #1821, .T. ) ;
#5844=CARTESIAN_POINT ( 'NONE',  ( 1.499999999999999556, 11.02759168516775290, -22.21333432029552668 ) ) ;
#5845=AXIS2_PLACEMENT_3D ( 'NONE', #2669, #895, #8302 ) ;
#5847=ORIENTED_EDGE ( 'NONE', *, *, #6292, .T. ) ;
#5848=VERTEX_POINT ( 'NONE', #5747 ) ;
#5849=CARTESIAN_POINT ( 'NONE',  ( 3.000000000000000888, -21.30300407174367905, 7.402892494506218668 ) ) ;
#5851=LINE ( 'NONE', #6700, #362 ) ;
#5853=EDGE_CURVE ( 'NONE', #5055, #11545, #8502, .T. ) ;
#5855=CYLINDRICAL_SURFACE ( 'NONE', #9769, 9.599999999999997868 ) ;
#5856=VERTEX_POINT ( 'NONE', #906 ) ;
#5858=AXIS2_PLACEMENT_3D ( 'NONE', #10943, #1519, #10021 ) ;
#5859=CARTESIAN_POINT ( 'NONE',  ( 0.000000000000000000, 23.24434456306337538, -8.645255683528764834 ) ) ;
#5860=EDGE_CURVE ( 'NONE', #4143, #5993, #4563, .T. ) ;
#5861=CARTESIAN_POINT ( 'NONE',  ( 3.000000000000000888, -21.14796121233203152, 9.039786367038763260 ) ) ;
#5862=DIRECTION ( 'NONE',  ( -1.000000000000000000, -0.000000000000000000, -0.000000000000000000 ) ) ;
#5863=CARTESIAN_POINT ( 'NONE',  ( -10.00000000000000000, 0.000000000000000000, 0.000000000000000000 ) ) ;
#5864=ADVANCED_FACE ( 'NONE', ( #4820 ), #963, .T. ) ;
#5866=EDGE_CURVE ( 'NONE', #5789, #8927, #4749, .T. ) ;
#5867=CIRCLE ( 'NONE', #7021, 24.80000000000000071 ) ;
#5868=DIRECTION ( 'NONE',  ( 0.000000000000000000, 0.5877852522924690293, 0.8090169943749504489 ) ) ;
#5869=ORIENTED_EDGE ( 'NONE', *, *, #6882, .T. ) ;
#5873=EDGE_CURVE ( 'NONE', #5271, #3286, #6853, .T. ) ;
#5874=ORIENTED_EDGE ( 'NONE', *, *, #10061, .F. ) ;
#5875=CARTESIAN_POINT ( 'NONE',  ( 3.000000000000000888, 6.668524164681629784, 23.88662356770117867 ) ) ;
#5877=FACE_OUTER_BOUND ( 'NONE', #5761, .T. ) ;
#5878=ORIENTED_EDGE ( 'NONE', *, *, #8983, .F. ) ;
#5879=VECTOR ( 'NONE', #9559, 1000.000000000000000 ) ;
#5880=DIRECTION ( 'NONE',  ( 0.000000000000000000, -0.8090169943749525583, 0.5877852522924661427 ) ) ;
#5882=DIRECTION ( 'NONE',  ( -1.000000000000000000, 0.000000000000000000, -0.000000000000000000 ) ) ;
#5884=ORIENTED_EDGE ( 'NONE', *, *, #10915, .F. ) ;
#5885=CYLINDRICAL_SURFACE ( 'NONE', #6278, 9.599999999999997868 ) ;
#5886=AXIS2_PLACEMENT_3D ( 'NONE', #10201, #7437, #959 ) ;
#5888=CARTESIAN_POINT ( 'NONE',  ( 3.000000000000000888, -18.80635025205160815, -13.23915371906974592 ) ) ;
#5889=AXIS2_PLACEMENT_3D ( 'NONE', #11749, #6246, #3437 ) ;
#5890=ORIENTED_EDGE ( 'NONE', *, *, #1621, .T. ) ;
#5892=DIRECTION ( 'NONE',  ( -1.000000000000000000, 0.000000000000000000, -0.000000000000000000 ) ) ;
#5893=DIRECTION ( 'NONE',  ( 0.000000000000000000, 1.000000000000000000, 3.491481338843133355E-15 ) ) ;
#5894=VECTOR ( 'NONE', #5375, 1000.000000000000000 ) ;
#5895=AXIS2_PLACEMENT_3D ( 'NONE', #5437, #9167, #785 ) ;
#5896=CARTESIAN_POINT ( 'NONE',  ( 0.000000000000000000, 4.240409074144393387, -22.15038895030644639 ) ) ;
#5898=AXIS2_PLACEMENT_3D ( 'NONE', #6034, #8618, #463 ) ;
#5899=CARTESIAN_POINT ( 'NONE',  ( 3.000000000000000888, -11.02759168516730881, -22.21333432029575050 ) ) ;
#5902=DIRECTION ( 'NONE',  ( -1.000000000000000000, 0.000000000000000000, -0.000000000000000000 ) ) ;
#5906=ORIENTED_EDGE ( 'NONE', *, *, #8689, .F. ) ;
#5907=DIRECTION ( 'NONE',  ( 0.000000000000000000, 0.6691306063588543518, 0.7431448254773976858 ) ) ;
#5909=DIRECTION ( 'NONE',  ( 1.000000000000000000, 0.000000000000000000, 0.000000000000000000 ) ) ;
#5910=ADVANCED_FACE ( 'NONE', ( #4080 ), #566, .T. ) ;
#5911=ADVANCED_FACE ( 'NONE', ( #4879 ), #8738, .T. ) ;
#5915=AXIS2_PLACEMENT_3D ( 'NONE', #7260, #2444, #7081 ) ;
#5920=VERTEX_POINT ( 'NONE', #8795 ) ;
#5922=CARTESIAN_POINT ( 'NONE',  ( 0.000000000000000000, 21.96011696265484403, 5.135568396240393518 ) ) ;
#5923=DIRECTION ( 'NONE',  ( -1.000000000000000000, 0.000000000000000000, 0.000000000000000000 ) ) ;
#5924=EDGE_CURVE ( 'NONE', #10265, #2252, #10502, .T. ) ;
#5925=CARTESIAN_POINT ( 'NONE',  ( 3.000000000000000888, 9.589108953447894379, 20.41249101028215307 ) ) ;
#5926=AXIS2_PLACEMENT_3D ( 'NONE', #10183, #11232, #11102 ) ;
#5929=AXIS2_PLACEMENT_3D ( 'NONE', #6055, #5998, #357 ) ;
#5931=ORIENTED_EDGE ( 'NONE', *, *, #10093, .F. ) ;
#5932=VECTOR ( 'NONE', #6411, 1000.000000000000000 ) ;
#5933=VERTEX_POINT ( 'NONE', #11546 ) ;
#5934=AXIS2_PLACEMENT_3D ( 'NONE', #5632, #6548, #11386 ) ;
#5939=FACE_OUTER_BOUND ( 'NONE', #7029, .T. ) ;
#5940=CARTESIAN_POINT ( 'NONE',  ( 3.000000000000000888, -13.79477846460808799, 18.40266524480583854 ) ) ;
#5941=CIRCLE ( 'NONE', #5357, 24.80000000000000071 ) ;
#5942=LINE ( 'NONE', #9668, #8922 ) ;
#5943=ORIENTED_EDGE ( 'NONE', *, *, #10443, .T. ) ;
#5945=CARTESIAN_POINT ( 'NONE',  ( 0.000000000000000000, 13.62355943574019435, 17.97274125076078732 ) ) ;
#5947=ORIENTED_EDGE ( 'NONE', *, *, #3605, .T. ) ;
#5948=CARTESIAN_POINT ( 'NONE',  ( 3.000000000000000888, -22.21333432029571142, 11.02759168516737276 ) ) ;
#5949=DIRECTION ( 'NONE',  ( -1.000000000000000000, -0.000000000000000000, -0.000000000000000000 ) ) ;
#5950=ORIENTED_EDGE ( 'NONE', *, *, #6577, .F. ) ;
#5951=EDGE_CURVE ( 'NONE', #474, #7150, #5330, .T. ) ;
#5953=CARTESIAN_POINT ( 'NONE',  ( 3.000000000000000888, -11.67026512804560134, 19.29833442572355651 ) ) ;
#5954=ORIENTED_EDGE ( 'NONE', *, *, #1050, .F. ) ;
#5955=VECTOR ( 'NONE', #8480, 1000.000000000000000 ) ;
#5956=DIRECTION ( 'NONE',  ( -1.000000000000000000, 0.000000000000000000, 0.000000000000000000 ) ) ;
#5957=EDGE_CURVE ( 'NONE', #8820, #2346, #1618, .T. ) ;
#5958=DIRECTION ( 'NONE',  ( -1.000000000000000000, 0.000000000000000000, -0.000000000000000000 ) ) ;
#5960=( LENGTH_UNIT ( ) NAMED_UNIT ( * ) SI_UNIT ( .MILLI., .METRE. ) );
#5962=DIRECTION ( 'NONE',  ( -1.000000000000000000, -0.000000000000000000, -0.000000000000000000 ) ) ;
#5963=DIRECTION ( 'NONE',  ( 1.000000000000000000, 0.000000000000000000, 0.000000000000000000 ) ) ;
#5964=ORIENTED_EDGE ( 'NONE', *, *, #6830, .F. ) ;
#5965=VERTEX_POINT ( 'NONE', #5859 ) ;
#5966=ORIENTED_EDGE ( 'NONE', *, *, #10256, .F. ) ;
#5968=CARTESIAN_POINT ( 'NONE',  ( 0.000000000000000000, -10.87771529938148518, -19.75591328264897228 ) ) ;
#5969=FACE_OUTER_BOUND ( 'NONE', #3359, .T. ) ;
#5973=CARTESIAN_POINT ( 'NONE',  ( 0.000000000000000000, 2.062268319295869734, -22.90635393027944389 ) ) ;
#5974=CARTESIAN_POINT ( 'NONE',  ( 1.500000000000000444, 8.645255683529011748, 23.24434456306327945 ) ) ;
#5975=ORIENTED_EDGE ( 'NONE', *, *, #11334, .T. ) ;
#5976=VERTEX_POINT ( 'NONE', #11769 ) ;
#5977=ORIENTED_EDGE ( 'NONE', *, *, #4678, .T. ) ;
#5978=CARTESIAN_POINT ( 'NONE',  ( 3.000000000000000888, -22.47229024614978599, 1.901833551798177036 ) ) ;
#5979=CIRCLE ( 'NONE', #3240, 9.599999999999996092 ) ;
#5980=DIRECTION ( 'NONE',  ( -1.000000000000000000, 0.000000000000000000, -0.000000000000000000 ) ) ;
#5981=EDGE_CURVE ( 'NONE', #9480, #8232, #7748, .T. ) ;
#5982=LINE ( 'NONE', #9766, #2313 ) ;
#5983=DIRECTION ( 'NONE',  ( -1.000000000000000000, 0.000000000000000000, 0.000000000000000000 ) ) ;
#5985=ADVANCED_FACE ( 'NONE', ( #5056 ), #10563, .T. ) ;
#5986=CIRCLE ( 'NONE', #5799, 22.99899999999999878 ) ;
#5987=EDGE_CURVE ( 'NONE', #4735, #11471, #7065, .T. ) ;
#5989=ORIENTED_EDGE ( 'NONE', *, *, #4255, .T. ) ;
#5991=EDGE_CURVE ( 'NONE', #11333, #5773, #634, .T. ) ;
#5993=VERTEX_POINT ( 'NONE', #6888 ) ;
#5994=DIRECTION ( 'NONE',  ( -1.000000000000000000, 0.000000000000000000, 0.000000000000000000 ) ) ;
#5995=DIRECTION ( 'NONE',  ( 0.000000000000000000, -0.9945218953682721796, -0.1045284632676635739 ) ) ;
#5996=CYLINDRICAL_SURFACE ( 'NONE', #9505, 22.99899999999999878 ) ;
#5997=ORIENTED_EDGE ( 'NONE', *, *, #5174, .T. ) ;
#5998=DIRECTION ( 'NONE',  ( -1.000000000000000000, -0.000000000000000000, -0.000000000000000000 ) ) ;
#5999=LINE ( 'NONE', #8704, #5717 ) ;
#6002=ORIENTED_EDGE ( 'NONE', *, *, #5987, .T. ) ;
#6003=DIRECTION ( 'NONE',  ( 1.000000000000000000, 0.000000000000000000, -0.000000000000000000 ) ) ;
#6004=DIRECTION ( 'NONE',  ( -1.000000000000000000, 0.000000000000000000, -0.000000000000000000 ) ) ;
#6005=ORIENTED_EDGE ( 'NONE', *, *, #1168, .F. ) ;
#6007=EDGE_CURVE ( 'NONE', #9404, #6354, #3265, .T. ) ;
#6008=CARTESIAN_POINT ( 'NONE',  ( 3.000000000000000888, 0.000000000000000000, 0.000000000000000000 ) ) ;
#6010=DIRECTION ( 'NONE',  ( -1.000000000000000000, 0.000000000000000000, 0.000000000000000000 ) ) ;
#6011=DIRECTION ( 'NONE',  ( 0.000000000000000000, 0.5877852522924690293, 0.8090169943749505599 ) ) ;
#6013=EDGE_CURVE ( 'NONE', #1910, #2001, #7361, .T. ) ;
#6014=CIRCLE ( 'NONE', #11507, 9.599999999999996092 ) ;
#6015=DIRECTION ( 'NONE',  ( 0.000000000000000000, 0.2079116908177597312, -0.9781476007338056888 ) ) ;
#6017=CYLINDRICAL_SURFACE ( 'NONE', #8811, 24.80000000000000071 ) ;
#6019=CARTESIAN_POINT ( 'NONE',  ( 0.000000000000000000, 6.532525787310969001, 21.58580335785678983 ) ) ;
#6020=ORIENTED_EDGE ( 'NONE', *, *, #9243, .F. ) ;
#6021=ORIENTED_EDGE ( 'NONE', *, *, #170, .T. ) ;
#6022=ADVANCED_FACE ( 'NONE', ( #9928 ), #8617, .T. ) ;
#6024=DIRECTION ( 'NONE',  ( 0.000000000000000000, 0.000000000000000000, 1.000000000000000000 ) ) ;
#6025=CARTESIAN_POINT ( 'NONE',  ( 0.000000000000000000, 22.37663021667344054, -2.811977935937859385 ) ) ;
#6026=DIRECTION ( 'NONE',  ( 0.000000000000000000, -0.9945218953682744001, 0.1045284632676437564 ) ) ;
#6029=CARTESIAN_POINT ( 'NONE',  ( 3.000000000000000888, 20.08719549084880640, -11.20082935824054182 ) ) ;
#6030=ORIENTED_EDGE ( 'NONE', *, *, #2461, .F. ) ;
#6031=VECTOR ( 'NONE', #11180, 1000.000000000000000 ) ;
#6032=ORIENTED_EDGE ( 'NONE', *, *, #2795, .F. ) ;
#6033=ORIENTED_EDGE ( 'NONE', *, *, #9609, .F. ) ;
#6034=CARTESIAN_POINT ( 'NONE',  ( 0.000000000000000000, -22.37663021667341923, -2.811977935938010376 ) ) ;
#6035=CIRCLE ( 'NONE', #360, 9.599999999999997868 ) ;
#6037=CARTESIAN_POINT ( 'NONE',  ( 1.499999999999999556, -4.135161237383400135, -24.45282072769605364 ) ) ;
#6038=DIRECTION ( 'NONE',  ( 0.000000000000000000, 0.000000000000000000, 1.000000000000000000 ) ) ;
#6040=CARTESIAN_POINT ( 'NONE',  ( 3.000000000000000888, 0.000000000000000000, 0.000000000000000000 ) ) ;
#6041=AXIS2_PLACEMENT_3D ( 'NONE', #7195, #9905, #11064 ) ;
#6042=CYLINDRICAL_SURFACE ( 'NONE', #6444, 24.80000000000000071 ) ;
#6043=AXIS2_PLACEMENT_3D ( 'NONE', #966, #5862, #2006 ) ;
#6045=ORIENTED_EDGE ( 'NONE', *, *, #7918, .F. ) ;
#6048=AXIS2_PLACEMENT_3D ( 'NONE', #9420, #8452, #2934 ) ;
#6049=ORIENTED_EDGE ( 'NONE', *, *, #5534, .F. ) ;
#6050=CARTESIAN_POINT ( 'NONE',  ( 3.000000000000000888, 15.42759117534407309, -16.45023496161649845 ) ) ;
#6051=DIRECTION ( 'NONE',  ( 0.000000000000000000, 0.000000000000000000, 1.000000000000000000 ) ) ;
#6052=CARTESIAN_POINT ( 'NONE',  ( 3.000000000000000888, 11.02759168516775112, -22.21333432029552668 ) ) ;
#6053=ORIENTED_EDGE ( 'NONE', *, *, #8983, .T. ) ;
#6055=CARTESIAN_POINT ( 'NONE',  ( 3.000000000000000888, 0.000000000000000000, 0.000000000000000000 ) ) ;
#6056=ADVANCED_FACE ( 'NONE', ( #3048 ), #2986, .T. ) ;
#6057=CIRCLE ( 'NONE', #776, 24.80000000000000071 ) ;
#6058=CYLINDRICAL_SURFACE ( 'NONE', #7062, 22.99899999999999878 ) ;
#6061=CARTESIAN_POINT ( 'NONE',  ( 0.000000000000000000, -9.589108953448036488, 20.41249101028208202 ) ) ;
#6062=ORIENTED_EDGE ( 'NONE', *, *, #11744, .T. ) ;
#6063=CARTESIAN_POINT ( 'NONE',  ( 3.000000000000000888, 0.000000000000000000, 0.000000000000000000 ) ) ;
#6064=AXIS2_PLACEMENT_3D ( 'NONE', #11049, #1985, #7359 ) ;
#6065=ORIENTED_EDGE ( 'NONE', *, *, #9457, .F. ) ;
#6068=ORIENTED_EDGE ( 'NONE', *, *, #11459, .F. ) ;
#6069=DIRECTION ( 'NONE',  ( -1.000000000000000000, 0.000000000000000000, 0.000000000000000000 ) ) ;
#6070=VERTEX_POINT ( 'NONE', #4930 ) ;
#6071=CARTESIAN_POINT ( 'NONE',  ( -10.00000000000000000, 0.000000000000000000, 0.000000000000000000 ) ) ;
#6072=DIRECTION ( 'NONE',  ( -1.000000000000000000, -0.000000000000000000, 0.000000000000000000 ) ) ;
#6074=AXIS2_PLACEMENT_3D ( 'NONE', #10971, #8096, #2341 ) ;
#6075=CARTESIAN_POINT ( 'NONE',  ( 3.000000000000000888, 19.74380051311539930, 11.79560690673879186 ) ) ;
#6076=CIRCLE ( 'NONE', #2357, 24.80000000000000071 ) ;
#6078=AXIS2_PLACEMENT_3D ( 'NONE', #8455, #53, #3801 ) ;
#6079=LINE ( 'NONE', #629, #3139 ) ;
#6081=CARTESIAN_POINT ( 'NONE',  ( 3.000000000000000888, 24.75110766671652129, 1.556492618230723046 ) ) ;
#6082=EDGE_LOOP ( 'NONE', ( #10275, #4625, #2583, #919 ) ) ;
#6083=ADVANCED_FACE ( 'NONE', ( #7553 ), #5663, .T. ) ;
#6085=CARTESIAN_POINT ( 'NONE',  ( 0.000000000000000000, 24.75110766671652129, 1.556492618230723046 ) ) ;
#6086=ORIENTED_EDGE ( 'NONE', *, *, #7020, .T. ) ;
#6087=CIRCLE ( 'NONE', #6078, 22.99899999999999523 ) ;
#6088=AXIS2_PLACEMENT_3D ( 'NONE', #6890, #5980, #7930 ) ;
#6090=FACE_OUTER_BOUND ( 'NONE', #10844, .T. ) ;
#6093=CYLINDRICAL_SURFACE ( 'NONE', #1990, 22.99899999999999878 ) ;
#6094=AXIS2_PLACEMENT_3D ( 'NONE', #3637, #2655, #2715 ) ;
#6095=DIRECTION ( 'NONE',  ( 0.000000000000000000, 0.000000000000000000, 1.000000000000000000 ) ) ;
#6096=VERTEX_POINT ( 'NONE', #7495 ) ;
#6097=ORIENTED_EDGE ( 'NONE', *, *, #10200, .T. ) ;
#6098=ORIENTED_EDGE ( 'NONE', *, *, #837, .T. ) ;
#6099=ADVANCED_FACE ( 'NONE', ( #201 ), #1927, .T. ) ;
#6100=DIRECTION ( 'NONE',  ( 0.000000000000000000, 0.8090169943749445647, 0.5877852522924771339 ) ) ;
#6102=AXIS2_PLACEMENT_3D ( 'NONE', #6241, #3369, #10834 ) ;
#6103=CARTESIAN_POINT ( 'NONE',  ( 3.000000000000000888, 5.117118920208487687, 22.42251312757881365 ) ) ;
#6104=CARTESIAN_POINT ( 'NONE',  ( 3.000000000000000888, -11.02759168516760369, 22.21333432029560484 ) ) ;
#6107=DIRECTION ( 'NONE',  ( 1.000000000000000000, 0.000000000000000000, 0.000000000000000000 ) ) ;
#6108=LINE ( 'NONE', #11555, #8797 ) ;
#6109=EDGE_LOOP ( 'NONE', ( #980, #1675, #10154, #3770 ) ) ;
#6111=ORIENTED_EDGE ( 'NONE', *, *, #7915, .T. ) ;
#6114=ORIENTED_EDGE ( 'NONE', *, *, #3559, .T. ) ;
#6115=DIRECTION ( 'NONE',  ( 0.000000000000000000, 0.000000000000000000, 1.000000000000000000 ) ) ;
#6117=CARTESIAN_POINT ( 'NONE',  ( 0.000000000000000000, 21.76479567747252020, -7.432877647174977120 ) ) ;
#6118=CARTESIAN_POINT ( 'NONE',  ( 3.000000000000000888, 0.000000000000000000, 0.000000000000000000 ) ) ;
#6119=EDGE_LOOP ( 'NONE', ( #10049, #5116, #867, #11036, #4200, #2228, #9790, #8692, #728, #6228, #1535, #11826, #9854, #9124, #11247, #660, #8525, #12020, #8064, #2663, #1771, #2696, #9172, #717, #10472, #5443, #10032, #7332, #7180, #6409, #6163, #11270, #615, #7306, #1926, #11850, #10190, #6647, #7078, #10771, #8878, #6136, #4701, #11262, #4773, #6938, #5455, #9104, #11881, #7297, #3716, #4, #2753, #2641, #2593, #8156, #10650, #4844, #12110, #4379, #3843, #7947, #10711, #8868, #487, #9332, #10202, #2649, #7190, #3704, #9225, #8371, #6572, #11172, #12109, #981, #7374, #5163, #3828, #4064, #5040, #492, #8723, #9454, #4160, #4028, #8262, #2116, #5508, #10276, #3668, #1060, #196, #8764, #9343, #10401, #4465, #10250, #8313, #3974, #1158, #5966, #2469, #3008, #5758, #10501, #9429, #10695, #5396, #8327, #461, #8266, #8308, #7564, #1184, #9085, #10589, #1368, #6049, #2863, #1658, #5731, #2818, #298, #4974, #3045, #11399, #8038, #2421, #382, #1443, #580, #10469, #2128, #4330, #7396, #2409, #9622, #3813, #2582, #11529, #6794, #7747, #2768, #6218, #2713, #9016, #410, #3919, #4201, #11656, #3961, #7615, #1222, #8941, #3990, #11658, #10454, #3381, #2449, #6775, #9003, #4552, #8760, #415, #11349, #5280, #3179, #7408, #6033, #11436, #11330, #1400, #6030, #4228, #3025, #5087, #6202, #1289, #9320, #12114, #168, #7551, #4178, #864, #2482, #5369, #2803, #4302, #7442, #4008, #7939, #2436, #5693, #744, #11075, #1597, #12035, #7474, #5448, #6739, #1710, #8544, #4772, #2821, #10946, #9053, #889, #1203, #5884, #2876, #11795, #4531, #9342, #4635, #3799, #9468, #3587, #3769, #10306, #1075, #10223, #8472, #6557, #9513, #5615, #7657, #6485, #1318, #1937, #9024, #5673, #10404, #6482, #775, #7563, #5446, #7164, #8387, #4764, #946, #11444, #150, #1266, #6971 ) ) ;
#6120=AXIS2_PLACEMENT_3D ( 'NONE', #7948, #3986, #4039 ) ;
#6121=DIRECTION ( 'NONE',  ( 1.000000000000000000, 0.000000000000000000, 0.000000000000000000 ) ) ;
#6124=CIRCLE ( 'NONE', #651, 9.599999999999996092 ) ;
#6126=VERTEX_POINT ( 'NONE', #2053 ) ;
#6127=DIRECTION ( 'NONE',  ( 0.000000000000000000, 0.000000000000000000, -1.000000000000000000 ) ) ;
#6128=CARTESIAN_POINT ( 'NONE',  ( 3.000000000000000888, 7.432877647175492264, -21.76479567747234256 ) ) ;
#6129=ORIENTED_EDGE ( 'NONE', *, *, #114, .T. ) ;
#6130=AXIS2_PLACEMENT_3D ( 'NONE', #9352, #3850, #10213 ) ;
#6131=EDGE_CURVE ( 'NONE', #6372, #3187, #7369, .T. ) ;
#6133=ORIENTED_EDGE ( 'NONE', *, *, #4714, .T. ) ;
#6134=CYLINDRICAL_SURFACE ( 'NONE', #1485, 22.99899999999999878 ) ;
#6135=DIRECTION ( 'NONE',  ( -1.000000000000000000, 0.000000000000000000, -0.000000000000000000 ) ) ;
#6136=ORIENTED_EDGE ( 'NONE', *, *, #6131, .F. ) ;
#6137=EDGE_CURVE ( 'NONE', #3516, #411, #3038, .T. ) ;
#6139=DIRECTION ( 'NONE',  ( 0.000000000000000000, 0.000000000000000000, 1.000000000000000000 ) ) ;
#6142=FACE_OUTER_BOUND ( 'NONE', #200, .T. ) ;
#6144=EDGE_CURVE ( 'NONE', #3273, #994, #6500, .T. ) ;
#6145=DIRECTION ( 'NONE',  ( -1.000000000000000000, -0.000000000000000000, 0.000000000000000000 ) ) ;
#6146=DIRECTION ( 'NONE',  ( 0.000000000000000000, 0.000000000000000000, 1.000000000000000000 ) ) ;
#6147=EDGE_CURVE ( 'NONE', #411, #9318, #8685, .T. ) ;
#6149=EDGE_CURVE ( 'NONE', #308, #1864, #10214, .T. ) ;
#6151=CIRCLE ( 'NONE', #10252, 9.599999999999997868 ) ;
#6152=DIRECTION ( 'NONE',  ( 0.000000000000000000, 0.000000000000000000, 1.000000000000000000 ) ) ;
#6153=VERTEX_POINT ( 'NONE', #4011 ) ;
#6154=LINE ( 'NONE', #388, #2518 ) ;
#6155=CARTESIAN_POINT ( 'NONE',  ( 3.000000000000000888, -22.54798042742717357, -0.4575788569254196636 ) ) ;
#6156=CARTESIAN_POINT ( 'NONE',  ( 1.499999999999999556, -22.21333432029556576, -11.02759168516767296 ) ) ;
#6158=CARTESIAN_POINT ( 'NONE',  ( 0.000000000000000000, 24.02068490260612776, 6.168200451485839508 ) ) ;
#6159=CIRCLE ( 'NONE', #3428, 9.599999999999996092 ) ;
#6160=CARTESIAN_POINT ( 'NONE',  ( 1.500000000000000444, 15.80756504416717334, -19.10918332567941036 ) ) ;
#6161=ORIENTED_EDGE ( 'NONE', *, *, #1738, .T. ) ;
#6163=ORIENTED_EDGE ( 'NONE', *, *, #7152, .F. ) ;
#6165=DIRECTION ( 'NONE',  ( -1.000000000000000000, -0.000000000000000000, 0.000000000000000000 ) ) ;
#6166=DIRECTION ( 'NONE',  ( -1.000000000000000000, -0.000000000000000000, -0.000000000000000000 ) ) ;
#6168=EDGE_CURVE ( 'NONE', #10871, #474, #5526, .T. ) ;
#6169=DIRECTION ( 'NONE',  ( 0.000000000000000000, 0.6691306063588594588, -0.7431448254773932449 ) ) ;
#6170=DIRECTION ( 'NONE',  ( 1.000000000000000000, -0.000000000000000000, -0.000000000000000000 ) ) ;
#6171=ORIENTED_EDGE ( 'NONE', *, *, #7697, .F. ) ;
#6172=ORIENTED_EDGE ( 'NONE', *, *, #2996, .F. ) ;
#6173=AXIS2_PLACEMENT_3D ( 'NONE', #7539, #4914, #1116 ) ;
#6177=DIRECTION ( 'NONE',  ( 0.000000000000000000, -0.8660254037844432595, 0.4999999999999919509 ) ) ;
#6179=EDGE_CURVE ( 'NONE', #2929, #8071, #10935, .T. ) ;
#6180=DIRECTION ( 'NONE',  ( 0.000000000000000000, 0.000000000000000000, 1.000000000000000000 ) ) ;
#6181=EDGE_LOOP ( 'NONE', ( #2823, #11437, #4891, #7519 ) ) ;
#6182=CYLINDRICAL_SURFACE ( 'NONE', #4567, 9.599999999999997868 ) ;
#6183=VECTOR ( 'NONE', #5892, 1000.000000000000000 ) ;
#6186=DIRECTION ( 'NONE',  ( -1.000000000000000000, 0.000000000000000000, 0.000000000000000000 ) ) ;
#6187=ORIENTED_EDGE ( 'NONE', *, *, #9356, .F. ) ;
#6188=DIRECTION ( 'NONE',  ( 0.000000000000000000, 0.000000000000000000, 1.000000000000000000 ) ) ;
#6189=VERTEX_POINT ( 'NONE', #10308 ) ;
#6190=VECTOR ( 'NONE', #5447, 1000.000000000000000 ) ;
#6192=ORIENTED_EDGE ( 'NONE', *, *, #7632, .F. ) ;
#6193=CARTESIAN_POINT ( 'NONE',  ( 3.000000000000000888, 9.039786367039127413, -21.14796121233187520 ) ) ;
#6194=CARTESIAN_POINT ( 'NONE',  ( 3.000000000000000888, 24.53384959170457691, 3.623565124517186931 ) ) ;
#6196=DIRECTION ( 'NONE',  ( -1.000000000000000000, -0.000000000000000000, 0.000000000000000000 ) ) ;
#6198=CARTESIAN_POINT ( 'NONE',  ( 3.000000000000000888, -11.67026512804534022, -19.29833442572371638 ) ) ;
#6200=CARTESIAN_POINT ( 'NONE',  ( 0.000000000000000000, 17.35216073792464897, -17.71842311621511712 ) ) ;
#6201=DIRECTION ( 'NONE',  ( -1.000000000000000000, -0.000000000000000000, 0.000000000000000000 ) ) ;
#6202=ORIENTED_EDGE ( 'NONE', *, *, #2324, .F. ) ;
#6204=DIRECTION ( 'NONE',  ( 0.000000000000000000, 0.000000000000000000, 1.000000000000000000 ) ) ;
#6206=ORIENTED_EDGE ( 'NONE', *, *, #633, .T. ) ;
#6208=EDGE_CURVE ( 'NONE', #6263, #7573, #11294, .T. ) ;
#6209=DIRECTION ( 'NONE',  ( 0.000000000000000000, 0.000000000000000000, 1.000000000000000000 ) ) ;
#6210=CARTESIAN_POINT ( 'NONE',  ( 1.499999999999999556, 6.168200451486086422, -24.02068490260606026 ) ) ;
#6212=DIRECTION ( 'NONE',  ( -1.000000000000000000, -0.000000000000000000, -0.000000000000000000 ) ) ;
#6214=DIRECTION ( 'NONE',  ( -1.000000000000000000, 0.000000000000000000, -0.000000000000000000 ) ) ;
#6215=ORIENTED_EDGE ( 'NONE', *, *, #8864, .T. ) ;
#6216=CIRCLE ( 'NONE', #6978, 9.599999999999997868 ) ;
#6218=ORIENTED_EDGE ( 'NONE', *, *, #10692, .F. ) ;
#6220=ADVANCED_FACE ( 'NONE', ( #2911 ), #6633, .T. ) ;
#6221=CARTESIAN_POINT ( 'NONE',  ( 3.000000000000000888, -2.062268319295407881, -22.90635393027948297 ) ) ;
#6222=CARTESIAN_POINT ( 'NONE',  ( 3.000000000000000888, 22.56530478845654386, -4.445336973060635799 ) ) ;
#6223=AXIS2_PLACEMENT_3D ( 'NONE', #5863, #1270, #11610 ) ;
#6224=CIRCLE ( 'NONE', #11694, 24.80000000000000071 ) ;
#6226=DIRECTION ( 'NONE',  ( -1.000000000000000000, 0.000000000000000000, 0.000000000000000000 ) ) ;
#6227=CARTESIAN_POINT ( 'NONE',  ( 3.000000000000000888, 22.83456483164689033, 2.745295967526073078 ) ) ;
#6228=ORIENTED_EDGE ( 'NONE', *, *, #11956, .F. ) ;
#6229=ORIENTED_EDGE ( 'NONE', *, *, #7399, .F. ) ;
#6230=EDGE_CURVE ( 'NONE', #3076, #8331, #2063, .T. ) ;
#6233=VECTOR ( 'NONE', #11054, 1000.000000000000000 ) ;
#6234=AXIS2_PLACEMENT_3D ( 'NONE', #6025, #9752, #2411 ) ;
#6236=DIRECTION ( 'NONE',  ( 0.000000000000000000, -0.3090169943749349057, -0.9510565162951577500 ) ) ;
#6238=FACE_OUTER_BOUND ( 'NONE', #5729, .T. ) ;
#6241=CARTESIAN_POINT ( 'NONE',  ( 3.000000000000000888, 0.000000000000000000, 0.000000000000000000 ) ) ;
#6244=ADVANCED_FACE ( 'NONE', ( #8726 ), #4067, .T. ) ;
#6246=DIRECTION ( 'NONE',  ( -1.000000000000000000, -0.000000000000000000, -0.000000000000000000 ) ) ;
#6247=ORIENTED_EDGE ( 'NONE', *, *, #11476, .F. ) ;
#6248=VERTEX_POINT ( 'NONE', #4989 ) ;
#6250=CIRCLE ( 'NONE', #4286, 19.99999999999999645 ) ;
#6251=ORIENTED_EDGE ( 'NONE', *, *, #7802, .T. ) ;
#6252=CARTESIAN_POINT ( 'NONE',  ( 0.000000000000000000, 24.77821629063821973, 1.039229259764575364 ) ) ;
#6253=CIRCLE ( 'NONE', #2335, 4.000000000000000000 ) ;
#6254=CARTESIAN_POINT ( 'NONE',  ( 3.000000000000000888, 8.753070780933159156, 20.78471918669863427 ) ) ;
#6255=DIRECTION ( 'NONE',  ( 0.000000000000000000, 0.2079116908177598144, -0.9781476007338055778 ) ) ;
#6257=FACE_OUTER_BOUND ( 'NONE', #1350, .T. ) ;
#6259=DIRECTION ( 'NONE',  ( -1.000000000000000000, 0.000000000000000000, 0.000000000000000000 ) ) ;
#6260=VERTEX_POINT ( 'NONE', #328 ) ;
#6262=VECTOR ( 'NONE', #8123, 1000.000000000000000 ) ;
#6263=VERTEX_POINT ( 'NONE', #4132 ) ;
#6265=DIRECTION ( 'NONE',  ( 0.000000000000000000, 0.000000000000000000, 1.000000000000000000 ) ) ;
#6266=EDGE_LOOP ( 'NONE', ( #9223, #7299, #10036, #6599 ) ) ;
#6267=AXIS2_PLACEMENT_3D ( 'NONE', #4418, #9015, #1426 ) ;
#6268=DIRECTION ( 'NONE',  ( -1.000000000000000000, 0.000000000000000000, 0.000000000000000000 ) ) ;
#6269=VECTOR ( 'NONE', #9115, 1000.000000000000000 ) ;
#6270=AXIS2_PLACEMENT_3D ( 'NONE', #9132, #4479, #1428 ) ;
#6271=CARTESIAN_POINT ( 'NONE',  ( 1.500000000000000444, -19.10918332567947076, -15.80756504416710229 ) ) ;
#6275=DIRECTION ( 'NONE',  ( -1.000000000000000000, -0.000000000000000000, -0.000000000000000000 ) ) ;
#6276=CARTESIAN_POINT ( 'NONE',  ( 3.000000000000000888, 22.54798042742718067, -0.4575788569252652871 ) ) ;
#6277=VERTEX_POINT ( 'NONE', #6085 ) ;
#6278=AXIS2_PLACEMENT_3D ( 'NONE', #4971, #8707, #1290 ) ;
#6279=ORIENTED_EDGE ( 'NONE', *, *, #4263, .T. ) ;
#6280=ADVANCED_FACE ( 'NONE', ( #450 ), #4243, .T. ) ;
#6282=ORIENTED_EDGE ( 'NONE', *, *, #2461, .T. ) ;
#6285=CARTESIAN_POINT ( 'NONE',  ( 0.000000000000000000, 19.75591328264900781, -10.87771529938142123 ) ) ;
#6286=CYLINDRICAL_SURFACE ( 'NONE', #3301, 9.599999999999997868 ) ;
#6287=CARTESIAN_POINT ( 'NONE',  ( 0.000000000000000000, 0.000000000000000000, 0.000000000000000000 ) ) ;
#6288=EDGE_CURVE ( 'NONE', #8212, #9360, #8323, .T. ) ;
#6289=CIRCLE ( 'NONE', #3349, 24.80000000000000071 ) ;
#6291=FACE_OUTER_BOUND ( 'NONE', #7656, .T. ) ;
#6292=EDGE_CURVE ( 'NONE', #2317, #10809, #691, .T. ) ;
#6293=DIRECTION ( 'NONE',  ( 0.000000000000000000, -0.9510565162951566398, 0.3090169943749382919 ) ) ;
#6295=ORIENTED_EDGE ( 'NONE', *, *, #5274, .T. ) ;
#6297=EDGE_CURVE ( 'NONE', #4270, #9364, #10866, .T. ) ;
#6298=AXIS2_PLACEMENT_3D ( 'NONE', #5783, #9506, #378 ) ;
#6299=ORIENTED_EDGE ( 'NONE', *, *, #8120, .F. ) ;
#6300=DIRECTION ( 'NONE',  ( -1.000000000000000000, 0.000000000000000000, 0.000000000000000000 ) ) ;
#6301=VECTOR ( 'NONE', #6731, 1000.000000000000000 ) ;
#6302=DIRECTION ( 'NONE',  ( 1.000000000000000000, -0.000000000000000000, -0.000000000000000000 ) ) ;
#6303=LINE ( 'NONE', #9052, #2279 ) ;
#6304=VERTEX_POINT ( 'NONE', #3212 ) ;
#6305=CARTESIAN_POINT ( 'NONE',  ( 0.000000000000000000, 8.645255683529311952, -23.24434456306316577 ) ) ;
#6306=FACE_OUTER_BOUND ( 'NONE', #636, .T. ) ;
#6308=CIRCLE ( 'NONE', #2785, 9.599999999999997868 ) ;
#6309=DIRECTION ( 'NONE',  ( 0.000000000000000000, 0.000000000000000000, 1.000000000000000000 ) ) ;
#6310=DIRECTION ( 'NONE',  ( 0.000000000000000000, -0.5877852522924797984, 0.8090169943749426773 ) ) ;
#6312=CYLINDRICAL_SURFACE ( 'NONE', #9, 24.80000000000000071 ) ;
#6313=EDGE_LOOP ( 'NONE', ( #6718, #10961, #8856, #6774 ) ) ;
#6316=( GEOMETRIC_REPRESENTATION_CONTEXT ( 3 ) GLOBAL_UNCERTAINTY_ASSIGNED_CONTEXT ( ( #9293 ) ) GLOBAL_UNIT_ASSIGNED_CONTEXT ( ( #5409, #568, #3459 ) ) REPRESENTATION_CONTEXT ( 'NONE', 'WORKASPACE' ) );
#6317=ORIENTED_EDGE ( 'NONE', *, *, #2282, .F. ) ;
#6318=DIRECTION ( 'NONE',  ( -1.000000000000000000, -0.000000000000000000, -0.000000000000000000 ) ) ;
#6319=ORIENTED_EDGE ( 'NONE', *, *, #6602, .F. ) ;
#6321=CARTESIAN_POINT ( 'NONE',  ( 0.000000000000000000, 9.128825345753028842, 23.05871956130125611 ) ) ;
#6322=CIRCLE ( 'NONE', #6703, 22.99900000000000233 ) ;
#6323=CYLINDRICAL_SURFACE ( 'NONE', #12010, 9.599999999999997868 ) ;
#6325=EDGE_CURVE ( 'NONE', #6367, #110, #11252, .T. ) ;
#6326=CYLINDRICAL_SURFACE ( 'NONE', #5298, 22.99899999999999878 ) ;
#6327=AXIS2_PLACEMENT_3D ( 'NONE', #9072, #683, #10965 ) ;
#6328=ORIENTED_EDGE ( 'NONE', *, *, #6655, .F. ) ;
#6329=DIRECTION ( 'NONE',  ( 0.000000000000000000, -0.6691306063588644548, 0.7431448254773885820 ) ) ;
#6330=ORIENTED_EDGE ( 'NONE', *, *, #6755, .T. ) ;
#6333=SURFACE_SIDE_STYLE ('',( #7167 ) ) ;
#6335=EDGE_CURVE ( 'NONE', #11607, #8421, #10072, .T. ) ;
#6336=CIRCLE ( 'NONE', #1057, 9.599999999999997868 ) ;
#6337=DIRECTION ( 'NONE',  ( -1.000000000000000000, 0.000000000000000000, -0.000000000000000000 ) ) ;
#6338=FACE_OUTER_BOUND ( 'NONE', #4501, .T. ) ;
#6339=DIRECTION ( 'NONE',  ( -1.000000000000000000, -0.000000000000000000, 0.000000000000000000 ) ) ;
#6341=LINE ( 'NONE', #7176, #10221 ) ;
#6342=FACE_OUTER_BOUND ( 'NONE', #480, .T. ) ;
#6343=ORIENTED_EDGE ( 'NONE', *, *, #10122, .T. ) ;
#6344=ORIENTED_EDGE ( 'NONE', *, *, #6395, .F. ) ;
#6345=AXIS2_PLACEMENT_3D ( 'NONE', #11099, #10916, #9028 ) ;
#6346=ORIENTED_EDGE ( 'NONE', *, *, #7399, .T. ) ;
#6348=CARTESIAN_POINT ( 'NONE',  ( 0.000000000000000000, -22.99643626497956461, -0.3433949777334098785 ) ) ;
#6349=DIRECTION ( 'NONE',  ( -1.000000000000000000, -0.000000000000000000, -0.000000000000000000 ) ) ;
#6351=CARTESIAN_POINT ( 'NONE',  ( 0.000000000000000000, 22.47229024614980020, -1.901833551798019162 ) ) ;
#6352=EDGE_LOOP ( 'NONE', ( #3499, #8033, #5586, #9774 ) ) ;
#6353=FACE_OUTER_BOUND ( 'NONE', #3733, .T. ) ;
#6354=VERTEX_POINT ( 'NONE', #10860 ) ;
#6355=ORIENTED_EDGE ( 'NONE', *, *, #32, .F. ) ;
#6358=DIRECTION ( 'NONE',  ( -1.000000000000000000, 0.000000000000000000, 0.000000000000000000 ) ) ;
#6359=CARTESIAN_POINT ( 'NONE',  ( -10.00000000000000000, 0.000000000000000000, 0.000000000000000000 ) ) ;
#6361=ADVANCED_FACE ( 'NONE', ( #1370 ), #7916, .T. ) ;
#6362=DIRECTION ( 'NONE',  ( -1.000000000000000000, -0.000000000000000000, 0.000000000000000000 ) ) ;
#6364=CIRCLE ( 'NONE', #11055, 24.80000000000000071 ) ;
#6365=ADVANCED_FACE ( 'NONE', ( #4190 ), #6986, .T. ) ;
#6366=CARTESIAN_POINT ( 'NONE',  ( 0.000000000000000000, -21.96011696265495061, 5.135568396239952982 ) ) ;
#6367=VERTEX_POINT ( 'NONE', #567 ) ;
#6368=DIRECTION ( 'NONE',  ( -1.000000000000000000, 0.000000000000000000, 0.000000000000000000 ) ) ;
#6369=VERTEX_POINT ( 'NONE', #5045 ) ;
#6370=EDGE_LOOP ( 'NONE', ( #3411, #6998, #6002, #4469 ) ) ;
#6372=VERTEX_POINT ( 'NONE', #4301 ) ;
#6373=CARTESIAN_POINT ( 'NONE',  ( 3.000000000000000888, 0.000000000000000000, 0.000000000000000000 ) ) ;
#6374=CIRCLE ( 'NONE', #6567, 22.99900000000000233 ) ;
#6375=ORIENTED_EDGE ( 'NONE', *, *, #2268, .T. ) ;
#6376=CARTESIAN_POINT ( 'NONE',  ( 8.000000000000000000, 0.000000000000000000, 0.000000000000000000 ) ) ;
#6377=CARTESIAN_POINT ( 'NONE',  ( 3.000000000000000888, -20.08719549084857192, -11.20082935824096459 ) ) ;
#6379=DIRECTION ( 'NONE',  ( -1.000000000000000000, 0.000000000000000000, 0.000000000000000000 ) ) ;
#6380=CARTESIAN_POINT ( 'NONE',  ( 0.000000000000000000, -16.45023496161675780, 15.42759117534379953 ) ) ;
#6382=CARTESIAN_POINT ( 'NONE',  ( 3.000000000000000000, 0.000000000000000000, 19.99999999999999645 ) ) ;
#6383=ORIENTED_EDGE ( 'NONE', *, *, #6728, .F. ) ;
#6384=ADVANCED_FACE ( 'NONE', ( #8037 ), #386, .T. ) ;
#6386=CYLINDRICAL_SURFACE ( 'NONE', #9099, 24.80000000000000071 ) ;
#6387=ADVANCED_FACE ( 'NONE', ( #3266 ), #10732, .T. ) ;
#6388=DIRECTION ( 'NONE',  ( 0.000000000000000000, -0.9510565162951503115, -0.3090169943749572767 ) ) ;
#6389=DIRECTION ( 'NONE',  ( 0.000000000000000000, 0.000000000000000000, 1.000000000000000000 ) ) ;
#6394=EDGE_LOOP ( 'NONE', ( #6229, #8554, #11971, #1953 ) ) ;
#6395=EDGE_CURVE ( 'NONE', #9406, #1101, #9084, .T. ) ;
#6397=VERTEX_POINT ( 'NONE', #7166 ) ;
#6400=DIRECTION ( 'NONE',  ( 0.000000000000000000, 0.000000000000000000, 1.000000000000000000 ) ) ;
#6402=AXIS2_PLACEMENT_3D ( 'NONE', #4020, #8680, #279 ) ;
#6404=EDGE_CURVE ( 'NONE', #6837, #1013, #5589, .T. ) ;
#6406=CARTESIAN_POINT ( 'NONE',  ( 3.000000000000000888, 0.000000000000000000, 0.000000000000000000 ) ) ;
#6407=ORIENTED_EDGE ( 'NONE', *, *, #8530, .F. ) ;
#6408=LINE ( 'NONE', #10013, #11536 ) ;
#6409=ORIENTED_EDGE ( 'NONE', *, *, #590, .F. ) ;
#6410=ORIENTED_EDGE ( 'NONE', *, *, #5684, .F. ) ;
#6411=DIRECTION ( 'NONE',  ( -1.000000000000000000, -0.000000000000000000, 0.000000000000000000 ) ) ;
#6413=AXIS2_PLACEMENT_3D ( 'NONE', #5196, #7137, #2499 ) ;
#6415=DIRECTION ( 'NONE',  ( -1.000000000000000000, -0.000000000000000000, 0.000000000000000000 ) ) ;
#6416=CARTESIAN_POINT ( 'NONE',  ( 3.000000000000000888, 0.000000000000000000, 0.000000000000000000 ) ) ;
#6417=DIRECTION ( 'NONE',  ( -1.000000000000000000, 0.000000000000000000, 0.000000000000000000 ) ) ;
#6419=LINE ( 'NONE', #10149, #6652 ) ;
#6420=VECTOR ( 'NONE', #954, 1000.000000000000000 ) ;
#6421=ORIENTED_EDGE ( 'NONE', *, *, #9833, .T. ) ;
#6422=ORIENTED_EDGE ( 'NONE', *, *, #12112, .T. ) ;
#6423=AXIS2_PLACEMENT_3D ( 'NONE', #8548, #1022, #6635 ) ;
#6424=LINE ( 'NONE', #1707, #2169 ) ;
#6425=ORIENTED_EDGE ( 'NONE', *, *, #303, .T. ) ;
#6426=ORIENTED_EDGE ( 'NONE', *, *, #5981, .T. ) ;
#6428=ADVANCED_FACE ( 'NONE', ( #5285 ), #6386, .T. ) ;
#6429=ORIENTED_EDGE ( 'NONE', *, *, #2304, .T. ) ;
#6430=LINE ( 'NONE', #4468, #2659 ) ;
#6432=EDGE_CURVE ( 'NONE', #7624, #3496, #3049, .T. ) ;
#6433=CIRCLE ( 'NONE', #3900, 24.80000000000000071 ) ;
#6434=CARTESIAN_POINT ( 'NONE',  ( 0.000000000000000000, 21.96011696265491153, -5.135568396240103084 ) ) ;
#6435=FACE_OUTER_BOUND ( 'NONE', #97, .T. ) ;
#6437=CARTESIAN_POINT ( 'NONE',  ( 3.000000000000000888, 0.000000000000000000, 0.000000000000000000 ) ) ;
#6438=VERTEX_POINT ( 'NONE', #3693 ) ;
#6439=CYLINDRICAL_SURFACE ( 'NONE', #8816, 24.80000000000000071 ) ;
#6440=ORIENTED_EDGE ( 'NONE', *, *, #2347, .F. ) ;
#6441=EDGE_CURVE ( 'NONE', #5393, #7011, #8721, .T. ) ;
#6443=ADVANCED_FACE ( 'NONE', ( #815 ), #8159, .T. ) ;
#6444=AXIS2_PLACEMENT_3D ( 'NONE', #346, #9898, #3176 ) ;
#6445=DIRECTION ( 'NONE',  ( -1.000000000000000000, -0.000000000000000000, -0.000000000000000000 ) ) ;
#6446=CARTESIAN_POINT ( 'NONE',  ( 3.000000000000000888, 12.88318129270179035, 18.51065745848382349 ) ) ;
#6447=CYLINDRICAL_SURFACE ( 'NONE', #467, 9.599999999999997868 ) ;
#6448=DIRECTION ( 'NONE',  ( 0.000000000000000000, -0.7431448254773863615, -0.6691306063588672304 ) ) ;
#6449=AXIS2_PLACEMENT_3D ( 'NONE', #1824, #153, #6646 ) ;
#6451=FACE_OUTER_BOUND ( 'NONE', #6727, .T. ) ;
#6452=AXIS2_PLACEMENT_3D ( 'NONE', #7913, #2972, #1254 ) ;
#6454=ORIENTED_EDGE ( 'NONE', *, *, #9134, .F. ) ;
#6455=EDGE_CURVE ( 'NONE', #3496, #4018, #10273, .T. ) ;
#6456=VERTEX_POINT ( 'NONE', #2598 ) ;
#6457=CYLINDRICAL_SURFACE ( 'NONE', #7602, 24.80000000000000071 ) ;
#6459=DIRECTION ( 'NONE',  ( -1.000000000000000000, 0.000000000000000000, -0.000000000000000000 ) ) ;
#6460=DIRECTION ( 'NONE',  ( -1.000000000000000000, 0.000000000000000000, 0.000000000000000000 ) ) ;
#6464=CYLINDRICAL_SURFACE ( 'NONE', #611, 9.599999999999997868 ) ;
#6466=VERTEX_POINT ( 'NONE', #11886 ) ;
#6467=ORIENTED_EDGE ( 'NONE', *, *, #6687, .T. ) ;
#6468=ORIENTED_EDGE ( 'NONE', *, *, #1127, .F. ) ;
#6469=DIRECTION ( 'NONE',  ( -1.000000000000000000, 0.000000000000000000, 0.000000000000000000 ) ) ;
#6470=CARTESIAN_POINT ( 'NONE',  ( 3.000000000000000888, 22.99643626497956816, -0.3433949777332470088 ) ) ;
#6471=AXIS2_PLACEMENT_3D ( 'NONE', #952, #3709, #2855 ) ;
#6472=AXIS2_PLACEMENT_3D ( 'NONE', #1509, #588, #4325 ) ;
#6473=CARTESIAN_POINT ( 'NONE',  ( 0.000000000000000000, -7.432877647175354596, 21.76479567747239230 ) ) ;
#6474=DIRECTION ( 'NONE',  ( 0.000000000000000000, 0.000000000000000000, 1.000000000000000000 ) ) ;
#6476=CARTESIAN_POINT ( 'NONE',  ( 3.000000000000000888, 1.556492618230640002, 24.75110766671652840 ) ) ;
#6479=CIRCLE ( 'NONE', #6298, 9.599999999999996092 ) ;
#6480=CARTESIAN_POINT ( 'NONE',  ( 0.000000000000000000, 0.000000000000000000, 0.000000000000000000 ) ) ;
#6481=ORIENTED_EDGE ( 'NONE', *, *, #596, .T. ) ;
#6482=ORIENTED_EDGE ( 'NONE', *, *, #3518, .F. ) ;
#6483=CARTESIAN_POINT ( 'NONE',  ( 3.000000000000000888, 0.000000000000000000, 0.000000000000000000 ) ) ;
#6484=VECTOR ( 'NONE', #11748, 1000.000000000000000 ) ;
#6485=ORIENTED_EDGE ( 'NONE', *, *, #2477, .F. ) ;
#6486=ORIENTED_EDGE ( 'NONE', *, *, #143, .T. ) ;
#6489=VERTEX_POINT ( 'NONE', #5464 ) ;
#6490=AXIS2_PLACEMENT_3D ( 'NONE', #10527, #10751, #3989 ) ;
#6491=AXIS2_PLACEMENT_3D ( 'NONE', #8640, #1407, #9672 ) ;
#6492=DIRECTION ( 'NONE',  ( 0.000000000000000000, 0.9945218953682736229, -0.1045284632676503622 ) ) ;
#6493=CARTESIAN_POINT ( 'NONE',  ( 0.000000000000000000, 2.811977935937781670, 22.37663021667345120 ) ) ;
#6495=CARTESIAN_POINT ( 'NONE',  ( 3.000000000000000888, 18.80635025205187816, -13.23915371906935867 ) ) ;
#6496=CARTESIAN_POINT ( 'NONE',  ( 0.000000000000000000, 0.000000000000000000, 0.000000000000000000 ) ) ;
#6497=ORIENTED_EDGE ( 'NONE', *, *, #1800, .F. ) ;
#6499=EDGE_CURVE ( 'NONE', #10656, #10872, #1286, .T. ) ;
#6500=CIRCLE ( 'NONE', #1838, 9.599999999999996092 ) ;
#6501=FACE_OUTER_BOUND ( 'NONE', #8737, .T. ) ;
#6502=VERTEX_POINT ( 'NONE', #12066 ) ;
#6503=CIRCLE ( 'NONE', #1228, 24.80000000000000071 ) ;
#6505=CIRCLE ( 'NONE', #5926, 22.99899999999999878 ) ;
#6507=LINE ( 'NONE', #10242, #6985 ) ;
#6508=DIRECTION ( 'NONE',  ( 0.000000000000000000, -0.2079116908177665313, 0.9781476007338041345 ) ) ;
#6511=CIRCLE ( 'NONE', #8858, 24.80000000000000071 ) ;
#6514=CARTESIAN_POINT ( 'NONE',  ( 0.000000000000000000, 0.000000000000000000, 0.000000000000000000 ) ) ;
#6515=CIRCLE ( 'NONE', #448, 24.80000000000000071 ) ;
#6516=AXIS2_PLACEMENT_3D ( 'NONE', #537, #8930, #5995 ) ;
#6517=ADVANCED_FACE ( 'NONE', ( #2775 ), #11945, .T. ) ;
#6518=VERTEX_POINT ( 'NONE', #10110 ) ;
#6519=ORIENTED_EDGE ( 'NONE', *, *, #6455, .T. ) ;
#6520=AXIS2_PLACEMENT_3D ( 'NONE', #3795, #1946, #2008 ) ;
#6521=DIRECTION ( 'NONE',  ( -1.000000000000000000, 0.000000000000000000, 0.000000000000000000 ) ) ;
#6523=CYLINDRICAL_SURFACE ( 'NONE', #2489, 24.80000000000000071 ) ;
#6527=VECTOR ( 'NONE', #755, 1000.000000000000000 ) ;
#6529=VERTEX_POINT ( 'NONE', #1619 ) ;
#6530=ORIENTED_EDGE ( 'NONE', *, *, #4874, .F. ) ;
#6531=ORIENTED_EDGE ( 'NONE', *, *, #969, .F. ) ;
#6532=LINE ( 'NONE', #5677, #5932 ) ;
#6533=FACE_OUTER_BOUND ( 'NONE', #8584, .T. ) ;
#6534=AXIS2_PLACEMENT_3D ( 'NONE', #1248, #376, #4115 ) ;
#6535=CARTESIAN_POINT ( 'NONE',  ( 3.000000000000000888, 0.000000000000000000, 0.000000000000000000 ) ) ;
#6536=CARTESIAN_POINT ( 'NONE',  ( 3.000000000000000888, -13.23915371906968019, 18.80635025205165078 ) ) ;
#6537=ADVANCED_FACE ( 'NONE', ( #2529 ), #12011, .T. ) ;
#6538=DIRECTION ( 'NONE',  ( -1.000000000000000000, 0.000000000000000000, -0.000000000000000000 ) ) ;
#6542=ORIENTED_EDGE ( 'NONE', *, *, #2048, .T. ) ;
#6543=ORIENTED_EDGE ( 'NONE', *, *, #3689, .T. ) ;
#6544=FACE_OUTER_BOUND ( 'NONE', #4419, .T. ) ;
#6545=EDGE_CURVE ( 'NONE', #1864, #8369, #11636, .T. ) ;
#6546=EDGE_LOOP ( 'NONE', ( #8575, #1834, #2194, #12048 ) ) ;
#6548=DIRECTION ( 'NONE',  ( -1.000000000000000000, 0.000000000000000000, 0.000000000000000000 ) ) ;
#6549=DIRECTION ( 'NONE',  ( -1.000000000000000000, 0.000000000000000000, -0.000000000000000000 ) ) ;
#6550=VERTEX_POINT ( 'NONE', #7415 ) ;
#6551=DIRECTION ( 'NONE',  ( -1.000000000000000000, 0.000000000000000000, 0.000000000000000000 ) ) ;
#6552=CARTESIAN_POINT ( 'NONE',  ( 3.000000000000000888, 0.000000000000000000, 0.000000000000000000 ) ) ;
#6554=DIRECTION ( 'NONE',  ( 0.000000000000000000, 0.000000000000000000, 1.000000000000000000 ) ) ;
#6555=DIRECTION ( 'NONE',  ( 0.000000000000000000, -0.8660254037844433705, 0.4999999999999919509 ) ) ;
#6556=CARTESIAN_POINT ( 'NONE',  ( 3.000000000000000888, 20.65684170206491643, 13.72351598154904018 ) ) ;
#6557=ORIENTED_EDGE ( 'NONE', *, *, #1451, .F. ) ;
#6558=DIRECTION ( 'NONE',  ( -1.000000000000000000, 0.000000000000000000, -0.000000000000000000 ) ) ;
#6559=ORIENTED_EDGE ( 'NONE', *, *, #938, .F. ) ;
#6562=DIRECTION ( 'NONE',  ( 0.000000000000000000, 0.000000000000000000, -1.000000000000000000 ) ) ;
#6564=CARTESIAN_POINT ( 'NONE',  ( 0.000000000000000000, -21.97702544527762214, 6.779701584702658046 ) ) ;
#6565=LINE ( 'NONE', #4676, #5955 ) ;
#6567=AXIS2_PLACEMENT_3D ( 'NONE', #1174, #74, #7723 ) ;
#6569=DIRECTION ( 'NONE',  ( -1.000000000000000000, 0.000000000000000000, -0.000000000000000000 ) ) ;
#6570=DIRECTION ( 'NONE',  ( -1.000000000000000000, 0.000000000000000000, 0.000000000000000000 ) ) ;
#6572=ORIENTED_EDGE ( 'NONE', *, *, #11685, .F. ) ;
#6573=ORIENTED_EDGE ( 'NONE', *, *, #9617, .T. ) ;
#6574=CIRCLE ( 'NONE', #5017, 9.599999999999997868 ) ;
#6577=EDGE_CURVE ( 'NONE', #11545, #4550, #6364, .T. ) ;
#6578=CARTESIAN_POINT ( 'NONE',  ( 0.000000000000000000, 17.97274125076074114, 13.62355943574025652 ) ) ;
#6579=EDGE_CURVE ( 'NONE', #9445, #5055, #12026, .T. ) ;
#6580=EDGE_CURVE ( 'NONE', #1587, #2893, #5787, .T. ) ;
#6582=CARTESIAN_POINT ( 'NONE',  ( 0.000000000000000000, 20.65684170206509762, -13.72351598154876484 ) ) ;
#6583=LINE ( 'NONE', #1816, #2563 ) ;
#6585=EDGE_LOOP ( 'NONE', ( #10583, #1227, #8204, #9257 ) ) ;
#6586=ORIENTED_EDGE ( 'NONE', *, *, #9803, .T. ) ;
#6587=EDGE_CURVE ( 'NONE', #117, #9866, #494, .T. ) ;
#6588=DIRECTION ( 'NONE',  ( -1.000000000000000000, 0.000000000000000000, 0.000000000000000000 ) ) ;
#6589=LINE ( 'NONE', #3720, #1392 ) ;
#6590=CYLINDRICAL_SURFACE ( 'NONE', #7992, 9.599999999999997868 ) ;
#6591=DIRECTION ( 'NONE',  ( -1.000000000000000000, 0.000000000000000000, 0.000000000000000000 ) ) ;
#6592=VECTOR ( 'NONE', #1194, 1000.000000000000000 ) ;
#6596=ADVANCED_FACE ( 'NONE', ( #255 ), #10479, .T. ) ;
#6597=CARTESIAN_POINT ( 'NONE',  ( 3.000000000000000888, 0.000000000000000000, 0.000000000000000000 ) ) ;
#6598=ORIENTED_EDGE ( 'NONE', *, *, #11596, .T. ) ;
#6599=ORIENTED_EDGE ( 'NONE', *, *, #2844, .T. ) ;
#6600=LINE ( 'NONE', #4831, #5308 ) ;
#6601=ORIENTED_EDGE ( 'NONE', *, *, #11661, .T. ) ;
#6602=EDGE_CURVE ( 'NONE', #6896, #662, #2453, .T. ) ;
#6603=AXIS2_PLACEMENT_3D ( 'NONE', #10098, #11084, #3565 ) ;
#6606=EDGE_LOOP ( 'NONE', ( #1545, #1976, #7734, #4230 ) ) ;
#6607=CYLINDRICAL_SURFACE ( 'NONE', #7485, 24.80000000000000071 ) ;
#6608=EDGE_CURVE ( 'NONE', #9071, #6916, #8408, .T. ) ;
#6609=LINE ( 'NONE', #2885, #230 ) ;
#6611=CIRCLE ( 'NONE', #4078, 9.599999999999997868 ) ;
#6612=DIRECTION ( 'NONE',  ( -1.000000000000000000, 0.000000000000000000, -0.000000000000000000 ) ) ;
#6613=CARTESIAN_POINT ( 'NONE',  ( 3.000000000000000888, 11.48910920600683738, 21.97817939804043519 ) ) ;
#6614=EDGE_LOOP ( 'NONE', ( #2433, #10050, #7634, #520 ) ) ;
#6616=CARTESIAN_POINT ( 'NONE',  ( 3.000000000000000888, 15.42759117534385993, 16.45023496161670451 ) ) ;
#6618=EDGE_CURVE ( 'NONE', #11471, #11794, #8729, .T. ) ;
#6620=AXIS2_PLACEMENT_3D ( 'NONE', #6050, #6780, #9777 ) ;
#6621=DIRECTION ( 'NONE',  ( 0.000000000000000000, 0.000000000000000000, 1.000000000000000000 ) ) ;
#6623=CARTESIAN_POINT ( 'NONE',  ( 1.500000000000000444, 13.72351598154897268, 20.65684170206496262 ) ) ;
#6624=EDGE_CURVE ( 'NONE', #4337, #2865, #10671, .T. ) ;
#6625=CYLINDRICAL_SURFACE ( 'NONE', #1066, 9.599999999999997868 ) ;
#6626=CARTESIAN_POINT ( 'NONE',  ( 0.000000000000000000, 6.532525787311267429, -21.58580335785669746 ) ) ;
#6627=CARTESIAN_POINT ( 'NONE',  ( 3.000000000000000888, -23.88662356770110762, -6.668524164681871369 ) ) ;
#6628=DIRECTION ( 'NONE',  ( -1.000000000000000000, 0.000000000000000000, 0.000000000000000000 ) ) ;
#6629=CARTESIAN_POINT ( 'NONE',  ( 3.000000000000000888, 0.000000000000000000, 0.000000000000000000 ) ) ;
#6630=ORIENTED_EDGE ( 'NONE', *, *, #5721, .T. ) ;
#6632=ORIENTED_EDGE ( 'NONE', *, *, #2854, .F. ) ;
#6633=CYLINDRICAL_SURFACE ( 'NONE', #3631, 22.99899999999999878 ) ;
#6635=DIRECTION ( 'NONE',  ( 0.000000000000000000, 0.4067366430758009299, -0.9135454576426005335 ) ) ;
#6636=AXIS2_PLACEMENT_3D ( 'NONE', #5063, #4208, #1327 ) ;
#6638=CARTESIAN_POINT ( 'NONE',  ( 0.000000000000000000, 4.898587196589412829E-16, -4.000000000000000000 ) ) ;
#6639=ORIENTED_EDGE ( 'NONE', *, *, #5866, .F. ) ;
#6640=VECTOR ( 'NONE', #5051, 1000.000000000000000 ) ;
#6641=ORIENTED_EDGE ( 'NONE', *, *, #90, .F. ) ;
#6642=EDGE_CURVE ( 'NONE', #3296, #3787, #9698, .T. ) ;
#6643=AXIS2_PLACEMENT_3D ( 'NONE', #6693, #383, #8842 ) ;
#6646=DIRECTION ( 'NONE',  ( 0.000000000000000000, 0.000000000000000000, 1.000000000000000000 ) ) ;
#6647=ORIENTED_EDGE ( 'NONE', *, *, #11197, .F. ) ;
#6648=LINE ( 'NONE', #9412, #1353 ) ;
#6649=DIRECTION ( 'NONE',  ( 1.000000000000000000, -0.000000000000000000, 0.000000000000000000 ) ) ;
#6650=CIRCLE ( 'NONE', #4117, 9.599999999999997868 ) ;
#6651=CYLINDRICAL_SURFACE ( 'NONE', #11023, 22.99899999999999878 ) ;
#6652=VECTOR ( 'NONE', #1766, 1000.000000000000000 ) ;
#6653=AXIS2_PLACEMENT_3D ( 'NONE', #10657, #5949, #8526 ) ;
#6655=EDGE_CURVE ( 'NONE', #4944, #7927, #7479, .T. ) ;
#6658=VERTEX_POINT ( 'NONE', #11402 ) ;
#6659=ORIENTED_EDGE ( 'NONE', *, *, #11707, .F. ) ;
#6660=DIRECTION ( 'NONE',  ( 1.000000000000000000, 0.000000000000000000, 0.000000000000000000 ) ) ;
#6661=AXIS2_PLACEMENT_3D ( 'NONE', #7041, #6145, #8469 ) ;
#6662=VERTEX_POINT ( 'NONE', #7596 ) ;
#6664=AXIS2_PLACEMENT_3D ( 'NONE', #4463, #9302, #9173 ) ;
#6665=VECTOR ( 'NONE', #9409, 1000.000000000000000 ) ;
#6666=LINE ( 'NONE', #6726, #2666 ) ;
#6669=CYLINDRICAL_SURFACE ( 'NONE', #4745, 24.80000000000000071 ) ;
#6671=AXIS2_PLACEMENT_3D ( 'NONE', #10802, #4135, #332 ) ;
#6673=DIRECTION ( 'NONE',  ( 1.000000000000000000, -0.000000000000000000, -0.000000000000000000 ) ) ;
#6674=CARTESIAN_POINT ( 'NONE',  ( 3.000000000000000888, -21.97702544527762214, 6.779701584702658046 ) ) ;
#6676=EDGE_LOOP ( 'NONE', ( #9493, #6086, #7820, #7389 ) ) ;
#6677=FACE_OUTER_BOUND ( 'NONE', #3841, .T. ) ;
#6678=ORIENTED_EDGE ( 'NONE', *, *, #7618, .F. ) ;
#6680=AXIS2_PLACEMENT_3D ( 'NONE', #11641, #10850, #9923 ) ;
#6681=VECTOR ( 'NONE', #9856, 1000.000000000000000 ) ;
#6682=DIRECTION ( 'NONE',  ( -1.000000000000000000, -0.000000000000000000, -0.000000000000000000 ) ) ;
#6683=ORIENTED_EDGE ( 'NONE', *, *, #4649, .F. ) ;
#6684=CARTESIAN_POINT ( 'NONE',  ( -10.00000000000000000, 0.000000000000000000, 0.000000000000000000 ) ) ;
#6685=DIRECTION ( 'NONE',  ( -1.000000000000000000, 0.000000000000000000, 0.000000000000000000 ) ) ;
#6687=EDGE_CURVE ( 'NONE', #4410, #264, #6759, .T. ) ;
#6688=SURFACE_STYLE_FILL_AREA ( #6747 ) ;
#6690=FACE_OUTER_BOUND ( 'NONE', #6119, .T. ) ;
#6691=AXIS2_PLACEMENT_3D ( 'NONE', #2569, #3491, #7201 ) ;
#6692=ORIENTED_EDGE ( 'NONE', *, *, #609, .F. ) ;
#6693=CARTESIAN_POINT ( 'NONE',  ( 3.000000000000000888, 6.532525787310969001, 21.58580335785678983 ) ) ;
#6694=ADVANCED_FACE ( 'NONE', ( #2961 ), #3997, .T. ) ;
#6695=EDGE_LOOP ( 'NONE', ( #6062, #2455, #2694, #9148 ) ) ;
#6696=DIRECTION ( 'NONE',  ( 0.000000000000000000, -0.4067366430758071472, 0.9135454576425979800 ) ) ;
#6699=CIRCLE ( 'NONE', #6327, 4.000000000000000000 ) ;
#6700=CARTESIAN_POINT ( 'NONE',  ( 3.000000000000000888, 7.432877647175492264, -21.76479567747234256 ) ) ;
#6702=AXIS2_PLACEMENT_3D ( 'NONE', #9048, #8250, #6115 ) ;
#6703=AXIS2_PLACEMENT_3D ( 'NONE', #1799, #5538, #4800 ) ;
#6705=CARTESIAN_POINT ( 'NONE',  ( 0.000000000000000000, 22.15038895030649257, 4.240409074144170454 ) ) ;
#6706=EDGE_LOOP ( 'NONE', ( #9033, #1276, #3628, #5340, #7347, #3510, #4535, #8080, #9117, #2065, #10447, #2354, #4423, #1410, #7692, #4514, #11719, #3115, #10014, #8013, #7718, #1457, #1697, #2513, #1687, #7060, #593, #11338, #6543, #11091, #37, #11263, #4715, #7782, #5701, #3355, #7016, #6053, #4452, #2686, #4806, #4276, #7269, #2923, #3676, #10548, #6421, #10003, #11058, #4859, #2674, #6279, #8181, #8996, #1714, #7392, #10237, #3993, #11510, #10379, #9259, #9456, #11060, #6519, #2689, #5166, #920, #2938, #1129, #9147, #11681, #9376, #594, #2724, #7069, #4565, #10034, #10284, #124, #9157, #6531, #5627, #11104, #2017, #8587, #5256, #10413, #1807, #6707, #6586, #2540, #2758, #10577, #1162, #5824, #3735, #792, #1840, #211, #9876, #7689, #6133, #1923, #11946, #9510, #16, #3322, #3800, #4127, #3731, #1155, #2861, #184, #1104, #3601, #2241, #5931, #3065, #10432, #11163, #10854, #8501, #3198, #2202, #2296, #54, #9799, #7901, #7046, #6129, #4093, #10219, #1206, #2805, #5018, #8676, #4816, #10474, #2165, #10549, #9932, #503, #7032, #4213, #5224, #6871, #3950, #229, #6721, #9815, #9514, #11483, #8631, #1275, #10104, #6897, #5025, #5377, #7008, #797, #5964, #9649, #11691, #9616, #10784, #1058, #5711, #688, #1968, #4669, #1786, #3343, #11628, #10884, #3015, #2074, #4500, #1219, #2789, #337, #932, #3177, #5054, #8828, #6020, #11730, #1089, #10078, #548, #11717, #1316, #12062, #11871, #6440, #812, #10118, #5512, #10018, #7208, #7131, #4233, #5528, #9122, #4052, #7241, #4031, #8132, #5349, #2556, #5299, #10090, #10811, #11785, #4997, #12053, #1237, #8124, #8985, #6171, #6791, #3525, #3438, #11303, #3740, #4407, #2000, #1126, #3802, #10415, #8215, #8168, #2910, #6598, #8567, #5629, #8003, #1130, #5557, #2579, #5488, #1969, #7574, #2609, #5559, #8453 ) ) ;
#6707=ORIENTED_EDGE ( 'NONE', *, *, #8864, .F. ) ;
#6708=CIRCLE ( 'NONE', #7688, 9.599999999999997868 ) ;
#6709=ORIENTED_EDGE ( 'NONE', *, *, #3739, .F. ) ;
#6710=DIRECTION ( 'NONE',  ( -1.000000000000000000, -0.000000000000000000, -0.000000000000000000 ) ) ;
#6711=DIRECTION ( 'NONE',  ( 0.000000000000000000, 0.000000000000000000, -1.000000000000000000 ) ) ;
#6712=ORIENTED_EDGE ( 'NONE', *, *, #5368, .F. ) ;
#6713=DIRECTION ( 'NONE',  ( 0.000000000000000000, 0.2079116908177532086, 0.9781476007338069101 ) ) ;
#6714=CARTESIAN_POINT ( 'NONE',  ( 3.000000000000000888, -11.79560690673886292, 19.74380051311536022 ) ) ;
#6715=LINE ( 'NONE', #10864, #9075 ) ;
#6717=DIRECTION ( 'NONE',  ( -1.000000000000000000, -0.000000000000000000, -0.000000000000000000 ) ) ;
#6718=ORIENTED_EDGE ( 'NONE', *, *, #12105, .F. ) ;
#6719=VERTEX_POINT ( 'NONE', #7663 ) ;
#6720=DIRECTION ( 'NONE',  ( 0.000000000000000000, 0.000000000000000000, -1.000000000000000000 ) ) ;
#6721=ORIENTED_EDGE ( 'NONE', *, *, #6587, .F. ) ;
#6722=CIRCLE ( 'NONE', #1449, 9.599999999999997868 ) ;
#6723=DIRECTION ( 'NONE',  ( -1.000000000000000000, -0.000000000000000000, 0.000000000000000000 ) ) ;
#6724=CARTESIAN_POINT ( 'NONE',  ( 0.000000000000000000, 0.000000000000000000, 0.000000000000000000 ) ) ;
#6725=ADVANCED_FACE ( 'NONE', ( #1000 ), #8478, .T. ) ;
#6726=CARTESIAN_POINT ( 'NONE',  ( 1.499999999999999556, -9.128825345752876075, -23.05871956130131650 ) ) ;
#6727=EDGE_LOOP ( 'NONE', ( #10412, #3424, #2494, #11668 ) ) ;
#6728=EDGE_CURVE ( 'NONE', #5072, #10349, #6374, .T. ) ;
#6729=CARTESIAN_POINT ( 'NONE',  ( 3.000000000000000888, -22.47229024614976112, -1.901833551798492561 ) ) ;
#6731=DIRECTION ( 'NONE',  ( 1.000000000000000000, -0.000000000000000000, -0.000000000000000000 ) ) ;
#6733=CIRCLE ( 'NONE', #8304, 24.80000000000000071 ) ;
#6734=DIRECTION ( 'NONE',  ( 0.000000000000000000, -0.3090169943749544457, 0.9510565162951514218 ) ) ;
#6735=VERTEX_POINT ( 'NONE', #11689 ) ;
#6736=CARTESIAN_POINT ( 'NONE',  ( 3.000000000000000888, 0.000000000000000000, 0.000000000000000000 ) ) ;
#6737=ORIENTED_EDGE ( 'NONE', *, *, #3544, .T. ) ;
#6738=DIRECTION ( 'NONE',  ( -1.000000000000000000, 0.000000000000000000, -0.000000000000000000 ) ) ;
#6739=ORIENTED_EDGE ( 'NONE', *, *, #11298, .F. ) ;
#6741=EDGE_CURVE ( 'NONE', #1245, #10167, #4976, .T. ) ;
#6742=DIRECTION ( 'NONE',  ( 0.000000000000000000, 0.000000000000000000, 1.000000000000000000 ) ) ;
#6743=ORIENTED_EDGE ( 'NONE', *, *, #4582, .F. ) ;
#6744=DIRECTION ( 'NONE',  ( -1.000000000000000000, -0.000000000000000000, -0.000000000000000000 ) ) ;
#6747=FILL_AREA_STYLE ('',( #8661 ) ) ;
#6750=EDGE_CURVE ( 'NONE', #7795, #8063, #11457, .T. ) ;
#6751=ORIENTED_EDGE ( 'NONE', *, *, #8843, .T. ) ;
#6752=AXIS2_PLACEMENT_3D ( 'NONE', #9501, #9322, #6562 ) ;
#6753=FACE_OUTER_BOUND ( 'NONE', #6370, .T. ) ;
#6754=ORIENTED_EDGE ( 'NONE', *, *, #10598, .F. ) ;
#6755=EDGE_CURVE ( 'NONE', #11218, #1648, #4287, .T. ) ;
#6756=DIRECTION ( 'NONE',  ( 0.000000000000000000, 0.000000000000000000, 1.000000000000000000 ) ) ;
#6758=DIRECTION ( 'NONE',  ( -1.000000000000000000, -0.000000000000000000, -0.000000000000000000 ) ) ;
#6759=CIRCLE ( 'NONE', #4025, 9.599999999999997868 ) ;
#6762=EDGE_CURVE ( 'NONE', #6502, #1587, #5211, .T. ) ;
#6764=DIRECTION ( 'NONE',  ( 0.000000000000000000, 0.000000000000000000, 1.000000000000000000 ) ) ;
#6765=ORIENTED_EDGE ( 'NONE', *, *, #214, .F. ) ;
#6766=VECTOR ( 'NONE', #5434, 1000.000000000000000 ) ;
#6767=ORIENTED_EDGE ( 'NONE', *, *, #7699, .F. ) ;
#6768=CARTESIAN_POINT ( 'NONE',  ( -10.00000000000000000, 0.000000000000000000, 0.000000000000000000 ) ) ;
#6770=CARTESIAN_POINT ( 'NONE',  ( 1.500000000000000444, 15.40502424595145214, 19.43515443678408161 ) ) ;
#6771=DIRECTION ( 'NONE',  ( -1.000000000000000000, -0.000000000000000000, 0.000000000000000000 ) ) ;
#6773=CARTESIAN_POINT ( 'NONE',  ( 3.000000000000000888, 0.000000000000000000, 0.000000000000000000 ) ) ;
#6774=ORIENTED_EDGE ( 'NONE', *, *, #5714, .T. ) ;
#6775=ORIENTED_EDGE ( 'NONE', *, *, #4862, .F. ) ;
#6780=DIRECTION ( 'NONE',  ( -1.000000000000000000, -0.000000000000000000, 0.000000000000000000 ) ) ;
#6781=LINE ( 'NONE', #418, #8870 ) ;
#6783=ORIENTED_EDGE ( 'NONE', *, *, #5241, .F. ) ;
#6785=CARTESIAN_POINT ( 'NONE',  ( 0.000000000000000000, 0.000000000000000000, 0.000000000000000000 ) ) ;
#6787=DIRECTION ( 'NONE',  ( -1.000000000000000000, 0.000000000000000000, 0.000000000000000000 ) ) ;
#6788=VERTEX_POINT ( 'NONE', #7844 ) ;
#6789=FACE_OUTER_BOUND ( 'NONE', #4037, .T. ) ;
#6790=VECTOR ( 'NONE', #10042, 1000.000000000000000 ) ;
#6791=ORIENTED_EDGE ( 'NONE', *, *, #10097, .T. ) ;
#6792=CARTESIAN_POINT ( 'NONE',  ( 3.000000000000000888, 0.000000000000000000, 0.000000000000000000 ) ) ;
#6793=ADVANCED_FACE ( 'NONE', ( #552 ), #2394, .T. ) ;
#6794=ORIENTED_EDGE ( 'NONE', *, *, #11961, .F. ) ;
#6795=EDGE_CURVE ( 'NONE', #7721, #8331, #9498, .T. ) ;
#6798=DIRECTION ( 'NONE',  ( 1.000000000000000000, 0.000000000000000000, 0.000000000000000000 ) ) ;
#6799=AXIS2_PLACEMENT_3D ( 'NONE', #11487, #6771, #6893 ) ;
#6800=DIRECTION ( 'NONE',  ( -1.000000000000000000, -0.000000000000000000, 0.000000000000000000 ) ) ;
#6802=CARTESIAN_POINT ( 'NONE',  ( 0.000000000000000000, 0.000000000000000000, 0.000000000000000000 ) ) ;
#6804=DIRECTION ( 'NONE',  ( -1.000000000000000000, 0.000000000000000000, -0.000000000000000000 ) ) ;
#6805=EDGE_CURVE ( 'NONE', #11900, #11379, #1354, .T. ) ;
#6806=FACE_OUTER_BOUND ( 'NONE', #2181, .T. ) ;
#6807=CARTESIAN_POINT ( 'NONE',  ( 3.000000000000000888, 24.02068490260612776, 6.168200451485839508 ) ) ;
#6809=CIRCLE ( 'NONE', #8161, 9.599999999999997868 ) ;
#6810=ORIENTED_EDGE ( 'NONE', *, *, #4034, .T. ) ;
#6814=DIRECTION ( 'NONE',  ( 0.000000000000000000, 0.000000000000000000, 1.000000000000000000 ) ) ;
#6818=FACE_OUTER_BOUND ( 'NONE', #7792, .T. ) ;
#6819=DIRECTION ( 'NONE',  ( 0.000000000000000000, 0.5877852522924741363, -0.8090169943749467851 ) ) ;
#6823=AXIS2_PLACEMENT_3D ( 'NONE', #10505, #8445, #4767 ) ;
#6825=AXIS2_PLACEMENT_3D ( 'NONE', #4088, #1510, #592 ) ;
#6826=DIRECTION ( 'NONE',  ( 0.000000000000000000, 0.000000000000000000, 1.000000000000000000 ) ) ;
#6827=DIRECTION ( 'NONE',  ( 0.000000000000000000, 0.000000000000000000, 1.000000000000000000 ) ) ;
#6830=EDGE_CURVE ( 'NONE', #5828, #5674, #107, .T. ) ;
#6831=AXIS2_PLACEMENT_3D ( 'NONE', #5313, #3480, #4748 ) ;
#6832=DIRECTION ( 'NONE',  ( -1.000000000000000000, 0.000000000000000000, -0.000000000000000000 ) ) ;
#6833=EDGE_LOOP ( 'NONE', ( #4421, #5351, #6951, #278 ) ) ;
#6834=VERTEX_POINT ( 'NONE', #7957 ) ;
#6837=VERTEX_POINT ( 'NONE', #6858 ) ;
#6838=DIRECTION ( 'NONE',  ( -1.000000000000000000, -0.000000000000000000, -0.000000000000000000 ) ) ;
#6839=CARTESIAN_POINT ( 'NONE',  ( 3.000000000000000888, 10.87771529938188486, -19.75591328264875202 ) ) ;
#6840=ADVANCED_FACE ( 'NONE', ( #2217 ), #7904, .T. ) ;
#6841=AXIS2_PLACEMENT_3D ( 'NONE', #10363, #2784, #9207 ) ;
#6842=DIRECTION ( 'NONE',  ( 0.000000000000000000, 0.000000000000000000, 1.000000000000000000 ) ) ;
#6843=AXIS2_PLACEMENT_3D ( 'NONE', #8939, #610, #11806 ) ;
#6844=VERTEX_POINT ( 'NONE', #11582 ) ;
#6845=AXIS2_PLACEMENT_3D ( 'NONE', #7042, #6201, #1546 ) ;
#6846=DIRECTION ( 'NONE',  ( -1.000000000000000000, -0.000000000000000000, -0.000000000000000000 ) ) ;
#6847=CARTESIAN_POINT ( 'NONE',  ( 1.500000000000000444, -17.35216073792428304, -17.71842311621547594 ) ) ;
#6849=VERTEX_POINT ( 'NONE', #3311 ) ;
#6851=CARTESIAN_POINT ( 'NONE',  ( 50.00005079999999680, 0.000000000000000000, 0.000000000000000000 ) ) ;
#6852=CIRCLE ( 'NONE', #3348, 9.599999999999997868 ) ;
#6853=CIRCLE ( 'NONE', #1586, 9.599999999999996092 ) ;
#6854=DIRECTION ( 'NONE',  ( -1.000000000000000000, -0.000000000000000000, 0.000000000000000000 ) ) ;
#6855=CIRCLE ( 'NONE', #605, 22.99900000000000233 ) ;
#6856=VERTEX_POINT ( 'NONE', #372 ) ;
#6858=CARTESIAN_POINT ( 'NONE',  ( 3.000000000000000888, 6.779701584703024864, -21.97702544527750845 ) ) ;
#6860=CARTESIAN_POINT ( 'NONE',  ( 0.000000000000000000, 0.000000000000000000, 0.000000000000000000 ) ) ;
#6861=AXIS2_PLACEMENT_3D ( 'NONE', #11481, #9522, #9759 ) ;
#6862=CARTESIAN_POINT ( 'NONE',  ( 3.000000000000000888, 0.000000000000000000, 0.000000000000000000 ) ) ;
#6864=CIRCLE ( 'NONE', #2765, 24.80000000000000071 ) ;
#6865=FACE_OUTER_BOUND ( 'NONE', #4437, .T. ) ;
#6866=DIRECTION ( 'NONE',  ( 0.000000000000000000, 0.000000000000000000, 1.000000000000000000 ) ) ;
#6867=LINE ( 'NONE', #5844, #10948 ) ;
#6868=CIRCLE ( 'NONE', #4329, 9.599999999999997868 ) ;
#6869=EDGE_LOOP ( 'NONE', ( #2675, #7272, #6984, #11942 ) ) ;
#6870=EDGE_CURVE ( 'NONE', #2802, #401, #2464, .T. ) ;
#6871=ORIENTED_EDGE ( 'NONE', *, *, #1520, .T. ) ;
#6872=ORIENTED_EDGE ( 'NONE', *, *, #10097, .F. ) ;
#6873=DIRECTION ( 'NONE',  ( -1.000000000000000000, -0.000000000000000000, 0.000000000000000000 ) ) ;
#6875=EDGE_CURVE ( 'NONE', #10349, #10186, #10873, .T. ) ;
#6877=ADVANCED_FACE ( 'NONE', ( #3252 ), #6134, .T. ) ;
#6878=CIRCLE ( 'NONE', #10204, 9.599999999999999645 ) ;
#6882=EDGE_CURVE ( 'NONE', #6658, #8357, #11644, .T. ) ;
#6883=CARTESIAN_POINT ( 'NONE',  ( 0.000000000000000000, -17.71842311621518462, -17.35216073792458857 ) ) ;
#6884=DIRECTION ( 'NONE',  ( 0.000000000000000000, 0.000000000000000000, 1.000000000000000000 ) ) ;
#6885=VERTEX_POINT ( 'NONE', #9800 ) ;
#6886=ORIENTED_EDGE ( 'NONE', *, *, #5957, .F. ) ;
#6887=ORIENTED_EDGE ( 'NONE', *, *, #3040, .T. ) ;
#6888=CARTESIAN_POINT ( 'NONE',  ( 3.000000000000000888, -16.85990652506889376, -15.64281154287614584 ) ) ;
#6889=AXIS2_PLACEMENT_3D ( 'NONE', #9400, #10199, #33 ) ;
#6890=CARTESIAN_POINT ( 'NONE',  ( 3.000000000000000888, 0.000000000000000000, 0.000000000000000000 ) ) ;
#6891=CARTESIAN_POINT ( 'NONE',  ( 3.000000000000000000, 0.000000000000000000, 0.000000000000000000 ) ) ;
#6892=VECTOR ( 'NONE', #10607, 1000.000000000000000 ) ;
#6893=DIRECTION ( 'NONE',  ( 0.000000000000000000, -0.7431448254773862505, -0.6691306063588672304 ) ) ;
#6895=FACE_OUTER_BOUND ( 'NONE', #6352, .T. ) ;
#6896=VERTEX_POINT ( 'NONE', #8888 ) ;
#6897=ORIENTED_EDGE ( 'NONE', *, *, #8826, .T. ) ;
#6901=ORIENTED_EDGE ( 'NONE', *, *, #444, .T. ) ;
#6903=FACE_OUTER_BOUND ( 'NONE', #8571, .T. ) ;
#6904=EDGE_CURVE ( 'NONE', #10278, #1309, #9690, .T. ) ;
#6905=AXIS2_PLACEMENT_3D ( 'NONE', #8817, #7765, #1285 ) ;
#6906=DIRECTION ( 'NONE',  ( -1.000000000000000000, 0.000000000000000000, 0.000000000000000000 ) ) ;
#6907=ORIENTED_EDGE ( 'NONE', *, *, #2288, .F. ) ;
#6908=CARTESIAN_POINT ( 'NONE',  ( 3.000000000000000888, 3.623565124517435176, -24.53384959170454138 ) ) ;
#6909=CARTESIAN_POINT ( 'NONE',  ( 3.000000000000000888, 15.42759117534385993, 16.45023496161670451 ) ) ;
#6911=VERTEX_POINT ( 'NONE', #3379 ) ;
#6912=EDGE_CURVE ( 'NONE', #10809, #5848, #6430, .T. ) ;
#6913=CARTESIAN_POINT ( 'NONE',  ( 0.000000000000000000, -13.28910708463113721, -20.93895013827595264 ) ) ;
#6914=CIRCLE ( 'NONE', #460, 24.80000000000000071 ) ;
#6915=DIRECTION ( 'NONE',  ( 0.000000000000000000, 0.7431448254773955764, -0.6691306063588569053 ) ) ;
#6916=VERTEX_POINT ( 'NONE', #680 ) ;
#6918=DIRECTION ( 'NONE',  ( -1.000000000000000000, 0.000000000000000000, 0.000000000000000000 ) ) ;
#6919=AXIS2_PLACEMENT_3D ( 'NONE', #10902, #8148, #11819 ) ;
#6920=CARTESIAN_POINT ( 'NONE',  ( 0.000000000000000000, -17.35216073792452107, 17.71842311621524146 ) ) ;
#6921=EDGE_CURVE ( 'NONE', #3750, #4226, #4411, .T. ) ;
#6922=CYLINDRICAL_SURFACE ( 'NONE', #4979, 9.599999999999997868 ) ;
#6925=CYLINDRICAL_SURFACE ( 'NONE', #3977, 22.99899999999999878 ) ;
#6926=CARTESIAN_POINT ( 'NONE',  ( 3.000000000000000888, 0.000000000000000000, 0.000000000000000000 ) ) ;
#6927=VERTEX_POINT ( 'NONE', #798 ) ;
#6928=DIRECTION ( 'NONE',  ( 0.000000000000000000, -0.3090169943749349057, -0.9510565162951577500 ) ) ;
#6929=ORIENTED_EDGE ( 'NONE', *, *, #4263, .F. ) ;
#6931=CARTESIAN_POINT ( 'NONE',  ( 3.000000000000000888, 0.000000000000000000, 0.000000000000000000 ) ) ;
#6934=AXIS2_PLACEMENT_3D ( 'NONE', #7971, #11705, #11595 ) ;
#6936=FACE_OUTER_BOUND ( 'NONE', #6082, .T. ) ;
#6937=CARTESIAN_POINT ( 'NONE',  ( 3.000000000000000888, 2.062268319295562424, 22.90635393027947231 ) ) ;
#6938=ORIENTED_EDGE ( 'NONE', *, *, #9304, .F. ) ;
#6939=VERTEX_POINT ( 'NONE', #10842 ) ;
#6940=EDGE_CURVE ( 'NONE', #6916, #6856, #3640, .T. ) ;
#6941=EDGE_LOOP ( 'NONE', ( #1754, #11020, #10365, #2623 ) ) ;
#6943=ADVANCED_FACE ( 'NONE', ( #11870 ), #4540, .T. ) ;
#6945=CARTESIAN_POINT ( 'NONE',  ( 8.000000000000000000, 0.000000000000000000, 0.000000000000000000 ) ) ;
#6947=CIRCLE ( 'NONE', #9897, 24.80000000000000071 ) ;
#6948=EDGE_CURVE ( 'NONE', #490, #8778, #5979, .T. ) ;
#6949=CARTESIAN_POINT ( 'NONE',  ( 3.000000000000000888, -7.402892494506152943, -21.30300407174369681 ) ) ;
#6951=ORIENTED_EDGE ( 'NONE', *, *, #1621, .F. ) ;
#6955=DIRECTION ( 'NONE',  ( -1.000000000000000000, 0.000000000000000000, 0.000000000000000000 ) ) ;
#6956=CARTESIAN_POINT ( 'NONE',  ( 3.000000000000000888, 0.000000000000000000, 0.000000000000000000 ) ) ;
#6957=CARTESIAN_POINT ( 'NONE',  ( 3.000000000000000888, 0.4575788569254873317, -22.54798042742717712 ) ) ;
#6958=AXIS2_PLACEMENT_3D ( 'NONE', #8070, #9163, #1701 ) ;
#6960=DIRECTION ( 'NONE',  ( -1.000000000000000000, 0.000000000000000000, 0.000000000000000000 ) ) ;
#6961=ADVANCED_FACE ( 'NONE', ( #10095 ), #8205, .T. ) ;
#6962=DIRECTION ( 'NONE',  ( -1.000000000000000000, -0.000000000000000000, -0.000000000000000000 ) ) ;
#6965=ADVANCED_FACE ( 'NONE', ( #3500 ), #7334, .T. ) ;
#6966=CARTESIAN_POINT ( 'NONE',  ( 0.000000000000000000, 19.10918332567958089, 15.80756504416697439 ) ) ;
#6967=VERTEX_POINT ( 'NONE', #9004 ) ;
#6968=CYLINDRICAL_SURFACE ( 'NONE', #4133, 22.99899999999999878 ) ;
#6969=ORIENTED_EDGE ( 'NONE', *, *, #4943, .F. ) ;
#6971=ORIENTED_EDGE ( 'NONE', *, *, #8542, .F. ) ;
#6972=DIRECTION ( 'NONE',  ( 0.000000000000000000, 0.4067366430758009299, -0.9135454576426005335 ) ) ;
#6974=ORIENTED_EDGE ( 'NONE', *, *, #9281, .T. ) ;
#6975=CARTESIAN_POINT ( 'NONE',  ( 0.000000000000000000, -6.779701584702581663, -21.97702544527764701 ) ) ;
#6976=LINE ( 'NONE', #11085, #2831 ) ;
#6978=AXIS2_PLACEMENT_3D ( 'NONE', #7416, #8410, #9381 ) ;
#6979=CARTESIAN_POINT ( 'NONE',  ( 3.000000000000000888, -24.53384959170455204, -3.623565124517360569 ) ) ;
#6981=EDGE_CURVE ( 'NONE', #2610, #10797, #2452, .T. ) ;
#6982=CARTESIAN_POINT ( 'NONE',  ( 3.000000000000000888, -15.40502424595132247, -19.43515443678418819 ) ) ;
#6983=DIRECTION ( 'NONE',  ( -1.000000000000000000, -0.000000000000000000, 0.000000000000000000 ) ) ;
#6984=ORIENTED_EDGE ( 'NONE', *, *, #9761, .F. ) ;
#6985=VECTOR ( 'NONE', #3876, 1000.000000000000000 ) ;
#6986=CYLINDRICAL_SURFACE ( 'NONE', #896, 24.80000000000000071 ) ;
#6987=VERTEX_POINT ( 'NONE', #6252 ) ;
#6988=EDGE_CURVE ( 'NONE', #11921, #11607, #10476, .T. ) ;
#6990=CARTESIAN_POINT ( 'NONE',  ( 3.000000000000000000, 2.265596578422603002E-15, -18.49999999999999645 ) ) ;
#6994=CARTESIAN_POINT ( 'NONE',  ( 3.000000000000000888, -6.668524164681463695, -23.88662356770122130 ) ) ;
#6995=ORIENTED_EDGE ( 'NONE', *, *, #8688, .F. ) ;
#6996=AXIS2_PLACEMENT_3D ( 'NONE', #3592, #9150, #2613 ) ;
#6997=EDGE_LOOP ( 'NONE', ( #7121, #9899, #11153, #10743 ) ) ;
#6998=ORIENTED_EDGE ( 'NONE', *, *, #10919, .F. ) ;
#6999=CARTESIAN_POINT ( 'NONE',  ( 1.499999999999999556, -24.75110766671651064, -1.556492618230889580 ) ) ;
#7000=CARTESIAN_POINT ( 'NONE',  ( 0.000000000000000000, -13.72351598154911478, 20.65684170206487025 ) ) ;
#7001=CARTESIAN_POINT ( 'NONE',  ( 0.000000000000000000, 18.80635025205170052, 13.23915371906961802 ) ) ;
#7003=DIRECTION ( 'NONE',  ( -1.000000000000000000, 0.000000000000000000, 0.000000000000000000 ) ) ;
#7004=EDGE_CURVE ( 'NONE', #1445, #3234, #2514, .T. ) ;
#7005=EDGE_CURVE ( 'NONE', #9959, #1167, #7151, .T. ) ;
#7006=CYLINDRICAL_SURFACE ( 'NONE', #6636, 9.599999999999997868 ) ;
#7007=VECTOR ( 'NONE', #4643, 1000.000000000000000 ) ;
#7008=ORIENTED_EDGE ( 'NONE', *, *, #9874, .T. ) ;
#7009=EDGE_LOOP ( 'NONE', ( #5189, #2484, #6995, #10973 ) ) ;
#7011=VERTEX_POINT ( 'NONE', #1602 ) ;
#7012=EDGE_CURVE ( 'NONE', #110, #9064, #7344, .T. ) ;
#7013=CARTESIAN_POINT ( 'NONE',  ( 0.000000000000000000, 0.000000000000000000, 0.000000000000000000 ) ) ;
#7014=CYLINDRICAL_SURFACE ( 'NONE', #4364, 18.49999999999999645 ) ;
#7015=CARTESIAN_POINT ( 'NONE',  ( 3.000000000000000888, 22.56530478845649057, 4.445336973060936891 ) ) ;
#7016=ORIENTED_EDGE ( 'NONE', *, *, #1168, .T. ) ;
#7017=CIRCLE ( 'NONE', #6449, 24.80000000000000071 ) ;
#7018=EDGE_CURVE ( 'NONE', #7573, #7873, #8342, .T. ) ;
#7019=CARTESIAN_POINT ( 'NONE',  ( 0.000000000000000000, 0.000000000000000000, 0.000000000000000000 ) ) ;
#7020=EDGE_CURVE ( 'NONE', #4653, #8232, #3462, .T. ) ;
#7021=AXIS2_PLACEMENT_3D ( 'NONE', #9813, #745, #6146 ) ;
#7022=LINE ( 'NONE', #10769, #6681 ) ;
#7024=EDGE_CURVE ( 'NONE', #4404, #67, #7937, .T. ) ;
#7025=ORIENTED_EDGE ( 'NONE', *, *, #11435, .F. ) ;
#7026=DIRECTION ( 'NONE',  ( 0.000000000000000000, 0.1045284632676538872, -0.9945218953682732899 ) ) ;
#7027=DIRECTION ( 'NONE',  ( -1.000000000000000000, -0.000000000000000000, 0.000000000000000000 ) ) ;
#7029=EDGE_LOOP ( 'NONE', ( #10532, #2483, #6161, #7780 ) ) ;
#7031=AXIS2_PLACEMENT_3D ( 'NONE', #10531, #6738, #6915 ) ;
#7032=ORIENTED_EDGE ( 'NONE', *, *, #5328, .T. ) ;
#7033=CARTESIAN_POINT ( 'NONE',  ( 0.000000000000000000, -8.753070780933295936, 20.78471918669858098 ) ) ;
#7035=ORIENTED_EDGE ( 'NONE', *, *, #4897, .T. ) ;
#7037=DIRECTION ( 'NONE',  ( -1.000000000000000000, -0.000000000000000000, 0.000000000000000000 ) ) ;
#7039=DIRECTION ( 'NONE',  ( -1.000000000000000000, 0.000000000000000000, 0.000000000000000000 ) ) ;
#7041=CARTESIAN_POINT ( 'NONE',  ( 0.000000000000000000, 10.87771529938188486, -19.75591328264875202 ) ) ;
#7042=CARTESIAN_POINT ( 'NONE',  ( 3.000000000000000888, 0.000000000000000000, 0.000000000000000000 ) ) ;
#7043=EDGE_LOOP ( 'NONE', ( #11782, #9472, #3072, #1612 ) ) ;
#7044=CIRCLE ( 'NONE', #5102, 24.80000000000000071 ) ;
#7046=ORIENTED_EDGE ( 'NONE', *, *, #1865, .F. ) ;
#7047=VECTOR ( 'NONE', #8043, 1000.000000000000000 ) ;
#7048=EDGE_CURVE ( 'NONE', #1491, #10316, #6666, .T. ) ;
#7049=FACE_OUTER_BOUND ( 'NONE', #2387, .T. ) ;
#7050=DIRECTION ( 'NONE',  ( 0.000000000000000000, 0.000000000000000000, 1.000000000000000000 ) ) ;
#7057=EDGE_CURVE ( 'NONE', #5430, #8902, #5817, .T. ) ;
#7058=AXIS2_PLACEMENT_3D ( 'NONE', #7144, #427, #1527 ) ;
#7059=VERTEX_POINT ( 'NONE', #8391 ) ;
#7060=ORIENTED_EDGE ( 'NONE', *, *, #11305, .T. ) ;
#7062=AXIS2_PLACEMENT_3D ( 'NONE', #4042, #1287, #2142 ) ;
#7063=FACE_OUTER_BOUND ( 'NONE', #11219, .T. ) ;
#7064=DIRECTION ( 'NONE',  ( -1.000000000000000000, -0.000000000000000000, 0.000000000000000000 ) ) ;
#7065=CIRCLE ( 'NONE', #4939, 22.99899999999999523 ) ;
#7067=DIRECTION ( 'NONE',  ( -1.000000000000000000, -0.000000000000000000, 0.000000000000000000 ) ) ;
#7068=DIRECTION ( 'NONE',  ( -1.000000000000000000, -0.000000000000000000, 0.000000000000000000 ) ) ;
#7069=ORIENTED_EDGE ( 'NONE', *, *, #5160, .T. ) ;
#7070=ORIENTED_EDGE ( 'NONE', *, *, #299, .F. ) ;
#7072=ORIENTED_EDGE ( 'NONE', *, *, #11726, .F. ) ;
#7073=DIRECTION ( 'NONE',  ( -1.000000000000000000, 0.000000000000000000, -0.000000000000000000 ) ) ;
#7074=DIRECTION ( 'NONE',  ( 1.000000000000000000, 0.000000000000000000, 0.000000000000000000 ) ) ;
#7075=CARTESIAN_POINT ( 'NONE',  ( 0.000000000000000000, 15.64281154287597353, 16.85990652506905363 ) ) ;
#7077=CARTESIAN_POINT ( 'NONE',  ( 3.000000000000000888, 19.74380051311539930, 11.79560690673879186 ) ) ;
#7078=ORIENTED_EDGE ( 'NONE', *, *, #2920, .F. ) ;
#7079=CIRCLE ( 'NONE', #1239, 9.599999999999996092 ) ;
#7080=CARTESIAN_POINT ( 'NONE',  ( 0.000000000000000000, 22.54798042742717712, 0.4575788569255671012 ) ) ;
#7081=DIRECTION ( 'NONE',  ( 0.000000000000000000, 0.000000000000000000, 1.000000000000000000 ) ) ;
#7084=AXIS2_PLACEMENT_3D ( 'NONE', #4777, #8515, #11321 ) ;
#7085=CARTESIAN_POINT ( 'NONE',  ( 3.000000000000000888, -21.76479567747246691, 7.432877647175128999 ) ) ;
#7087=VERTEX_POINT ( 'NONE', #4724 ) ;
#7088=ADVANCED_FACE ( 'NONE', ( #12113 ), #8332, .T. ) ;
#7091=EDGE_CURVE ( 'NONE', #8051, #7087, #922, .T. ) ;
#7092=VERTEX_POINT ( 'NONE', #11140 ) ;
#7093=DIRECTION ( 'NONE',  ( 0.000000000000000000, 0.000000000000000000, 1.000000000000000000 ) ) ;
#7094=EDGE_LOOP ( 'NONE', ( #7928, #4969, #8953, #3394 ) ) ;
#7095=EDGE_CURVE ( 'NONE', #35, #5430, #4818, .T. ) ;
#7096=CARTESIAN_POINT ( 'NONE',  ( 0.000000000000000000, -22.15038895030646060, -4.240409074144325885 ) ) ;
#7097=DIRECTION ( 'NONE',  ( -1.000000000000000000, 0.000000000000000000, 0.000000000000000000 ) ) ;
#7099=CIRCLE ( 'NONE', #1839, 22.99899999999999878 ) ;
#7100=CYLINDRICAL_SURFACE ( 'NONE', #8046, 22.99899999999999878 ) ;
#7102=CARTESIAN_POINT ( 'NONE',  ( 3.000000000000000888, 0.000000000000000000, 0.000000000000000000 ) ) ;
#7104=DIRECTION ( 'NONE',  ( -1.000000000000000000, 0.000000000000000000, 0.000000000000000000 ) ) ;
#7105=VERTEX_POINT ( 'NONE', #12054 ) ;
#7106=ADVANCED_FACE ( 'NONE', ( #57 ), #8574, .T. ) ;
#7107=DIRECTION ( 'NONE',  ( 0.000000000000000000, -0.5000000000000072164, 0.8660254037844345998 ) ) ;
#7109=SURFACE_STYLE_USAGE ( .BOTH. , #6333 ) ;
#7110=ORIENTED_EDGE ( 'NONE', *, *, #2922, .T. ) ;
#7111=CARTESIAN_POINT ( 'NONE',  ( 8.000000000000000000, 0.000000000000000000, 18.49999999999999645 ) ) ;
#7113=CARTESIAN_POINT ( 'NONE',  ( 3.000000000000000888, -19.10918332567947076, -15.80756504416710229 ) ) ;
#7114=EDGE_CURVE ( 'NONE', #6489, #3556, #912, .T. ) ;
#7116=AXIS2_PLACEMENT_3D ( 'NONE', #3444, #5520, #738 ) ;
#7117=CARTESIAN_POINT ( 'NONE',  ( 0.000000000000000000, -18.40266524480579236, -13.79477846460815194 ) ) ;
#7118=VERTEX_POINT ( 'NONE', #1103 ) ;
#7120=EDGE_LOOP ( 'NONE', ( #7744, #7980, #6192, #10727 ) ) ;
#7121=ORIENTED_EDGE ( 'NONE', *, *, #767, .T. ) ;
#7122=EDGE_CURVE ( 'NONE', #4609, #6489, #6574, .T. ) ;
#7124=CARTESIAN_POINT ( 'NONE',  ( 3.000000000000000888, 2.745295967525994918, 22.83456483164690098 ) ) ;
#7125=DIRECTION ( 'NONE',  ( 0.000000000000000000, 0.000000000000000000, 1.000000000000000000 ) ) ;
#7128=CARTESIAN_POINT ( 'NONE',  ( 0.000000000000000000, 0.000000000000000000, 0.000000000000000000 ) ) ;
#7129=CYLINDRICAL_SURFACE ( 'NONE', #2141, 9.599999999999997868 ) ;
#7130=ORIENTED_EDGE ( 'NONE', *, *, #9751, .F. ) ;
#7131=ORIENTED_EDGE ( 'NONE', *, *, #4834, .T. ) ;
#7132=AXIS2_PLACEMENT_3D ( 'NONE', #8847, #2287, #9695 ) ;
#7135=CARTESIAN_POINT ( 'NONE',  ( 3.000000000000000888, 20.86861857134734421, 9.667200211209893368 ) ) ;
#7136=DIRECTION ( 'NONE',  ( 0.000000000000000000, 0.9945218953682737340, -0.1045284632676502651 ) ) ;
#7137=DIRECTION ( 'NONE',  ( -1.000000000000000000, 0.000000000000000000, -0.000000000000000000 ) ) ;
#7138=ORIENTED_EDGE ( 'NONE', *, *, #4953, .T. ) ;
#7139=EDGE_CURVE ( 'NONE', #5674, #12055, #11210, .T. ) ;
#7140=DIRECTION ( 'NONE',  ( 0.000000000000000000, -0.4999999999999887867, -0.8660254037844449249 ) ) ;
#7141=AXIS2_PLACEMENT_3D ( 'NONE', #10353, #8654, #4739 ) ;
#7142=CARTESIAN_POINT ( 'NONE',  ( 3.000000000000000888, 5.135568396240030253, 21.96011696265493285 ) ) ;
#7144=CARTESIAN_POINT ( 'NONE',  ( 0.000000000000000000, -0.4575788569253416149, 22.54798042742717712 ) ) ;
#7145=CYLINDRICAL_SURFACE ( 'NONE', #9596, 9.599999999999997868 ) ;
#7147=ORIENTED_EDGE ( 'NONE', *, *, #2427, .F. ) ;
#7148=VECTOR ( 'NONE', #7644, 1000.000000000000000 ) ;
#7150=VERTEX_POINT ( 'NONE', #9366 ) ;
#7151=LINE ( 'NONE', #6193, #2871 ) ;
#7152=EDGE_CURVE ( 'NONE', #5430, #10713, #5986, .T. ) ;
#7154=CARTESIAN_POINT ( 'NONE',  ( 0.000000000000000000, 0.000000000000000000, 0.000000000000000000 ) ) ;
#7156=LINE ( 'NONE', #10668, #1801 ) ;
#7158=CARTESIAN_POINT ( 'NONE',  ( 3.000000000000000888, -4.445336973061013275, 22.56530478845647991 ) ) ;
#7159=ORIENTED_EDGE ( 'NONE', *, *, #10840, .F. ) ;
#7160=ADVANCED_FACE ( 'NONE', ( #1900 ), #2882, .T. ) ;
#7161=ORIENTED_EDGE ( 'NONE', *, *, #8065, .F. ) ;
#7162=EDGE_CURVE ( 'NONE', #6372, #1694, #1958, .T. ) ;
#7163=DIRECTION ( 'NONE',  ( -1.000000000000000000, -0.000000000000000000, 0.000000000000000000 ) ) ;
#7164=ORIENTED_EDGE ( 'NONE', *, *, #7867, .F. ) ;
#7166=CARTESIAN_POINT ( 'NONE',  ( 3.000000000000000888, -21.76479567747236743, -7.432877647175426539 ) ) ;
#7167=SURFACE_STYLE_FILL_AREA ( #3400 ) ;
#7168=ORIENTED_EDGE ( 'NONE', *, *, #466, .T. ) ;
#7169=CIRCLE ( 'NONE', #729, 24.80000000000000071 ) ;
#7170=DIRECTION ( 'NONE',  ( 0.000000000000000000, 0.000000000000000000, 1.000000000000000000 ) ) ;
#7171=CARTESIAN_POINT ( 'NONE',  ( 3.000000000000000888, -20.41249101028218149, 9.589108953447823325 ) ) ;
#7172=DIRECTION ( 'NONE',  ( 0.000000000000000000, -0.9135454576425964257, -0.4067366430758103668 ) ) ;
#7174=EDGE_CURVE ( 'NONE', #9646, #9620, #7746, .T. ) ;
#7176=CARTESIAN_POINT ( 'NONE',  ( 8.000000000000000000, 0.000000000000000000, 18.49999999999999645 ) ) ;
#7177=ADVANCED_FACE ( 'NONE', ( #5877 ), #2201, .T. ) ;
#7180=ORIENTED_EDGE ( 'NONE', *, *, #3112, .F. ) ;
#7182=LINE ( 'NONE', #6221, #6031 ) ;
#7183=CARTESIAN_POINT ( 'NONE',  ( 0.000000000000000000, -23.88662356770119644, 6.668524164681547184 ) ) ;
#7184=CIRCLE ( 'NONE', #7970, 9.599999999999997868 ) ;
#7185=EDGE_CURVE ( 'NONE', #4549, #3254, #5942, .T. ) ;
#7187=CARTESIAN_POINT ( 'NONE',  ( 3.000000000000000888, 6.779701584702736206, 21.97702544527760082 ) ) ;
#7188=LINE ( 'NONE', #11004, #8984 ) ;
#7189=ORIENTED_EDGE ( 'NONE', *, *, #7004, .F. ) ;
#7190=ORIENTED_EDGE ( 'NONE', *, *, #3339, .F. ) ;
#7191=VERTEX_POINT ( 'NONE', #6052 ) ;
#7192=DIRECTION ( 'NONE',  ( 0.000000000000000000, 0.4999999999999950040, 0.8660254037844415942 ) ) ;
#7193=AXIS2_PLACEMENT_3D ( 'NONE', #236, #3981, #417 ) ;
#7194=CIRCLE ( 'NONE', #1537, 22.99899999999999878 ) ;
#7195=CARTESIAN_POINT ( 'NONE',  ( 3.000000000000000888, 0.000000000000000000, 0.000000000000000000 ) ) ;
#7196=UNCERTAINTY_MEASURE_WITH_UNIT (LENGTH_MEASURE( 1.000000000000000082E-05 ), #3634, 'distance_accuracy_value', 'NONE');
#7197=CARTESIAN_POINT ( 'NONE',  ( -10.00000000000000000, 0.000000000000000000, 0.000000000000000000 ) ) ;
#7198=VERTEX_POINT ( 'NONE', #4164 ) ;
#7199=EDGE_CURVE ( 'NONE', #4173, #9819, #318, .T. ) ;
#7200=DIRECTION ( 'NONE',  ( -1.000000000000000000, -0.000000000000000000, -0.000000000000000000 ) ) ;
#7201=DIRECTION ( 'NONE',  ( 0.000000000000000000, 0.000000000000000000, -1.000000000000000000 ) ) ;
#7203=AXIS2_PLACEMENT_3D ( 'NONE', #9961, #11912, #1582 ) ;
#7204=CIRCLE ( 'NONE', #1941, 9.599999999999999645 ) ;
#7206=DIRECTION ( 'NONE',  ( 1.000000000000000000, 0.000000000000000000, 0.000000000000000000 ) ) ;
#7207=EDGE_CURVE ( 'NONE', #1101, #10684, #8736, .T. ) ;
#7208=ORIENTED_EDGE ( 'NONE', *, *, #10122, .F. ) ;
#7209=ORIENTED_EDGE ( 'NONE', *, *, #2385, .F. ) ;
#7211=AXIS2_PLACEMENT_3D ( 'NONE', #908, #2004, #965 ) ;
#7212=VERTEX_POINT ( 'NONE', #355 ) ;
#7213=CARTESIAN_POINT ( 'NONE',  ( 0.000000000000000000, 0.000000000000000000, 0.000000000000000000 ) ) ;
#7214=EDGE_LOOP ( 'NONE', ( #10263, #3573, #8990, #12092 ) ) ;
#7215=AXIS2_PLACEMENT_3D ( 'NONE', #6597, #6717, #10453 ) ;
#7216=DIRECTION ( 'NONE',  ( 0.000000000000000000, 0.000000000000000000, 1.000000000000000000 ) ) ;
#7217=CARTESIAN_POINT ( 'NONE',  ( 1.499999999999999556, -1.556492618230471692, -24.75110766671653906 ) ) ;
#7219=DIRECTION ( 'NONE',  ( -1.000000000000000000, 0.000000000000000000, 0.000000000000000000 ) ) ;
#7220=AXIS2_PLACEMENT_3D ( 'NONE', #9144, #9389, #1736 ) ;
#7221=CARTESIAN_POINT ( 'NONE',  ( 0.000000000000000000, 22.54798042742718067, -0.4575788569252652871 ) ) ;
#7222=ORIENTED_EDGE ( 'NONE', *, *, #3523, .F. ) ;
#7224=CIRCLE ( 'NONE', #9388, 24.80000000000000071 ) ;
#7227=CARTESIAN_POINT ( 'NONE',  ( -10.00000000000000000, 0.000000000000000000, 0.000000000000000000 ) ) ;
#7228=EDGE_LOOP ( 'NONE', ( #5332, #2246, #11082, #9374 ) ) ;
#7230=AXIS2_PLACEMENT_3D ( 'NONE', #5507, #7572, #5868 ) ;
#7231=CARTESIAN_POINT ( 'NONE',  ( 0.000000000000000000, 0.000000000000000000, 0.000000000000000000 ) ) ;
#7235=CARTESIAN_POINT ( 'NONE',  ( 0.000000000000000000, 13.72351598154897268, 20.65684170206496262 ) ) ;
#7236=DIRECTION ( 'NONE',  ( -1.000000000000000000, 0.000000000000000000, -0.000000000000000000 ) ) ;
#7237=EDGE_CURVE ( 'NONE', #7440, #12091, #297, .T. ) ;
#7238=ORIENTED_EDGE ( 'NONE', *, *, #5583, .F. ) ;
#7239=AXIS2_PLACEMENT_3D ( 'NONE', #11245, #11057, #5670 ) ;
#7240=AXIS2_PLACEMENT_3D ( 'NONE', #10414, #6004, #9495 ) ;
#7241=ORIENTED_EDGE ( 'NONE', *, *, #9355, .T. ) ;
#7245=DIRECTION ( 'NONE',  ( 0.000000000000000000, 1.000000000000000000, 3.491481338843133355E-15 ) ) ;
#7246=CIRCLE ( 'NONE', #8801, 24.80000000000000071 ) ;
#7248=CARTESIAN_POINT ( 'NONE',  ( 0.000000000000000000, 0.000000000000000000, 0.000000000000000000 ) ) ;
#7249=DIRECTION ( 'NONE',  ( -1.000000000000000000, -0.000000000000000000, -0.000000000000000000 ) ) ;
#7250=ORIENTED_EDGE ( 'NONE', *, *, #7955, .F. ) ;
#7251=VERTEX_POINT ( 'NONE', #5071 ) ;
#7253=AXIS2_PLACEMENT_3D ( 'NONE', #8950, #3446, #8837 ) ;
#7254=ORIENTED_EDGE ( 'NONE', *, *, #3326, .F. ) ;
#7255=CARTESIAN_POINT ( 'NONE',  ( 8.000000000000000000, 2.449293598294706119E-15, -19.99999999999999645 ) ) ;
#7256=AXIS2_PLACEMENT_3D ( 'NONE', #304, #11504, #3127 ) ;
#7257=LINE ( 'NONE', #8988, #12101 ) ;
#7258=LINE ( 'NONE', #11980, #3281 ) ;
#7260=CARTESIAN_POINT ( 'NONE',  ( 3.000000000000000888, 11.67026512804547345, 19.29833442572363822 ) ) ;
#7262=CIRCLE ( 'NONE', #8259, 9.599999999999997868 ) ;
#7263=EDGE_CURVE ( 'NONE', #9548, #11784, #7946, .T. ) ;
#7264=CARTESIAN_POINT ( 'NONE',  ( 3.000000000000000888, 21.58580335785676496, 6.532525787311040943 ) ) ;
#7265=VERTEX_POINT ( 'NONE', #3237 ) ;
#7266=DIRECTION ( 'NONE',  ( -1.000000000000000000, -0.000000000000000000, 0.000000000000000000 ) ) ;
#7267=ORIENTED_EDGE ( 'NONE', *, *, #5312, .F. ) ;
#7268=EDGE_CURVE ( 'NONE', #5236, #6096, #6947, .T. ) ;
#7269=ORIENTED_EDGE ( 'NONE', *, *, #10878, .F. ) ;
#7271=CIRCLE ( 'NONE', #4762, 22.99899999999999523 ) ;
#7272=ORIENTED_EDGE ( 'NONE', *, *, #2658, .F. ) ;
#7273=DIRECTION ( 'NONE',  ( -1.000000000000000000, 0.000000000000000000, -0.000000000000000000 ) ) ;
#7275=DIRECTION ( 'NONE',  ( -1.000000000000000000, 0.000000000000000000, -0.000000000000000000 ) ) ;
#7276=AXIS2_PLACEMENT_3D ( 'NONE', #5657, #9387, #5726 ) ;
#7278=CARTESIAN_POINT ( 'NONE',  ( 3.000000000000000888, 0.000000000000000000, 0.000000000000000000 ) ) ;
#7280=CARTESIAN_POINT ( 'NONE',  ( 3.000000000000000888, 0.4575788569251889593, 22.54798042742718067 ) ) ;
#7281=DIRECTION ( 'NONE',  ( -1.000000000000000000, 0.000000000000000000, 0.000000000000000000 ) ) ;
#7282=AXIS2_PLACEMENT_3D ( 'NONE', #2502, #4399, #3367 ) ;
#7283=ORIENTED_EDGE ( 'NONE', *, *, #5617, .T. ) ;
#7284=CARTESIAN_POINT ( 'NONE',  ( 3.000000000000000888, 5.117118920208487687, 22.42251312757881365 ) ) ;
#7285=ORIENTED_EDGE ( 'NONE', *, *, #8539, .T. ) ;
#7286=AXIS2_PLACEMENT_3D ( 'NONE', #7708, #11441, #477 ) ;
#7288=CARTESIAN_POINT ( 'NONE',  ( 3.000000000000000888, -17.97274125076064877, -13.62355943574037731 ) ) ;
#7289=ORIENTED_EDGE ( 'NONE', *, *, #5232, .T. ) ;
#7291=DIRECTION ( 'NONE',  ( -1.000000000000000000, 0.000000000000000000, -0.000000000000000000 ) ) ;
#7292=CYLINDRICAL_SURFACE ( 'NONE', #1257, 22.99899999999999878 ) ;
#7295=CARTESIAN_POINT ( 'NONE',  ( 3.000000000000000888, 4.240409074144097623, 22.15038895030650679 ) ) ;
#7296=FACE_OUTER_BOUND ( 'NONE', #3118, .T. ) ;
#7297=ORIENTED_EDGE ( 'NONE', *, *, #3011, .F. ) ;
#7298=AXIS2_PLACEMENT_3D ( 'NONE', #9754, #1495, #3332 ) ;
#7299=ORIENTED_EDGE ( 'NONE', *, *, #4197, .T. ) ;
#7301=DIRECTION ( 'NONE',  ( 1.000000000000000000, 0.000000000000000000, 0.000000000000000000 ) ) ;
#7302=DIRECTION ( 'NONE',  ( -1.000000000000000000, 0.000000000000000000, 0.000000000000000000 ) ) ;
#7303=AXIS2_PLACEMENT_3D ( 'NONE', #9325, #11228, #2098 ) ;
#7304=CARTESIAN_POINT ( 'NONE',  ( 0.000000000000000000, -11.02759168516730703, -22.21333432029575050 ) ) ;
#7306=ORIENTED_EDGE ( 'NONE', *, *, #8179, .F. ) ;
#7308=CARTESIAN_POINT ( 'NONE',  ( 3.000000000000000888, 0.000000000000000000, 0.000000000000000000 ) ) ;
#7309=ORIENTED_EDGE ( 'NONE', *, *, #2477, .T. ) ;
#7310=EDGE_CURVE ( 'NONE', #10316, #10278, #509, .T. ) ;
#7311=EDGE_CURVE ( 'NONE', #11877, #8696, #10703, .T. ) ;
#7313=ORIENTED_EDGE ( 'NONE', *, *, #11448, .F. ) ;
#7314=DIRECTION ( 'NONE',  ( -1.000000000000000000, -0.000000000000000000, -0.000000000000000000 ) ) ;
#7315=DIRECTION ( 'NONE',  ( -1.000000000000000000, -0.000000000000000000, 0.000000000000000000 ) ) ;
#7316=DIRECTION ( 'NONE',  ( -1.000000000000000000, -0.000000000000000000, 0.000000000000000000 ) ) ;
#7319=FACE_OUTER_BOUND ( 'NONE', #4787, .T. ) ;
#7320=DIRECTION ( 'NONE',  ( -1.000000000000000000, -0.000000000000000000, 0.000000000000000000 ) ) ;
#7322=EDGE_CURVE ( 'NONE', #8746, #8808, #11567, .T. ) ;
#7323=AXIS2_PLACEMENT_3D ( 'NONE', #9931, #3633, #7349 ) ;
#7324=ADVANCED_FACE ( 'NONE', ( #2260 ), #5996, .T. ) ;
#7325=CARTESIAN_POINT ( 'NONE',  ( 3.000000000000000888, 20.93895013827600593, -13.28910708463105905 ) ) ;
#7326=ORIENTED_EDGE ( 'NONE', *, *, #11956, .T. ) ;
#7327=ORIENTED_EDGE ( 'NONE', *, *, #4802, .T. ) ;
#7328=DIRECTION ( 'NONE',  ( -1.000000000000000000, -0.000000000000000000, -0.000000000000000000 ) ) ;
#7329=EDGE_LOOP ( 'NONE', ( #5249, #7285, #10528, #10907 ) ) ;
#7330=EDGE_LOOP ( 'NONE', ( #9494, #8271, #2850, #9367 ) ) ;
#7332=ORIENTED_EDGE ( 'NONE', *, *, #5549, .F. ) ;
#7333=EDGE_CURVE ( 'NONE', #2104, #348, #10588, .T. ) ;
#7334=CYLINDRICAL_SURFACE ( 'NONE', #8528, 9.599999999999997868 ) ;
#7335=AXIS2_PLACEMENT_3D ( 'NONE', #3758, #2897, #1974 ) ;
#7336=ORIENTED_EDGE ( 'NONE', *, *, #6545, .F. ) ;
#7337=CARTESIAN_POINT ( 'NONE',  ( 3.000000000000000888, 20.08719549084865008, 11.20082935824082249 ) ) ;
#7338=DIRECTION ( 'NONE',  ( 0.000000000000000000, 1.000000000000000000, 3.614007241618348376E-15 ) ) ;
#7340=EDGE_CURVE ( 'NONE', #5268, #8050, #10484, .T. ) ;
#7341=EDGE_CURVE ( 'NONE', #1233, #9863, #238, .T. ) ;
#7342=DIRECTION ( 'NONE',  ( -1.000000000000000000, 0.000000000000000000, 0.000000000000000000 ) ) ;
#7343=DIRECTION ( 'NONE',  ( -1.000000000000000000, 0.000000000000000000, 0.000000000000000000 ) ) ;
#7344=CIRCLE ( 'NONE', #4036, 9.599999999999996092 ) ;
#7345=ORIENTED_EDGE ( 'NONE', *, *, #7310, .T. ) ;
#7346=CARTESIAN_POINT ( 'NONE',  ( 3.000000000000000888, 2.745295967526300451, -22.83456483164686546 ) ) ;
#7347=ORIENTED_EDGE ( 'NONE', *, *, #5241, .T. ) ;
#7349=DIRECTION ( 'NONE',  ( 0.000000000000000000, 0.000000000000000000, 1.000000000000000000 ) ) ;
#7351=ORIENTED_EDGE ( 'NONE', *, *, #2125, .F. ) ;
#7352=DIRECTION ( 'NONE',  ( -1.000000000000000000, -0.000000000000000000, -0.000000000000000000 ) ) ;
#7353=FACE_OUTER_BOUND ( 'NONE', #4063, .T. ) ;
#7354=DIRECTION ( 'NONE',  ( -1.000000000000000000, 0.000000000000000000, 0.000000000000000000 ) ) ;
#7356=EDGE_CURVE ( 'NONE', #6096, #5168, #2474, .T. ) ;
#7358=CARTESIAN_POINT ( 'NONE',  ( 3.000000000000000888, 18.51065745848395849, -12.88318129270159673 ) ) ;
#7359=DIRECTION ( 'NONE',  ( 0.000000000000000000, -0.9945218953682724017, -0.1045284632676636294 ) ) ;
#7360=ORIENTED_EDGE ( 'NONE', *, *, #7498, .T. ) ;
#7361=CIRCLE ( 'NONE', #336, 24.80000000000000071 ) ;
#7362=EDGE_CURVE ( 'NONE', #9796, #5920, #1695, .T. ) ;
#7363=ORIENTED_EDGE ( 'NONE', *, *, #10970, .T. ) ;
#7366=CARTESIAN_POINT ( 'NONE',  ( 3.000000000000000888, -1.556492618230475022, -24.75110766671653906 ) ) ;
#7369=CIRCLE ( 'NONE', #8364, 9.599999999999999645 ) ;
#7370=CARTESIAN_POINT ( 'NONE',  ( 3.000000000000000888, -2.745295967526151237, 22.83456483164687967 ) ) ;
#7371=AXIS2_PLACEMENT_3D ( 'NONE', #5722, #129, #3761 ) ;
#7372=CARTESIAN_POINT ( 'NONE',  ( 3.000000000000000888, -22.42251312757876036, -5.117118920208720390 ) ) ;
#7373=EDGE_LOOP ( 'NONE', ( #2851, #165, #11397, #2014 ) ) ;
#7374=ORIENTED_EDGE ( 'NONE', *, *, #338, .F. ) ;
#7375=ORIENTED_EDGE ( 'NONE', *, *, #3888, .T. ) ;
#7376=DIRECTION ( 'NONE',  ( 0.000000000000000000, 0.000000000000000000, 1.000000000000000000 ) ) ;
#7377=CARTESIAN_POINT ( 'NONE',  ( 3.000000000000000888, -22.83456483164690809, 2.745295967525920311 ) ) ;
#7379=CIRCLE ( 'NONE', #1333, 9.599999999999997868 ) ;
#7380=DIRECTION ( 'NONE',  ( -1.000000000000000000, 0.000000000000000000, -0.000000000000000000 ) ) ;
#7381=CARTESIAN_POINT ( 'NONE',  ( 3.000000000000000888, 0.000000000000000000, 0.000000000000000000 ) ) ;
#7382=ADVANCED_FACE ( 'NONE', ( #10081 ), #4336, .T. ) ;
#7385=DIRECTION ( 'NONE',  ( -1.000000000000000000, 0.000000000000000000, 0.000000000000000000 ) ) ;
#7386=CIRCLE ( 'NONE', #2323, 22.99899999999999878 ) ;
#7387=EDGE_CURVE ( 'NONE', #7388, #5574, #1585, .T. ) ;
#7388=VERTEX_POINT ( 'NONE', #10889 ) ;
#7389=ORIENTED_EDGE ( 'NONE', *, *, #4728, .F. ) ;
#7391=CARTESIAN_POINT ( 'NONE',  ( 0.000000000000000000, 0.4575788569254873317, -22.54798042742717712 ) ) ;
#7392=ORIENTED_EDGE ( 'NONE', *, *, #2175, .T. ) ;
#7393=VERTEX_POINT ( 'NONE', #8933 ) ;
#7395=EDGE_CURVE ( 'NONE', #4467, #4143, #6303, .T. ) ;
#7396=ORIENTED_EDGE ( 'NONE', *, *, #6404, .F. ) ;
#7397=DIRECTION ( 'NONE',  ( -1.000000000000000000, 0.000000000000000000, -0.000000000000000000 ) ) ;
#7398=ORIENTED_EDGE ( 'NONE', *, *, #4810, .T. ) ;
#7399=EDGE_CURVE ( 'NONE', #2310, #9213, #11065, .T. ) ;
#7400=CIRCLE ( 'NONE', #2127, 9.599999999999997868 ) ;
#7401=CARTESIAN_POINT ( 'NONE',  ( 0.000000000000000000, -18.80635025205160815, -13.23915371906974592 ) ) ;
#7403=DIRECTION ( 'NONE',  ( 0.000000000000000000, -6.982962677686266711E-15, 1.000000000000000000 ) ) ;
#7405=DIRECTION ( 'NONE',  ( -1.000000000000000000, 0.000000000000000000, 0.000000000000000000 ) ) ;
#7406=CARTESIAN_POINT ( 'NONE',  ( 3.000000000000000888, -6.168200451485582825, -24.02068490260619171 ) ) ;
#7407=ORIENTED_EDGE ( 'NONE', *, *, #893, .F. ) ;
#7408=ORIENTED_EDGE ( 'NONE', *, *, #6988, .F. ) ;
#7409=LINE ( 'NONE', #8471, #400 ) ;
#7410=EDGE_LOOP ( 'NONE', ( #9907, #1442, #5390, #1293 ) ) ;
#7412=CIRCLE ( 'NONE', #3125, 22.99899999999999523 ) ;
#7414=VECTOR ( 'NONE', #5490, 1000.000000000000000 ) ;
#7415=CARTESIAN_POINT ( 'NONE',  ( 3.000000000000000888, -22.21333432029556221, -11.02759168516767474 ) ) ;
#7416=CARTESIAN_POINT ( 'NONE',  ( 3.000000000000000888, 22.54798042742717712, 0.4575788569255671012 ) ) ;
#7417=DIRECTION ( 'NONE',  ( 0.000000000000000000, -0.5877852522924797984, 0.8090169943749425663 ) ) ;
#7418=DIRECTION ( 'NONE',  ( 1.000000000000000000, 0.000000000000000000, 0.000000000000000000 ) ) ;
#7420=DIRECTION ( 'NONE',  ( 0.000000000000000000, 0.000000000000000000, 1.000000000000000000 ) ) ;
#7421=CIRCLE ( 'NONE', #3909, 9.599999999999999645 ) ;
#7422=DIRECTION ( 'NONE',  ( 0.000000000000000000, -0.6691306063588494668, -0.7431448254774020157 ) ) ;
#7423=ORIENTED_EDGE ( 'NONE', *, *, #5832, .F. ) ;
#7424=VERTEX_POINT ( 'NONE', #7077 ) ;
#7425=AXIS2_PLACEMENT_3D ( 'NONE', #8952, #2402, #4296 ) ;
#7427=DIRECTION ( 'NONE',  ( -1.000000000000000000, -0.000000000000000000, -0.000000000000000000 ) ) ;
#7428=AXIS2_PLACEMENT_3D ( 'NONE', #9063, #672, #10772 ) ;
#7430=VECTOR ( 'NONE', #4736, 1000.000000000000000 ) ;
#7431=DIRECTION ( 'NONE',  ( 0.000000000000000000, 0.000000000000000000, 1.000000000000000000 ) ) ;
#7432=FACE_OUTER_BOUND ( 'NONE', #8889, .T. ) ;
#7436=AXIS2_PLACEMENT_3D ( 'NONE', #1720, #8211, #7469 ) ;
#7437=DIRECTION ( 'NONE',  ( -1.000000000000000000, -0.000000000000000000, -0.000000000000000000 ) ) ;
#7438=VECTOR ( 'NONE', #7561, 1000.000000000000000 ) ;
#7439=CIRCLE ( 'NONE', #4315, 22.99899999999999878 ) ;
#7440=VERTEX_POINT ( 'NONE', #3609 ) ;
#7441=ORIENTED_EDGE ( 'NONE', *, *, #3070, .F. ) ;
#7442=ORIENTED_EDGE ( 'NONE', *, *, #2275, .F. ) ;
#7443=DIRECTION ( 'NONE',  ( 0.000000000000000000, 0.000000000000000000, 1.000000000000000000 ) ) ;
#7444=LINE ( 'NONE', #8503, #6665 ) ;
#7445=CIRCLE ( 'NONE', #6471, 22.99899999999999878 ) ;
#7446=AXIS2_PLACEMENT_3D ( 'NONE', #5472, #6570, #5540 ) ;
#7447=CARTESIAN_POINT ( 'NONE',  ( 3.000000000000000888, 21.30300407174362576, -7.402892494506364329 ) ) ;
#7448=DIRECTION ( 'NONE',  ( 0.000000000000000000, 0.000000000000000000, 1.000000000000000000 ) ) ;
#7449=VECTOR ( 'NONE', #1199, 1000.000000000000000 ) ;
#7450=AXIS2_PLACEMENT_3D ( 'NONE', #1209, #2361, #7691 ) ;
#7451=LINE ( 'NONE', #2814, #2410 ) ;
#7454=DIRECTION ( 'NONE',  ( -1.000000000000000000, 0.000000000000000000, 0.000000000000000000 ) ) ;
#7455=ORIENTED_EDGE ( 'NONE', *, *, #10084, .F. ) ;
#7456=ORIENTED_EDGE ( 'NONE', *, *, #9094, .T. ) ;
#7457=CARTESIAN_POINT ( 'NONE',  ( -10.00000000000000000, 0.000000000000000000, 0.000000000000000000 ) ) ;
#7458=CIRCLE ( 'NONE', #8814, 24.80000000000000071 ) ;
#7459=ORIENTED_EDGE ( 'NONE', *, *, #7900, .T. ) ;
#7460=ORIENTED_EDGE ( 'NONE', *, *, #3223, .F. ) ;
#7461=DIRECTION ( 'NONE',  ( -1.000000000000000000, 0.000000000000000000, 0.000000000000000000 ) ) ;
#7463=EDGE_LOOP ( 'NONE', ( #367, #5100, #11302, #3036 ) ) ;
#7464=AXIS2_PLACEMENT_3D ( 'NONE', #5325, #11983, #3549 ) ;
#7465=DIRECTION ( 'NONE',  ( 1.000000000000000000, 0.000000000000000000, 0.000000000000000000 ) ) ;
#7466=DIRECTION ( 'NONE',  ( -1.000000000000000000, 0.000000000000000000, -0.000000000000000000 ) ) ;
#7468=FACE_OUTER_BOUND ( 'NONE', #8882, .T. ) ;
#7469=DIRECTION ( 'NONE',  ( 0.000000000000000000, -6.866613759074863256E-15, 1.000000000000000000 ) ) ;
#7470=ORIENTED_EDGE ( 'NONE', *, *, #10394, .T. ) ;
#7471=ORIENTED_EDGE ( 'NONE', *, *, #6149, .F. ) ;
#7472=CARTESIAN_POINT ( 'NONE',  ( 3.000000000000000888, -22.99643626497957172, 0.3433949777330864706 ) ) ;
#7473=ADVANCED_FACE ( 'NONE', ( #10023 ), #4397, .T. ) ;
#7474=ORIENTED_EDGE ( 'NONE', *, *, #12045, .F. ) ;
#7476=ADVANCED_FACE ( 'NONE', ( #4275 ), #9962, .T. ) ;
#7479=LINE ( 'NONE', #10239, #3451 ) ;
#7482=DIRECTION ( 'NONE',  ( 0.000000000000000000, -0.6691306063588495778, -0.7431448254774020157 ) ) ;
#7483=CARTESIAN_POINT ( 'NONE',  ( 0.000000000000000000, 24.53384959170457336, 3.623565124517186931 ) ) ;
#7485=AXIS2_PLACEMENT_3D ( 'NONE', #9310, #2760, #5635 ) ;
#7488=ADVANCED_FACE ( 'NONE', ( #11856 ), #3431, .T. ) ;
#7490=AXIS2_PLACEMENT_3D ( 'NONE', #8372, #6469, #10206 ) ;
#7491=VECTOR ( 'NONE', #2377, 1000.000000000000000 ) ;
#7492=ORIENTED_EDGE ( 'NONE', *, *, #7341, .F. ) ;
#7493=ORIENTED_EDGE ( 'NONE', *, *, #3890, .F. ) ;
#7494=EDGE_LOOP ( 'NONE', ( #1455, #4718, #10389, #7829 ) ) ;
#7495=CARTESIAN_POINT ( 'NONE',  ( 3.000000000000000888, 19.43515443678402832, 15.40502424595151254 ) ) ;
#7497=DIRECTION ( 'NONE',  ( 0.000000000000000000, -0.7431448254773999063, 0.6691306063588519093 ) ) ;
#7498=EDGE_CURVE ( 'NONE', #9819, #8966, #7258, .T. ) ;
#7500=CARTESIAN_POINT ( 'NONE',  ( 3.000000000000000888, 0.000000000000000000, 0.000000000000000000 ) ) ;
#7501=ADVANCED_FACE ( 'NONE', ( #539 ), #603, .T. ) ;
#7502=AXIS2_PLACEMENT_3D ( 'NONE', #8107, #5535, #4618 ) ;
#7503=DIRECTION ( 'NONE',  ( 1.000000000000000000, -0.000000000000000000, -0.000000000000000000 ) ) ;
#7504=ORIENTED_EDGE ( 'NONE', *, *, #3077, .T. ) ;
#7505=ORIENTED_EDGE ( 'NONE', *, *, #6805, .T. ) ;
#7506=ORIENTED_EDGE ( 'NONE', *, *, #170, .F. ) ;
#7507=ORIENTED_EDGE ( 'NONE', *, *, #11815, .T. ) ;
#7508=CARTESIAN_POINT ( 'NONE',  ( 3.000000000000000888, 18.80635025205169697, 13.23915371906961447 ) ) ;
#7509=CARTESIAN_POINT ( 'NONE',  ( 3.000000000000000888, 2.811977935937781670, 22.37663021667345120 ) ) ;
#7510=ADVANCED_FACE ( 'NONE', ( #6238 ), #3488, .T. ) ;
#7511=AXIS2_PLACEMENT_3D ( 'NONE', #11518, #9807, #6139 ) ;
#7516=CARTESIAN_POINT ( 'NONE',  ( 3.000000000000000888, 0.000000000000000000, 0.000000000000000000 ) ) ;
#7517=FACE_OUTER_BOUND ( 'NONE', #6941, .T. ) ;
#7518=VERTEX_POINT ( 'NONE', #12039 ) ;
#7519=ORIENTED_EDGE ( 'NONE', *, *, #1207, .T. ) ;
#7520=CARTESIAN_POINT ( 'NONE',  ( 3.000000000000000888, -17.71842311621518107, -17.35216073792458502 ) ) ;
#7521=ORIENTED_EDGE ( 'NONE', *, *, #1369, .F. ) ;
#7522=EDGE_CURVE ( 'NONE', #2524, #1721, #7184, .T. ) ;
#7524=ADVANCED_FACE ( 'NONE', ( #5501 ), #1758, .T. ) ;
#7526=ORIENTED_EDGE ( 'NONE', *, *, #2305, .F. ) ;
#7527=CARTESIAN_POINT ( 'NONE',  ( 3.000000000000000888, 21.97702544527757951, 6.779701584702809924 ) ) ;
#7528=DIRECTION ( 'NONE',  ( -1.000000000000000000, -0.000000000000000000, -0.000000000000000000 ) ) ;
#7530=CARTESIAN_POINT ( 'NONE',  ( 3.000000000000000888, -1.039229259764660407, 24.77821629063821263 ) ) ;
#7531=CARTESIAN_POINT ( 'NONE',  ( 3.000000000000000888, -2.062268319295407881, -22.90635393027948297 ) ) ;
#7532=LINE ( 'NONE', #11276, #5506 ) ;
#7533=ORIENTED_EDGE ( 'NONE', *, *, #709, .F. ) ;
#7534=ORIENTED_EDGE ( 'NONE', *, *, #2324, .T. ) ;
#7535=DIRECTION ( 'NONE',  ( -1.000000000000000000, -0.000000000000000000, -0.000000000000000000 ) ) ;
#7536=ORIENTED_EDGE ( 'NONE', *, *, #9202, .F. ) ;
#7537=AXIS2_PLACEMENT_3D ( 'NONE', #10419, #3936, #6742 ) ;
#7539=CARTESIAN_POINT ( 'NONE',  ( 3.000000000000000888, 18.51065745848377730, 12.88318129270185430 ) ) ;
#7540=CARTESIAN_POINT ( 'NONE',  ( 3.000000000000000888, -13.79477846460808799, 18.40266524480583854 ) ) ;
#7541=DIRECTION ( 'NONE',  ( 0.000000000000000000, -0.8090169943749407899, -0.5877852522924822409 ) ) ;
#7543=DIRECTION ( 'NONE',  ( 0.000000000000000000, 0.000000000000000000, 1.000000000000000000 ) ) ;
#7544=DIRECTION ( 'NONE',  ( -1.000000000000000000, -0.000000000000000000, -0.000000000000000000 ) ) ;
#7545=ADVANCED_FACE ( 'NONE', ( #4768 ), #11310, .T. ) ;
#7547=CARTESIAN_POINT ( 'NONE',  ( 3.000000000000000888, -22.15038895030646060, -4.240409074144325885 ) ) ;
#7548=EDGE_LOOP ( 'NONE', ( #9469, #11865, #11973, #10133 ) ) ;
#7549=DIRECTION ( 'NONE',  ( 0.000000000000000000, 0.000000000000000000, 1.000000000000000000 ) ) ;
#7551=ORIENTED_EDGE ( 'NONE', *, *, #1247, .F. ) ;
#7552=VECTOR ( 'NONE', #11801, 1000.000000000000000 ) ;
#7553=FACE_OUTER_BOUND ( 'NONE', #11361, .T. ) ;
#7557=CARTESIAN_POINT ( 'NONE',  ( 3.000000000000000888, 0.000000000000000000, 0.000000000000000000 ) ) ;
#7561=DIRECTION ( 'NONE',  ( 1.000000000000000000, -0.000000000000000000, 0.000000000000000000 ) ) ;
#7562=ORIENTED_EDGE ( 'NONE', *, *, #3965, .T. ) ;
#7563=ORIENTED_EDGE ( 'NONE', *, *, #3756, .F. ) ;
#7564=ORIENTED_EDGE ( 'NONE', *, *, #8904, .F. ) ;
#7565=FACE_OUTER_BOUND ( 'NONE', #1113, .T. ) ;
#7566=DIRECTION ( 'NONE',  ( 0.000000000000000000, 0.8660254037844363761, 0.5000000000000039968 ) ) ;
#7567=CARTESIAN_POINT ( 'NONE',  ( 3.000000000000000888, -22.37663021667341923, 6.788022064061986605 ) ) ;
#7568=DIRECTION ( 'NONE',  ( 0.000000000000000000, 0.000000000000000000, 1.000000000000000000 ) ) ;
#7569=AXIS2_PLACEMENT_3D ( 'NONE', #8958, #11535, #4134 ) ;
#7570=DIRECTION ( 'NONE',  ( -1.000000000000000000, -0.000000000000000000, 0.000000000000000000 ) ) ;
#7572=DIRECTION ( 'NONE',  ( -1.000000000000000000, 0.000000000000000000, 0.000000000000000000 ) ) ;
#7573=VERTEX_POINT ( 'NONE', #10142 ) ;
#7574=ORIENTED_EDGE ( 'NONE', *, *, #5184, .T. ) ;
#7576=ORIENTED_EDGE ( 'NONE', *, *, #10921, .T. ) ;
#7577=CIRCLE ( 'NONE', #3092, 9.599999999999997868 ) ;
#7578=CARTESIAN_POINT ( 'NONE',  ( 1.500000000000000444, 15.80756504416690866, 19.10918332567963773 ) ) ;
#7579=ADVANCED_FACE ( 'NONE', ( #4587 ), #8376, .T. ) ;
#7581=ORIENTED_EDGE ( 'NONE', *, *, #5239, .F. ) ;
#7585=AXIS2_PLACEMENT_3D ( 'NONE', #8506, #3848, #7813 ) ;
#7586=VECTOR ( 'NONE', #3109, 1000.000000000000000 ) ;
#7587=DIRECTION ( 'NONE',  ( -1.000000000000000000, 0.000000000000000000, 0.000000000000000000 ) ) ;
#7588=EDGE_CURVE ( 'NONE', #4018, #6189, #44, .T. ) ;
#7589=DIRECTION ( 'NONE',  ( 0.000000000000000000, 0.000000000000000000, 1.000000000000000000 ) ) ;
#7590=ORIENTED_EDGE ( 'NONE', *, *, #626, .T. ) ;
#7591=ORIENTED_EDGE ( 'NONE', *, *, #2922, .F. ) ;
#7592=DIRECTION ( 'NONE',  ( 0.000000000000000000, 0.000000000000000000, -1.000000000000000000 ) ) ;
#7595=CIRCLE ( 'NONE', #5251, 9.599999999999996092 ) ;
#7596=CARTESIAN_POINT ( 'NONE',  ( 3.000000000000000888, -23.88662356770119644, 6.668524164681547184 ) ) ;
#7597=CARTESIAN_POINT ( 'NONE',  ( 3.000000000000000888, 11.48910920600714647, -21.97817939804027532 ) ) ;
#7598=DIRECTION ( 'NONE',  ( 0.000000000000000000, 0.000000000000000000, 1.000000000000000000 ) ) ;
#7600=SURFACE_SIDE_STYLE ('',( #6688 ) ) ;
#7601=DIRECTION ( 'NONE',  ( 0.000000000000000000, 0.000000000000000000, 1.000000000000000000 ) ) ;
#7602=AXIS2_PLACEMENT_3D ( 'NONE', #5194, #7427, #536 ) ;
#7604=ORIENTED_EDGE ( 'NONE', *, *, #7005, .T. ) ;
#7605=DIRECTION ( 'NONE',  ( 1.000000000000000000, 0.000000000000000000, -0.000000000000000000 ) ) ;
#7606=CIRCLE ( 'NONE', #974, 9.599999999999997868 ) ;
#7607=EDGE_LOOP ( 'NONE', ( #36, #2372, #11206, #7138 ) ) ;
#7608=CARTESIAN_POINT ( 'NONE',  ( 0.000000000000000000, 22.47229024614977533, 1.901833551798334909 ) ) ;
#7610=CARTESIAN_POINT ( 'NONE',  ( 0.000000000000000000, -22.42251312757883142, 5.117118920208414856 ) ) ;
#7612=ADVANCED_FACE ( 'NONE', ( #1827 ), #10388, .T. ) ;
#7614=DIRECTION ( 'NONE',  ( -1.000000000000000000, 0.000000000000000000, 0.000000000000000000 ) ) ;
#7615=ORIENTED_EDGE ( 'NONE', *, *, #9914, .F. ) ;
#7616=AXIS2_PLACEMENT_3D ( 'NONE', #4682, #11103, #827 ) ;
#7617=ADVANCED_FACE ( 'NONE', ( #3904 ), #9475, .T. ) ;
#7618=EDGE_CURVE ( 'NONE', #2737, #9019, #12097, .T. ) ;
#7619=CIRCLE ( 'NONE', #10171, 22.99899999999999878 ) ;
#7620=ORIENTED_EDGE ( 'NONE', *, *, #4340, .T. ) ;
#7621=CARTESIAN_POINT ( 'NONE',  ( 1.500000000000000444, 13.28910708463128287, 20.93895013827586382 ) ) ;
#7622=FACE_OUTER_BOUND ( 'NONE', #8869, .T. ) ;
#7623=ADVANCED_FACE ( 'NONE', ( #1945 ), #1091, .T. ) ;
#7624=VERTEX_POINT ( 'NONE', #4823 ) ;
#7625=CARTESIAN_POINT ( 'NONE',  ( 3.000000000000000888, -17.97274125076083351, 13.62355943574013750 ) ) ;
#7626=CARTESIAN_POINT ( 'NONE',  ( 3.000000000000000888, 0.000000000000000000, 0.000000000000000000 ) ) ;
#7627=CIRCLE ( 'NONE', #7826, 9.600000000000001421 ) ;
#7628=DIRECTION ( 'NONE',  ( -1.000000000000000000, 0.000000000000000000, 0.000000000000000000 ) ) ;
#7632=EDGE_CURVE ( 'NONE', #2061, #10333, #3722, .T. ) ;
#7633=CARTESIAN_POINT ( 'NONE',  ( 3.000000000000000888, -22.54798042742718422, 0.4575788569251160731 ) ) ;
#7634=ORIENTED_EDGE ( 'NONE', *, *, #626, .F. ) ;
#7635=VERTEX_POINT ( 'NONE', #2991 ) ;
#7638=CIRCLE ( 'NONE', #4130, 22.99899999999999523 ) ;
#7639=EDGE_LOOP ( 'NONE', ( #8114, #11796, #7423, #1291 ) ) ;
#7640=VECTOR ( 'NONE', #245, 1000.000000000000000 ) ;
#7641=LINE ( 'NONE', #3005, #61 ) ;
#7642=AXIS2_PLACEMENT_3D ( 'NONE', #9029, #6339, #4308 ) ;
#7643=VECTOR ( 'NONE', #4947, 1000.000000000000000 ) ;
#7644=DIRECTION ( 'NONE',  ( 1.000000000000000000, 0.000000000000000000, -0.000000000000000000 ) ) ;
#7645=ORIENTED_EDGE ( 'NONE', *, *, #4369, .T. ) ;
#7646=DIRECTION ( 'NONE',  ( -1.000000000000000000, 0.000000000000000000, 0.000000000000000000 ) ) ;
#7648=CARTESIAN_POINT ( 'NONE',  ( -10.00000000000000000, 0.000000000000000000, 0.000000000000000000 ) ) ;
#7650=AXIS2_PLACEMENT_3D ( 'NONE', #8400, #4668, #9336 ) ;
#7651=CARTESIAN_POINT ( 'NONE',  ( 3.000000000000000888, -16.45023496161654819, -15.42759117534402513 ) ) ;
#7652=ORIENTED_EDGE ( 'NONE', *, *, #9512, .F. ) ;
#7654=ADVANCED_FACE ( 'NONE', ( #5680 ), #1038, .T. ) ;
#7655=PLANE ( 'NONE',  #406 ) ;
#7656=EDGE_LOOP ( 'NONE', ( #8924, #1501, #3484, #7590 ) ) ;
#7657=ORIENTED_EDGE ( 'NONE', *, *, #3888, .F. ) ;
#7659=ORIENTED_EDGE ( 'NONE', *, *, #2347, .T. ) ;
#7661=STYLED_ITEM ( 'NONE', ( #9567 ), #302 ) ;
#7662=AXIS2_PLACEMENT_3D ( 'NONE', #6909, #10652, #2265 ) ;
#7663=CARTESIAN_POINT ( 'NONE',  ( 0.000000000000000000, 13.72351598154924979, -20.65684170206477788 ) ) ;
#7665=ADVANCED_FACE ( 'NONE', ( #7933 ), #7752, .T. ) ;
#7666=CARTESIAN_POINT ( 'NONE',  ( 3.000000000000000888, 0.000000000000000000, 0.000000000000000000 ) ) ;
#7667=DIRECTION ( 'NONE',  ( -1.000000000000000000, -0.000000000000000000, -0.000000000000000000 ) ) ;
#7669=CARTESIAN_POINT ( 'NONE',  ( 3.000000000000000888, -5.135568396239877487, -21.96011696265496838 ) ) ;
#7670=DIRECTION ( 'NONE',  ( -1.000000000000000000, 0.000000000000000000, 0.000000000000000000 ) ) ;
#7673=ORIENTED_EDGE ( 'NONE', *, *, #7588, .F. ) ;
#7674=CARTESIAN_POINT ( 'NONE',  ( 3.000000000000000888, 17.71842311621552923, -17.35216073792422620 ) ) ;
#7675=VERTEX_POINT ( 'NONE', #4885 ) ;
#7676=VERTEX_POINT ( 'NONE', #3967 ) ;
#7677=EDGE_CURVE ( 'NONE', #8902, #9734, #7379, .T. ) ;
#7678=DIRECTION ( 'NONE',  ( -1.000000000000000000, 0.000000000000000000, 0.000000000000000000 ) ) ;
#7680=CIRCLE ( 'NONE', #5929, 24.80000000000000071 ) ;
#7681=CARTESIAN_POINT ( 'NONE',  ( 0.000000000000000000, 11.02759168516744737, 22.21333432029567589 ) ) ;
#7683=CIRCLE ( 'NONE', #3395, 9.599999999999997868 ) ;
#7684=CIRCLE ( 'NONE', #7877, 24.80000000000000071 ) ;
#7686=DIRECTION ( 'NONE',  ( -1.000000000000000000, 0.000000000000000000, 0.000000000000000000 ) ) ;
#7688=AXIS2_PLACEMENT_3D ( 'NONE', #7080, #722, #4526 ) ;
#7689=ORIENTED_EDGE ( 'NONE', *, *, #81, .F. ) ;
#7690=DIRECTION ( 'NONE',  ( -1.000000000000000000, -0.000000000000000000, -0.000000000000000000 ) ) ;
#7691=DIRECTION ( 'NONE',  ( 0.000000000000000000, 0.000000000000000000, 1.000000000000000000 ) ) ;
#7692=ORIENTED_EDGE ( 'NONE', *, *, #2318, .F. ) ;
#7693=DIRECTION ( 'NONE',  ( -1.000000000000000000, 0.000000000000000000, 0.000000000000000000 ) ) ;
#7694=LINE ( 'NONE', #8622, #351 ) ;
#7696=DIRECTION ( 'NONE',  ( -1.000000000000000000, 0.000000000000000000, -0.000000000000000000 ) ) ;
#7697=EDGE_CURVE ( 'NONE', #5247, #900, #4664, .T. ) ;
#7699=EDGE_CURVE ( 'NONE', #9994, #8613, #7694, .T. ) ;
#7700=DIRECTION ( 'NONE',  ( 0.000000000000000000, 0.000000000000000000, 1.000000000000000000 ) ) ;
#7702=ORIENTED_EDGE ( 'NONE', *, *, #6741, .F. ) ;
#7705=ORIENTED_EDGE ( 'NONE', *, *, #705, .T. ) ;
#7706=VECTOR ( 'NONE', #5343, 1000.000000000000000 ) ;
#7707=CARTESIAN_POINT ( 'NONE',  ( 3.000000000000000888, -21.97702544527762214, 6.779701584702658046 ) ) ;
#7708=CARTESIAN_POINT ( 'NONE',  ( 0.000000000000000000, 13.62355943574044481, -17.97274125076060258 ) ) ;
#7709=CARTESIAN_POINT ( 'NONE',  ( 3.000000000000000888, -18.80635025205178579, 13.23915371906949012 ) ) ;
#7710=VERTEX_POINT ( 'NONE', #8741 ) ;
#7712=DIRECTION ( 'NONE',  ( 0.000000000000000000, -0.4999999999999888978, -0.8660254037844452579 ) ) ;
#7713=EDGE_CURVE ( 'NONE', #1256, #4254, #11308, .T. ) ;
#7714=CARTESIAN_POINT ( 'NONE',  ( 0.000000000000000000, 6.779701584702736206, 21.97702544527760082 ) ) ;
#7716=CIRCLE ( 'NONE', #7116, 24.80000000000000071 ) ;
#7717=DIRECTION ( 'NONE',  ( 0.000000000000000000, -0.4999999999999887867, -0.8660254037844449249 ) ) ;
#7718=ORIENTED_EDGE ( 'NONE', *, *, #3483, .T. ) ;
#7719=DIRECTION ( 'NONE',  ( 0.000000000000000000, 0.000000000000000000, 1.000000000000000000 ) ) ;
#7720=CYLINDRICAL_SURFACE ( 'NONE', #9784, 22.99899999999999878 ) ;
#7721=VERTEX_POINT ( 'NONE', #10506 ) ;
#7723=DIRECTION ( 'NONE',  ( 0.000000000000000000, 0.6691306063588543518, 0.7431448254773976858 ) ) ;
#7724=FACE_OUTER_BOUND ( 'NONE', #136, .T. ) ;
#7725=ADVANCED_FACE ( 'NONE', ( #8862 ), #2122, .T. ) ;
#7726=DIRECTION ( 'NONE',  ( -1.000000000000000000, 0.000000000000000000, 0.000000000000000000 ) ) ;
#7728=SURFACE_STYLE_USAGE ( .BOTH. , #7600 ) ;
#7729=DIRECTION ( 'NONE',  ( -1.000000000000000000, -0.000000000000000000, -0.000000000000000000 ) ) ;
#7730=CARTESIAN_POINT ( 'NONE',  ( 0.000000000000000000, -19.74380051311548456, 11.79560690673865331 ) ) ;
#7731=ORIENTED_EDGE ( 'NONE', *, *, #5497, .F. ) ;
#7732=AXIS2_PLACEMENT_3D ( 'NONE', #11095, #6445, #5531 ) ;
#7733=DIRECTION ( 'NONE',  ( 0.000000000000000000, 0.000000000000000000, -1.000000000000000000 ) ) ;
#7734=ORIENTED_EDGE ( 'NONE', *, *, #5046, .T. ) ;
#7735=CARTESIAN_POINT ( 'NONE',  ( 3.000000000000000888, -21.58580335785681115, 6.532525787310899723 ) ) ;
#7737=EDGE_CURVE ( 'NONE', #2001, #11239, #5003, .T. ) ;
#7738=DIRECTION ( 'NONE',  ( -1.000000000000000000, 0.000000000000000000, 0.000000000000000000 ) ) ;
#7742=LINE ( 'NONE', #5109, #11750 ) ;
#7743=CARTESIAN_POINT ( 'NONE',  ( 1.500000000000000444, 19.10918332567958089, 15.80756504416697439 ) ) ;
#7744=ORIENTED_EDGE ( 'NONE', *, *, #8688, .T. ) ;
#7745=EDGE_CURVE ( 'NONE', #8512, #6967, #3100, .T. ) ;
#7746=CIRCLE ( 'NONE', #11278, 22.99899999999999878 ) ;
#7747=ORIENTED_EDGE ( 'NONE', *, *, #8931, .F. ) ;
#7748=LINE ( 'NONE', #341, #11194 ) ;
#7751=LINE ( 'NONE', #11486, #11114 ) ;
#7752=CYLINDRICAL_SURFACE ( 'NONE', #10119, 24.80000000000000071 ) ;
#7754=DIRECTION ( 'NONE',  ( 0.000000000000000000, -0.4067366430758071472, 0.9135454576425979800 ) ) ;
#7755=ORIENTED_EDGE ( 'NONE', *, *, #11895, .T. ) ;
#7756=ORIENTED_EDGE ( 'NONE', *, *, #9298, .F. ) ;
#7759=VERTEX_POINT ( 'NONE', #284 ) ;
#7760=CARTESIAN_POINT ( 'NONE',  ( 3.000000000000000888, 13.79477846460795831, 18.40266524480593802 ) ) ;
#7762=AXIS2_PLACEMENT_3D ( 'NONE', #6578, #2111, #9580 ) ;
#7765=DIRECTION ( 'NONE',  ( -1.000000000000000000, -0.000000000000000000, -0.000000000000000000 ) ) ;
#7766=DIRECTION ( 'NONE',  ( 0.000000000000000000, 0.000000000000000000, 1.000000000000000000 ) ) ;
#7768=ADVANCED_FACE ( 'NONE', ( #4023 ), #3110, .F. ) ;
#7769=ORIENTED_EDGE ( 'NONE', *, *, #1195, .F. ) ;
#7770=FACE_OUTER_BOUND ( 'NONE', #4498, .T. ) ;
#7772=DIRECTION ( 'NONE',  ( -1.000000000000000000, -0.000000000000000000, 0.000000000000000000 ) ) ;
#7776=ADVANCED_FACE ( 'NONE', ( #9655 ), #2301, .T. ) ;
#7777=CARTESIAN_POINT ( 'NONE',  ( 0.000000000000000000, -12.88318129270165890, -18.51065745848391586 ) ) ;
#7778=EDGE_CURVE ( 'NONE', #6987, #4516, #1387, .T. ) ;
#7780=ORIENTED_EDGE ( 'NONE', *, *, #5449, .T. ) ;
#7782=ORIENTED_EDGE ( 'NONE', *, *, #8678, .T. ) ;
#7783=AXIS2_PLACEMENT_3D ( 'NONE', #6945, #2248, #6827 ) ;
#7784=LINE ( 'NONE', #10537, #9533 ) ;
#7785=AXIS2_PLACEMENT_3D ( 'NONE', #11844, #11964, #11904 ) ;
#7788=DIRECTION ( 'NONE',  ( -1.000000000000000000, 0.000000000000000000, -0.000000000000000000 ) ) ;
#7790=DIRECTION ( 'NONE',  ( 0.000000000000000000, 0.000000000000000000, 1.000000000000000000 ) ) ;
#7791=DIRECTION ( 'NONE',  ( 0.000000000000000000, 0.000000000000000000, 1.000000000000000000 ) ) ;
#7792=EDGE_LOOP ( 'NONE', ( #3037, #10205, #507, #7951 ) ) ;
#7793=AXIS2_PLACEMENT_3D ( 'NONE', #9217, #6460, #10195 ) ;
#7794=CIRCLE ( 'NONE', #6234, 9.599999999999996092 ) ;
#7795=VERTEX_POINT ( 'NONE', #11663 ) ;
#7796=ORIENTED_EDGE ( 'NONE', *, *, #9947, .T. ) ;
#7799=FACE_OUTER_BOUND ( 'NONE', #4865, .T. ) ;
#7801=AXIS2_PLACEMENT_3D ( 'NONE', #7013, #4628, #3647 ) ;
#7802=EDGE_CURVE ( 'NONE', #10397, #6438, #404, .T. ) ;
#7804=DIRECTION ( 'NONE',  ( -1.000000000000000000, 0.000000000000000000, 0.000000000000000000 ) ) ;
#7805=CYLINDRICAL_SURFACE ( 'NONE', #20, 9.599999999999997868 ) ;
#7806=VERTEX_POINT ( 'NONE', #6714 ) ;
#7809=AXIS2_PLACEMENT_3D ( 'NONE', #11013, #9161, #11738 ) ;
#7810=DIRECTION ( 'NONE',  ( 0.000000000000000000, 0.000000000000000000, 1.000000000000000000 ) ) ;
#7811=CYLINDRICAL_SURFACE ( 'NONE', #6088, 22.99899999999999878 ) ;
#7813=DIRECTION ( 'NONE',  ( 0.000000000000000000, 0.000000000000000000, 1.000000000000000000 ) ) ;
#7814=EDGE_CURVE ( 'NONE', #3187, #6304, #5439, .T. ) ;
#7816=AXIS2_PLACEMENT_3D ( 'NONE', #4996, #2178, #6764 ) ;
#7817=CIRCLE ( 'NONE', #2547, 24.80000000000000071 ) ;
#7818=DIRECTION ( 'NONE',  ( 0.000000000000000000, 0.000000000000000000, 1.000000000000000000 ) ) ;
#7819=ORIENTED_EDGE ( 'NONE', *, *, #9945, .F. ) ;
#7820=ORIENTED_EDGE ( 'NONE', *, *, #5981, .F. ) ;
#7825=CARTESIAN_POINT ( 'NONE',  ( 3.000000000000000888, -4.240409074143949297, -22.15038895030653521 ) ) ;
#7826=AXIS2_PLACEMENT_3D ( 'NONE', #1484, #9811, #561 ) ;
#7828=VECTOR ( 'NONE', #8883, 1000.000000000000000 ) ;
#7829=ORIENTED_EDGE ( 'NONE', *, *, #11678, .T. ) ;
#7830=CIRCLE ( 'NONE', #5685, 24.80000000000000071 ) ;
#7831=DIRECTION ( 'NONE',  ( 0.000000000000000000, 0.000000000000000000, 1.000000000000000000 ) ) ;
#7833=DIRECTION ( 'NONE',  ( 0.000000000000000000, 0.2079116908177532641, 0.9781476007338070211 ) ) ;
#7835=VERTEX_POINT ( 'NONE', #6222 ) ;
#7836=CIRCLE ( 'NONE', #6661, 9.599999999999999645 ) ;
#7837=CARTESIAN_POINT ( 'NONE',  ( 3.000000000000000888, -7.432877647175053504, -21.76479567747249178 ) ) ;
#7838=AXIS2_PLACEMENT_3D ( 'NONE', #4815, #4695, #34 ) ;
#7839=ORIENTED_EDGE ( 'NONE', *, *, #8724, .T. ) ;
#7840=FACE_OUTER_BOUND ( 'NONE', #3090, .T. ) ;
#7841=AXIS2_PLACEMENT_3D ( 'NONE', #7391, #11134, #1835 ) ;
#7844=CARTESIAN_POINT ( 'NONE',  ( 0.000000000000000000, -19.43515443678413135, 15.40502424595139530 ) ) ;
#7846=AXIS2_PLACEMENT_3D ( 'NONE', #638, #2532, #3463 ) ;
#7847=DIRECTION ( 'NONE',  ( 0.000000000000000000, 0.9781476007338062439, -0.2079116908177564282 ) ) ;
#7849=CIRCLE ( 'NONE', #2576, 9.599999999999997868 ) ;
#7850=CARTESIAN_POINT ( 'NONE',  ( 0.000000000000000000, 0.000000000000000000, 0.000000000000000000 ) ) ;
#7852=CARTESIAN_POINT ( 'NONE',  ( 0.000000000000000000, -22.56530478845651544, 4.445336973060782348 ) ) ;
#7854=EDGE_CURVE ( 'NONE', #9879, #9423, #9348, .T. ) ;
#7855=CARTESIAN_POINT ( 'NONE',  ( -10.00000000000000000, 0.000000000000000000, 0.000000000000000000 ) ) ;
#7857=EDGE_CURVE ( 'NONE', #11802, #8511, #155, .T. ) ;
#7858=DIRECTION ( 'NONE',  ( 0.000000000000000000, 0.000000000000000000, 1.000000000000000000 ) ) ;
#7859=VERTEX_POINT ( 'NONE', #7001 ) ;
#7860=VECTOR ( 'NONE', #1164, 1000.000000000000000 ) ;
#7861=ORIENTED_EDGE ( 'NONE', *, *, #11230, .F. ) ;
#7862=CIRCLE ( 'NONE', #9000, 9.599999999999996092 ) ;
#7863=DIRECTION ( 'NONE',  ( -1.000000000000000000, 0.000000000000000000, -0.000000000000000000 ) ) ;
#7865=CARTESIAN_POINT ( 'NONE',  ( 3.000000000000000888, -17.35216073792452462, 17.71842311621524146 ) ) ;
#7867=EDGE_CURVE ( 'NONE', #3556, #4653, #11692, .T. ) ;
#7869=AXIS2_PLACEMENT_3D ( 'NONE', #8555, #4765, #7443 ) ;
#7870=CARTESIAN_POINT ( 'NONE',  ( 1.499999999999999556, -11.02759168516730881, -22.21333432029574695 ) ) ;
#7871=ORIENTED_EDGE ( 'NONE', *, *, #11138, .F. ) ;
#7872=ORIENTED_EDGE ( 'NONE', *, *, #7162, .T. ) ;
#7873=VERTEX_POINT ( 'NONE', #7183 ) ;
#7874=EDGE_CURVE ( 'NONE', #1383, #9137, #7595, .T. ) ;
#7875=LINE ( 'NONE', #6999, #7643 ) ;
#7877=AXIS2_PLACEMENT_3D ( 'NONE', #1734, #9328, #11289 ) ;
#7879=EDGE_CURVE ( 'NONE', #3959, #9646, #7386, .T. ) ;
#7881=DIRECTION ( 'NONE',  ( 0.000000000000000000, -0.4067366430757888285, -0.9135454576426059736 ) ) ;
#7882=VERTEX_POINT ( 'NONE', #3417 ) ;
#7883=EDGE_LOOP ( 'NONE', ( #4612, #777, #10862, #3194 ) ) ;
#7884=VECTOR ( 'NONE', #9545, 1000.000000000000000 ) ;
#7887=EDGE_LOOP ( 'NONE', ( #10121, #3854, #6765, #2092 ) ) ;
#7888=CARTESIAN_POINT ( 'NONE',  ( 3.000000000000000888, 22.15038895030654942, -4.240409074143872914 ) ) ;
#7891=ORIENTED_EDGE ( 'NONE', *, *, #8438, .T. ) ;
#7892=ADVANCED_FACE ( 'NONE', ( #526 ), #11845, .T. ) ;
#7893=DIRECTION ( 'NONE',  ( -1.000000000000000000, 0.000000000000000000, -0.000000000000000000 ) ) ;
#7894=CARTESIAN_POINT ( 'NONE',  ( 3.000000000000000888, 0.000000000000000000, 0.000000000000000000 ) ) ;
#7896=VERTEX_POINT ( 'NONE', #10932 ) ;
#7897=DIRECTION ( 'NONE',  ( 0.000000000000000000, 0.000000000000000000, -1.000000000000000000 ) ) ;
#7898=CIRCLE ( 'NONE', #1646, 22.99899999999999878 ) ;
#7899=FACE_OUTER_BOUND ( 'NONE', #1723, .T. ) ;
#7900=EDGE_CURVE ( 'NONE', #6856, #4609, #9151, .T. ) ;
#7901=ORIENTED_EDGE ( 'NONE', *, *, #6013, .T. ) ;
#7903=ORIENTED_EDGE ( 'NONE', *, *, #1207, .F. ) ;
#7904=CYLINDRICAL_SURFACE ( 'NONE', #1680, 9.599999999999997868 ) ;
#7906=AXIS2_PLACEMENT_3D ( 'NONE', #4981, #3203, #497 ) ;
#7907=DIRECTION ( 'NONE',  ( -1.000000000000000000, -0.000000000000000000, -0.000000000000000000 ) ) ;
#7908=CARTESIAN_POINT ( 'NONE',  ( 3.000000000000000888, 2.062268319295869290, -22.90635393027944033 ) ) ;
#7912=CARTESIAN_POINT ( 'NONE',  ( 0.000000000000000000, -3.623565124516940461, -24.53384959170461599 ) ) ;
#7913=CARTESIAN_POINT ( 'NONE',  ( 0.000000000000000000, 0.000000000000000000, 0.000000000000000000 ) ) ;
#7914=ORIENTED_EDGE ( 'NONE', *, *, #4868, .T. ) ;
#7915=EDGE_CURVE ( 'NONE', #9364, #4270, #11506, .T. ) ;
#7916=CYLINDRICAL_SURFACE ( 'NONE', #1872, 9.599999999999994316 ) ;
#7917=DIRECTION ( 'NONE',  ( 0.000000000000000000, 0.000000000000000000, 1.000000000000000000 ) ) ;
#7918=EDGE_CURVE ( 'NONE', #5065, #1084, #1735, .T. ) ;
#7919=CYLINDRICAL_SURFACE ( 'NONE', #7298, 22.99899999999999878 ) ;
#7921=AXIS2_PLACEMENT_3D ( 'NONE', #1489, #6873, #2232 ) ;
#7923=FACE_OUTER_BOUND ( 'NONE', #1576, .T. ) ;
#7924=CYLINDRICAL_SURFACE ( 'NONE', #4697, 9.599999999999997868 ) ;
#7925=ADVANCED_FACE ( 'NONE', ( #1568 ), #6286, .T. ) ;
#7926=EDGE_LOOP ( 'NONE', ( #905, #12106, #11347, #5323 ) ) ;
#7927=VERTEX_POINT ( 'NONE', #6104 ) ;
#7928=ORIENTED_EDGE ( 'NONE', *, *, #8556, .T. ) ;
#7929=EDGE_CURVE ( 'NONE', #6719, #9406, #5648, .T. ) ;
#7930=DIRECTION ( 'NONE',  ( 0.000000000000000000, 0.000000000000000000, 1.000000000000000000 ) ) ;
#7931=EDGE_CURVE ( 'NONE', #9213, #2104, #5058, .T. ) ;
#7932=DIRECTION ( 'NONE',  ( 0.000000000000000000, 0.8090169943749445647, 0.5877852522924771339 ) ) ;
#7933=FACE_OUTER_BOUND ( 'NONE', #8263, .T. ) ;
#7934=EDGE_CURVE ( 'NONE', #2892, #11802, #6035, .T. ) ;
#7936=CARTESIAN_POINT ( 'NONE',  ( 0.000000000000000000, -6.168200451485919444, 24.02068490260611000 ) ) ;
#7937=CIRCLE ( 'NONE', #2081, 22.99900000000000233 ) ;
#7938=CARTESIAN_POINT ( 'NONE',  ( 0.000000000000000000, -6.668524164681792321, 23.88662356770113249 ) ) ;
#7939=ORIENTED_EDGE ( 'NONE', *, *, #207, .F. ) ;
#7940=ORIENTED_EDGE ( 'NONE', *, *, #11812, .F. ) ;
#7943=DIRECTION ( 'NONE',  ( 0.000000000000000000, 0.000000000000000000, -1.000000000000000000 ) ) ;
#7946=LINE ( 'NONE', #2136, #10677 ) ;
#7947=ORIENTED_EDGE ( 'NONE', *, *, #10436, .F. ) ;
#7948=CARTESIAN_POINT ( 'NONE',  ( 3.000000000000000888, 0.000000000000000000, 0.000000000000000000 ) ) ;
#7949=CARTESIAN_POINT ( 'NONE',  ( 0.000000000000000000, 0.000000000000000000, 0.000000000000000000 ) ) ;
#7951=ORIENTED_EDGE ( 'NONE', *, *, #2240, .T. ) ;
#7952=CARTESIAN_POINT ( 'NONE',  ( 3.000000000000000888, 15.64281154287620446, -16.85990652506883691 ) ) ;
#7953=DIRECTION ( 'NONE',  ( 0.000000000000000000, 0.000000000000000000, 1.000000000000000000 ) ) ;
#7954=ORIENTED_EDGE ( 'NONE', *, *, #9546, .T. ) ;
#7955=EDGE_CURVE ( 'NONE', #11767, #2929, #8188, .T. ) ;
#7957=CARTESIAN_POINT ( 'NONE',  ( 0.000000000000000000, -24.77821629063820907, -1.039229259764747004 ) ) ;
#7960=EDGE_CURVE ( 'NONE', #10168, #10729, #11113, .T. ) ;
#7961=FACE_OUTER_BOUND ( 'NONE', #10220, .T. ) ;
#7963=CIRCLE ( 'NONE', #5630, 24.80000000000000071 ) ;
#7964=DIRECTION ( 'NONE',  ( -1.000000000000000000, -0.000000000000000000, -0.000000000000000000 ) ) ;
#7966=DIRECTION ( 'NONE',  ( -1.000000000000000000, -0.000000000000000000, 0.000000000000000000 ) ) ;
#7967=ORIENTED_EDGE ( 'NONE', *, *, #4065, .T. ) ;
#7968=FACE_OUTER_BOUND ( 'NONE', #7410, .T. ) ;
#7970=AXIS2_PLACEMENT_3D ( 'NONE', #3660, #11371, #853 ) ;
#7971=CARTESIAN_POINT ( 'NONE',  ( 8.000000000000000000, 0.000000000000000000, 0.000000000000000000 ) ) ;
#7973=CARTESIAN_POINT ( 'NONE',  ( 3.000000000000000888, -15.64281154287585807, -16.85990652506916021 ) ) ;
#7974=DIRECTION ( 'NONE',  ( 0.000000000000000000, 0.000000000000000000, 1.000000000000000000 ) ) ;
#7977=FACE_OUTER_BOUND ( 'NONE', #11188, .T. ) ;
#7978=VECTOR ( 'NONE', #5994, 1000.000000000000000 ) ;
#7979=CARTESIAN_POINT ( 'NONE',  ( 3.000000000000000888, 15.13242714128143440, -17.31945870441131419 ) ) ;
#7980=ORIENTED_EDGE ( 'NONE', *, *, #330, .F. ) ;
#7982=ORIENTED_EDGE ( 'NONE', *, *, #3289, .F. ) ;
#7984=CIRCLE ( 'NONE', #8196, 24.80000000000000071 ) ;
#7986=DIRECTION ( 'NONE',  ( 0.000000000000000000, 0.9781476007338062439, -0.2079116908177564282 ) ) ;
#7989=CYLINDRICAL_SURFACE ( 'NONE', #5300, 9.599999999999997868 ) ;
#7990=EDGE_CURVE ( 'NONE', #246, #2892, #9748, .T. ) ;
#7991=DIRECTION ( 'NONE',  ( -1.000000000000000000, -0.000000000000000000, 0.000000000000000000 ) ) ;
#7992=AXIS2_PLACEMENT_3D ( 'NONE', #9594, #43, #5679 ) ;
#7993=EDGE_LOOP ( 'NONE', ( #11139, #5207, #9828, #3264 ) ) ;
#7996=ADVANCED_FACE ( 'NONE', ( #7432 ), #5482, .T. ) ;
#7997=CIRCLE ( 'NONE', #11714, 22.99900000000000233 ) ;
#7999=DIRECTION ( 'NONE',  ( -1.000000000000000000, 0.000000000000000000, 0.000000000000000000 ) ) ;
#8000=CARTESIAN_POINT ( 'NONE',  ( 3.000000000000000888, 0.000000000000000000, 0.000000000000000000 ) ) ;
#8001=CYLINDRICAL_SURFACE ( 'NONE', #2331, 22.99899999999999878 ) ;
#8003=ORIENTED_EDGE ( 'NONE', *, *, #11435, .T. ) ;
#8004=CARTESIAN_POINT ( 'NONE',  ( 1.500000000000000444, -19.43515443678392529, -15.40502424595165110 ) ) ;
#8006=CARTESIAN_POINT ( 'NONE',  ( 3.000000000000000888, 0.000000000000000000, 0.000000000000000000 ) ) ;
#8008=EDGE_CURVE ( 'NONE', #11191, #1896, #4470, .T. ) ;
#8010=DIRECTION ( 'NONE',  ( 1.000000000000000000, 0.000000000000000000, 0.000000000000000000 ) ) ;
#8011=CARTESIAN_POINT ( 'NONE',  ( 0.000000000000000000, -4.240409074143949297, -22.15038895030653521 ) ) ;
#8012=AXIS2_PLACEMENT_3D ( 'NONE', #4923, #1253, #6866 ) ;
#8013=ORIENTED_EDGE ( 'NONE', *, *, #2385, .T. ) ;
#8015=VECTOR ( 'NONE', #2404, 1000.000000000000000 ) ;
#8016=ORIENTED_EDGE ( 'NONE', *, *, #4269, .T. ) ;
#8017=EDGE_CURVE ( 'NONE', #11921, #8297, #1813, .T. ) ;
#8018=CARTESIAN_POINT ( 'NONE',  ( 3.000000000000000888, 0.000000000000000000, 0.000000000000000000 ) ) ;
#8020=DIRECTION ( 'NONE',  ( -1.000000000000000000, 0.000000000000000000, -0.000000000000000000 ) ) ;
#8022=DIRECTION ( 'NONE',  ( 0.000000000000000000, 0.000000000000000000, 1.000000000000000000 ) ) ;
#8023=CARTESIAN_POINT ( 'NONE',  ( 3.000000000000000888, 15.64281154287597353, 16.85990652506905363 ) ) ;
#8025=AXIS2_PLACEMENT_3D ( 'NONE', #1667, #10290, #1010 ) ;
#8026=ADVANCED_FACE ( 'NONE', ( #11965 ), #10258, .T. ) ;
#8027=FACE_OUTER_BOUND ( 'NONE', #10994, .T. ) ;
#8029=AXIS2_PLACEMENT_3D ( 'NONE', #3616, #789, #11922 ) ;
#8030=DIRECTION ( 'NONE',  ( -1.000000000000000000, -0.000000000000000000, 0.000000000000000000 ) ) ;
#8032=CARTESIAN_POINT ( 'NONE',  ( 3.000000000000000888, 0.000000000000000000, 0.000000000000000000 ) ) ;
#8033=ORIENTED_EDGE ( 'NONE', *, *, #7356, .T. ) ;
#8035=DIRECTION ( 'NONE',  ( -1.000000000000000000, 0.000000000000000000, 0.000000000000000000 ) ) ;
#8037=FACE_OUTER_BOUND ( 'NONE', #5203, .T. ) ;
#8038=ORIENTED_EDGE ( 'NONE', *, *, #2927, .F. ) ;
#8039=CIRCLE ( 'NONE', #817, 24.80000000000000071 ) ;
#8040=CIRCLE ( 'NONE', #1784, 22.99899999999999878 ) ;
#8041=CARTESIAN_POINT ( 'NONE',  ( 0.000000000000000000, 0.000000000000000000, 0.000000000000000000 ) ) ;
#8042=CARTESIAN_POINT ( 'NONE',  ( 3.000000000000000888, 0.3433949777331667397, 22.99643626497956816 ) ) ;
#8043=DIRECTION ( 'NONE',  ( -1.000000000000000000, -0.000000000000000000, 0.000000000000000000 ) ) ;
#8046=AXIS2_PLACEMENT_3D ( 'NONE', #1541, #2339, #8094 ) ;
#8047=CARTESIAN_POINT ( 'NONE',  ( 3.000000000000000888, -20.78471918669866270, 8.753070780933086326 ) ) ;
#8048=EDGE_LOOP ( 'NONE', ( #3391, #10515, #3819, #9762 ) ) ;
#8049=CIRCLE ( 'NONE', #7428, 9.599999999999997868 ) ;
#8050=VERTEX_POINT ( 'NONE', #2731 ) ;
#8051=VERTEX_POINT ( 'NONE', #10126 ) ;
#8053=AXIS2_PLACEMENT_3D ( 'NONE', #12004, #11149, #5401 ) ;
#8054=CIRCLE ( 'NONE', #10007, 24.80000000000000071 ) ;
#8056=VECTOR ( 'NONE', #8035, 1000.000000000000000 ) ;
#8057=CARTESIAN_POINT ( 'NONE',  ( 0.000000000000000000, 9.667200211209820537, 20.86861857134737619 ) ) ;
#8059=CARTESIAN_POINT ( 'NONE',  ( 3.000000000000000888, -19.43515443678412424, 15.40502424595139175 ) ) ;
#8060=CARTESIAN_POINT ( 'NONE',  ( 0.000000000000000000, 24.02068490260621303, -6.168200451485523317 ) ) ;
#8061=ORIENTED_EDGE ( 'NONE', *, *, #6013, .F. ) ;
#8062=VECTOR ( 'NONE', #839, 1000.000000000000000 ) ;
#8063=VERTEX_POINT ( 'NONE', #5551 ) ;
#8064=ORIENTED_EDGE ( 'NONE', *, *, #2699, .F. ) ;
#8065=EDGE_CURVE ( 'NONE', #4775, #4413, #759, .T. ) ;
#8066=LINE ( 'NONE', #1458, #3975 ) ;
#8067=AXIS2_PLACEMENT_3D ( 'NONE', #1558, #4250, #758 ) ;
#8068=CARTESIAN_POINT ( 'NONE',  ( 3.000000000000000888, -18.51065745848368849, -12.88318129270198042 ) ) ;
#8069=DIRECTION ( 'NONE',  ( -1.000000000000000000, 0.000000000000000000, -0.000000000000000000 ) ) ;
#8070=CARTESIAN_POINT ( 'NONE',  ( 0.000000000000000000, 0.000000000000000000, 0.000000000000000000 ) ) ;
#8071=VERTEX_POINT ( 'NONE', #8362 ) ;
#8072=CIRCLE ( 'NONE', #3390, 22.99899999999999523 ) ;
#8073=CYLINDRICAL_SURFACE ( 'NONE', #11981, 24.80000000000000071 ) ;
#8074=EDGE_CURVE ( 'NONE', #8486, #7265, #4691, .T. ) ;
#8075=DIRECTION ( 'NONE',  ( 0.000000000000000000, -0.5000000000000072164, 0.8660254037844345998 ) ) ;
#8079=DIRECTION ( 'NONE',  ( -1.000000000000000000, -0.000000000000000000, -0.000000000000000000 ) ) ;
#8080=ORIENTED_EDGE ( 'NONE', *, *, #9683, .T. ) ;
#8084=EDGE_CURVE ( 'NONE', #8218, #10492, #2796, .T. ) ;
#8085=ORIENTED_EDGE ( 'NONE', *, *, #9121, .F. ) ;
#8087=LINE ( 'NONE', #4288, #10147 ) ;
#8088=EDGE_LOOP ( 'NONE', ( #5494, #11316, #2750, #1767 ) ) ;
#8089=ADVANCED_FACE ( 'NONE', ( #3778 ), #12025, .T. ) ;
#8090=LINE ( 'NONE', #7337, #6790 ) ;
#8091=CARTESIAN_POINT ( 'NONE',  ( 3.000000000000000888, 0.000000000000000000, 0.000000000000000000 ) ) ;
#8094=DIRECTION ( 'NONE',  ( 0.000000000000000000, 0.000000000000000000, 1.000000000000000000 ) ) ;
#8096=DIRECTION ( 'NONE',  ( -1.000000000000000000, 0.000000000000000000, 0.000000000000000000 ) ) ;
#8098=DIRECTION ( 'NONE',  ( 1.000000000000000000, 0.000000000000000000, 0.000000000000000000 ) ) ;
#8101=AXIS2_PLACEMENT_3D ( 'NONE', #6802, #2221, #11760 ) ;
#8102=EDGE_CURVE ( 'NONE', #11246, #4392, #8809, .T. ) ;
#8103=DIRECTION ( 'NONE',  ( -1.000000000000000000, -0.000000000000000000, -0.000000000000000000 ) ) ;
#8105=ORIENTED_EDGE ( 'NONE', *, *, #3066, .T. ) ;
#8106=CARTESIAN_POINT ( 'NONE',  ( 0.000000000000000000, 0.000000000000000000, 0.000000000000000000 ) ) ;
#8107=CARTESIAN_POINT ( 'NONE',  ( 3.000000000000000888, -20.41249101028205004, -9.589108953448107542 ) ) ;
#8110=DIRECTION ( 'NONE',  ( -1.000000000000000000, -0.000000000000000000, -0.000000000000000000 ) ) ;
#8111=DIRECTION ( 'NONE',  ( 0.000000000000000000, 0.000000000000000000, 1.000000000000000000 ) ) ;
#8114=ORIENTED_EDGE ( 'NONE', *, *, #2951, .F. ) ;
#8117=CARTESIAN_POINT ( 'NONE',  ( 0.000000000000000000, -22.83456483164690809, 2.745295967525920311 ) ) ;
#8118=DIRECTION ( 'NONE',  ( 0.000000000000000000, 0.000000000000000000, 1.000000000000000000 ) ) ;
#8119=AXIS2_PLACEMENT_3D ( 'NONE', #10675, #8782, #11532 ) ;
#8120=EDGE_CURVE ( 'NONE', #7087, #3509, #9552, .T. ) ;
#8122=LINE ( 'NONE', #4509, #11936 ) ;
#8123=DIRECTION ( 'NONE',  ( -1.000000000000000000, 0.000000000000000000, 0.000000000000000000 ) ) ;
#8124=ORIENTED_EDGE ( 'NONE', *, *, #5239, .T. ) ;
#8125=VERTEX_POINT ( 'NONE', #3061 ) ;
#8126=AXIS2_PLACEMENT_3D ( 'NONE', #751, #4486, #8285 ) ;
#8128=ORIENTED_EDGE ( 'NONE', *, *, #5160, .F. ) ;
#8129=FACE_OUTER_BOUND ( 'NONE', #1698, .T. ) ;
#8130=CARTESIAN_POINT ( 'NONE',  ( 0.000000000000000000, 11.67026512804547345, 19.29833442572363822 ) ) ;
#8131=DIRECTION ( 'NONE',  ( -1.000000000000000000, -0.000000000000000000, 0.000000000000000000 ) ) ;
#8132=ORIENTED_EDGE ( 'NONE', *, *, #5345, .F. ) ;
#8133=CARTESIAN_POINT ( 'NONE',  ( 0.000000000000000000, -16.85990652506910692, 15.64281154287591669 ) ) ;
#8135=CARTESIAN_POINT ( 'NONE',  ( 0.000000000000000000, -9.039786367038983528, 21.14796121233193560 ) ) ;
#8137=LINE ( 'NONE', #10218, #6269 ) ;
#8138=EDGE_LOOP ( 'NONE', ( #7533, #9159, #6712, #11645 ) ) ;
#8139=CARTESIAN_POINT ( 'NONE',  ( 3.000000000000000888, 22.83456483164689033, 2.745295967526073078 ) ) ;
#8140=ORIENTED_EDGE ( 'NONE', *, *, #1738, .F. ) ;
#8141=ORIENTED_EDGE ( 'NONE', *, *, #2578, .F. ) ;
#8142=AXIS2_PLACEMENT_3D ( 'NONE', #5016, #8877, #8752 ) ;
#8145=CARTESIAN_POINT ( 'NONE',  ( 1.500000000000000444, 4.135161237383916166, -24.45282072769597193 ) ) ;
#8146=ADVANCED_FACE ( 'NONE', ( #5939 ), #4161, .T. ) ;
#8147=DIRECTION ( 'NONE',  ( 0.000000000000000000, 0.000000000000000000, -1.000000000000000000 ) ) ;
#8148=DIRECTION ( 'NONE',  ( -1.000000000000000000, 0.000000000000000000, -0.000000000000000000 ) ) ;
#8150=FACE_OUTER_BOUND ( 'NONE', #9188, .T. ) ;
#8152=CYLINDRICAL_SURFACE ( 'NONE', #7425, 9.599999999999997868 ) ;
#8153=ORIENTED_EDGE ( 'NONE', *, *, #1520, .F. ) ;
#8154=CARTESIAN_POINT ( 'NONE',  ( 3.000000000000000888, 2.811977935938088535, -22.37663021667340857 ) ) ;
#8155=EDGE_CURVE ( 'NONE', #6438, #3896, #11896, .T. ) ;
#8156=ORIENTED_EDGE ( 'NONE', *, *, #8650, .F. ) ;
#8157=EDGE_CURVE ( 'NONE', #10684, #3630, #3004, .T. ) ;
#8159=CYLINDRICAL_SURFACE ( 'NONE', #99, 24.80000000000000071 ) ;
#8160=EDGE_LOOP ( 'NONE', ( #879, #6425, #4761, #6215 ) ) ;
#8161=AXIS2_PLACEMENT_3D ( 'NONE', #5968, #4245, #8728 ) ;
#8162=CYLINDRICAL_SURFACE ( 'NONE', #10307, 9.599999999999997868 ) ;
#8163=CARTESIAN_POINT ( 'NONE',  ( 3.000000000000000888, 22.15038895030649257, 4.240409074144170454 ) ) ;
#8166=FACE_OUTER_BOUND ( 'NONE', #11925, .T. ) ;
#8167=DIRECTION ( 'NONE',  ( 1.000000000000000000, -0.000000000000000000, 0.000000000000000000 ) ) ;
#8168=ORIENTED_EDGE ( 'NONE', *, *, #4598, .F. ) ;
#8169=AXIS2_PLACEMENT_3D ( 'NONE', #11585, #5956, #3202 ) ;
#8170=ORIENTED_EDGE ( 'NONE', *, *, #3662, .T. ) ;
#8171=ORIENTED_EDGE ( 'NONE', *, *, #9496, .F. ) ;
#8173=CARTESIAN_POINT ( 'NONE',  ( 3.000000000000000888, 16.85990652506900389, 15.64281154287603215 ) ) ;
#8174=EDGE_CURVE ( 'NONE', #1307, #277, #4032, .T. ) ;
#8175=DIRECTION ( 'NONE',  ( -1.000000000000000000, 0.000000000000000000, -0.000000000000000000 ) ) ;
#8176=VECTOR ( 'NONE', #6649, 1000.000000000000000 ) ;
#8179=EDGE_CURVE ( 'NONE', #7150, #8200, #163, .T. ) ;
#8181=ORIENTED_EDGE ( 'NONE', *, *, #9094, .F. ) ;
#8182=CARTESIAN_POINT ( 'NONE',  ( 0.000000000000000000, -1.039229259764318680, -24.77821629063823394 ) ) ;
#8183=VERTEX_POINT ( 'NONE', #4894 ) ;
#8184=ADVANCED_FACE ( 'NONE', ( #1401 ), #4094, .T. ) ;
#8186=VERTEX_POINT ( 'NONE', #10584 ) ;
#8187=LINE ( 'NONE', #2560, #11011 ) ;
#8188=CIRCLE ( 'NONE', #8589, 22.99899999999999878 ) ;
#8189=CIRCLE ( 'NONE', #3478, 9.599999999999999645 ) ;
#8190=DIRECTION ( 'NONE',  ( 0.000000000000000000, 0.000000000000000000, 1.000000000000000000 ) ) ;
#8191=EDGE_CURVE ( 'NONE', #2147, #9529, #10700, .T. ) ;
#8192=CARTESIAN_POINT ( 'NONE',  ( 1.499999999999999556, -24.45282072769597903, -4.135161237383830901 ) ) ;
#8193=DIRECTION ( 'NONE',  ( 0.000000000000000000, 0.000000000000000000, 1.000000000000000000 ) ) ;
#8194=CARTESIAN_POINT ( 'NONE',  ( 3.000000000000000888, 17.97274125076092233, -13.62355943574001671 ) ) ;
#8196=AXIS2_PLACEMENT_3D ( 'NONE', #11178, #5603, #10191 ) ;
#8197=DIRECTION ( 'NONE',  ( -1.000000000000000000, 0.000000000000000000, -0.000000000000000000 ) ) ;
#8199=VERTEX_POINT ( 'NONE', #1334 ) ;
#8200=VERTEX_POINT ( 'NONE', #8750 ) ;
#8201=VECTOR ( 'NONE', #141, 1000.000000000000000 ) ;
#8203=CIRCLE ( 'NONE', #3907, 9.599999999999999645 ) ;
#8204=ORIENTED_EDGE ( 'NONE', *, *, #1797, .T. ) ;
#8205=CYLINDRICAL_SURFACE ( 'NONE', #311, 9.599999999999997868 ) ;
#8206=VERTEX_POINT ( 'NONE', #2078 ) ;
#8207=AXIS2_PLACEMENT_3D ( 'NONE', #5730, #11908, #1015 ) ;
#8209=LINE ( 'NONE', #7217, #881 ) ;
#8211=DIRECTION ( 'NONE',  ( -1.000000000000000000, 0.000000000000000000, 0.000000000000000000 ) ) ;
#8212=VERTEX_POINT ( 'NONE', #11440 ) ;
#8213=DIRECTION ( 'NONE',  ( -1.000000000000000000, 0.000000000000000000, 0.000000000000000000 ) ) ;
#8214=AXIS2_PLACEMENT_3D ( 'NONE', #8666, #4187, #265 ) ;
#8215=ORIENTED_EDGE ( 'NONE', *, *, #288, .T. ) ;
#8218=VERTEX_POINT ( 'NONE', #353 ) ;
#8219=AXIS2_PLACEMENT_3D ( 'NONE', #11290, #11955, #7422 ) ;
#8220=DIRECTION ( 'NONE',  ( -1.000000000000000000, 0.000000000000000000, 0.000000000000000000 ) ) ;
#8221=VECTOR ( 'NONE', #2011, 1000.000000000000000 ) ;
#8222=ADVANCED_FACE ( 'NONE', ( #9606 ), #1281, .T. ) ;
#8223=AXIS2_PLACEMENT_3D ( 'NONE', #9439, #9375, #995 ) ;
#8224=LINE ( 'NONE', #11949, #10385 ) ;
#8225=DIRECTION ( 'NONE',  ( -1.000000000000000000, -0.000000000000000000, -0.000000000000000000 ) ) ;
#8228=EDGE_CURVE ( 'NONE', #490, #110, #2314, .T. ) ;
#8229=DIRECTION ( 'NONE',  ( -1.000000000000000000, 0.000000000000000000, 0.000000000000000000 ) ) ;
#8230=EDGE_CURVE ( 'NONE', #2524, #5042, #3502, .T. ) ;
#8231=CARTESIAN_POINT ( 'NONE',  ( 0.000000000000000000, -22.21333432029571497, 11.02759168516737098 ) ) ;
#8232=VERTEX_POINT ( 'NONE', #5875 ) ;
#8233=AXIS2_PLACEMENT_3D ( 'NONE', #6380, #65, #1849 ) ;
#8234=EDGE_LOOP ( 'NONE', ( #11605, #11617, #11403, #5745 ) ) ;
#8235=CIRCLE ( 'NONE', #7841, 9.599999999999994316 ) ;
#8237=VECTOR ( 'NONE', #3901, 1000.000000000000000 ) ;
#8239=EDGE_CURVE ( 'NONE', #7393, #5404, #2720, .T. ) ;
#8240=CARTESIAN_POINT ( 'NONE',  ( 0.000000000000000000, 17.31945870441147406, 15.13242714128125499 ) ) ;
#8241=CARTESIAN_POINT ( 'NONE',  ( 3.000000000000000888, -20.41249101028218149, 9.589108953447823325 ) ) ;
#8242=AXIS2_PLACEMENT_3D ( 'NONE', #11488, #4152, #6038 ) ;
#8244=DIRECTION ( 'NONE',  ( 0.000000000000000000, 0.000000000000000000, 1.000000000000000000 ) ) ;
#8245=DIRECTION ( 'NONE',  ( 0.000000000000000000, 0.000000000000000000, 1.000000000000000000 ) ) ;
#8246=VERTEX_POINT ( 'NONE', #1159 ) ;
#8247=EDGE_CURVE ( 'NONE', #531, #10744, #4960, .T. ) ;
#8249=ORIENTED_EDGE ( 'NONE', *, *, #7263, .F. ) ;
#8250=DIRECTION ( 'NONE',  ( -1.000000000000000000, -0.000000000000000000, -0.000000000000000000 ) ) ;
#8251=AXIS2_PLACEMENT_3D ( 'NONE', #10144, #4278, #1703 ) ;
#8252=EDGE_CURVE ( 'NONE', #8421, #8183, #6433, .T. ) ;
#8253=LINE ( 'NONE', #10139, #573 ) ;
#8254=EDGE_CURVE ( 'NONE', #9915, #10265, #964, .T. ) ;
#8255=DIRECTION ( 'NONE',  ( -1.000000000000000000, 0.000000000000000000, 0.000000000000000000 ) ) ;
#8256=DIRECTION ( 'NONE',  ( 0.000000000000000000, 0.000000000000000000, 1.000000000000000000 ) ) ;
#8257=CARTESIAN_POINT ( 'NONE',  ( 3.000000000000000888, -1.901833551798412847, 22.47229024614976822 ) ) ;
#8259=AXIS2_PLACEMENT_3D ( 'NONE', #8257, #8993, #11804 ) ;
#8260=FACE_OUTER_BOUND ( 'NONE', #8702, .T. ) ;
#8261=CARTESIAN_POINT ( 'NONE',  ( 0.000000000000000000, 21.30300407174362576, -7.402892494506364329 ) ) ;
#8262=ORIENTED_EDGE ( 'NONE', *, *, #8476, .F. ) ;
#8263=EDGE_LOOP ( 'NONE', ( #8638, #6032, #3152, #10630 ) ) ;
#8264=DIRECTION ( 'NONE',  ( -1.000000000000000000, 0.000000000000000000, -0.000000000000000000 ) ) ;
#8265=ORIENTED_EDGE ( 'NONE', *, *, #3694, .T. ) ;
#8266=ORIENTED_EDGE ( 'NONE', *, *, #6292, .F. ) ;
#8268=EDGE_CURVE ( 'NONE', #6126, #5192, #8973, .T. ) ;
#8269=ORIENTED_EDGE ( 'NONE', *, *, #11334, .F. ) ;
#8270=DIRECTION ( 'NONE',  ( 0.000000000000000000, 0.000000000000000000, 1.000000000000000000 ) ) ;
#8271=ORIENTED_EDGE ( 'NONE', *, *, #11033, .T. ) ;
#8274=CYLINDRICAL_SURFACE ( 'NONE', #10813, 9.599999999999997868 ) ;
#8275=VECTOR ( 'NONE', #921, 1000.000000000000000 ) ;
#8276=DIRECTION ( 'NONE',  ( -1.000000000000000000, 0.000000000000000000, -0.000000000000000000 ) ) ;
#8278=LINE ( 'NONE', #11875, #38 ) ;
#8279=EDGE_CURVE ( 'NONE', #962, #7624, #4681, .T. ) ;
#8280=CARTESIAN_POINT ( 'NONE',  ( 3.000000000000000888, 0.000000000000000000, 0.000000000000000000 ) ) ;
#8281=CIRCLE ( 'NONE', #8489, 9.599999999999996092 ) ;
#8282=CARTESIAN_POINT ( 'NONE',  ( 3.000000000000000888, 0.000000000000000000, 22.99899999999999878 ) ) ;
#8283=ORIENTED_EDGE ( 'NONE', *, *, #1054, .F. ) ;
#8285=DIRECTION ( 'NONE',  ( 0.000000000000000000, -0.6691306063588495778, -0.7431448254774020157 ) ) ;
#8286=CIRCLE ( 'NONE', #8495, 22.99899999999999878 ) ;
#8288=CARTESIAN_POINT ( 'NONE',  ( 3.000000000000000888, -7.432877647175053504, -21.76479567747249178 ) ) ;
#8289=CARTESIAN_POINT ( 'NONE',  ( 0.000000000000000000, 14.74749645580011226, 17.06259499759949705 ) ) ;
#8290=CYLINDRICAL_SURFACE ( 'NONE', #5709, 9.599999999999997868 ) ;
#8292=CARTESIAN_POINT ( 'NONE',  ( 3.000000000000000888, 6.168200451485758684, 24.02068490260614908 ) ) ;
#8294=ORIENTED_EDGE ( 'NONE', *, *, #8074, .T. ) ;
#8295=VERTEX_POINT ( 'NONE', #8987 ) ;
#8297=VERTEX_POINT ( 'NONE', #12022 ) ;
#8298=CARTESIAN_POINT ( 'NONE',  ( 3.000000000000000888, -22.99643626497956461, -0.3433949777334098785 ) ) ;
#8300=ADVANCED_FACE ( 'NONE', ( #3705 ), #9904, .T. ) ;
#8301=DIRECTION ( 'NONE',  ( 1.000000000000000000, 0.000000000000000000, 0.000000000000000000 ) ) ;
#8302=DIRECTION ( 'NONE',  ( 0.000000000000000000, 0.7431448254773955764, -0.6691306063588569053 ) ) ;
#8304=AXIS2_PLACEMENT_3D ( 'NONE', #4473, #2700, #684 ) ;
#8305=EDGE_CURVE ( 'NONE', #5168, #7882, #9756, .T. ) ;
#8307=CYLINDRICAL_SURFACE ( 'NONE', #1583, 22.99899999999999878 ) ;
#8308=ORIENTED_EDGE ( 'NONE', *, *, #10970, .F. ) ;
#8309=ADVANCED_FACE ( 'NONE', ( #4273 ), #6457, .T. ) ;
#8310=ORIENTED_EDGE ( 'NONE', *, *, #4108, .T. ) ;
#8311=ORIENTED_EDGE ( 'NONE', *, *, #179, .T. ) ;
#8312=EDGE_CURVE ( 'NONE', #10744, #7896, #7984, .T. ) ;
#8313=ORIENTED_EDGE ( 'NONE', *, *, #9218, .F. ) ;
#8316=DIRECTION ( 'NONE',  ( 0.000000000000000000, -1.000000000000000000, -1.047444401652940007E-14 ) ) ;
#8317=CARTESIAN_POINT ( 'NONE',  ( 3.000000000000000888, -22.56530478845645860, -4.445336973061090546 ) ) ;
#8319=DIRECTION ( 'NONE',  ( -1.000000000000000000, 0.000000000000000000, 0.000000000000000000 ) ) ;
#8320=DIRECTION ( 'NONE',  ( -1.000000000000000000, 0.000000000000000000, 0.000000000000000000 ) ) ;
#8323=CIRCLE ( 'NONE', #8119, 24.80000000000000071 ) ;
#8324=CARTESIAN_POINT ( 'NONE',  ( 0.000000000000000000, -15.13242714128107913, -17.31945870441162683 ) ) ;
#8325=DIRECTION ( 'NONE',  ( -1.000000000000000000, 0.000000000000000000, -0.000000000000000000 ) ) ;
#8326=ORIENTED_EDGE ( 'NONE', *, *, #5924, .F. ) ;
#8327=ORIENTED_EDGE ( 'NONE', *, *, #7310, .F. ) ;
#8328=CARTESIAN_POINT ( 'NONE',  ( 0.000000000000000000, 0.000000000000000000, 0.000000000000000000 ) ) ;
#8329=VERTEX_POINT ( 'NONE', #1808 ) ;
#8331=VERTEX_POINT ( 'NONE', #5477 ) ;
#8332=CYLINDRICAL_SURFACE ( 'NONE', #11068, 22.99899999999999878 ) ;
#8333=VECTOR ( 'NONE', #9625, 1000.000000000000000 ) ;
#8334=EDGE_LOOP ( 'NONE', ( #5631, #4876, #347, #4786 ) ) ;
#8336=CARTESIAN_POINT ( 'NONE',  ( 3.000000000000000888, -9.039786367038701087, -21.14796121233205284 ) ) ;
#8339=ADVANCED_FACE ( 'NONE', ( #10886 ), #5547, .T. ) ;
#8341=ORIENTED_EDGE ( 'NONE', *, *, #5206, .F. ) ;
#8342=CIRCLE ( 'NONE', #5602, 24.80000000000000071 ) ;
#8343=VERTEX_POINT ( 'NONE', #9276 ) ;
#8344=DIRECTION ( 'NONE',  ( 0.000000000000000000, 0.8660254037844398178, -0.4999999999999979461 ) ) ;
#8345=ORIENTED_EDGE ( 'NONE', *, *, #218, .T. ) ;
#8349=EDGE_CURVE ( 'NONE', #4464, #11993, #4280, .T. ) ;
#8351=LINE ( 'NONE', #10984, #5555 ) ;
#8352=CARTESIAN_POINT ( 'NONE',  ( 3.000000000000000888, 19.75591328264900781, -10.87771529938142123 ) ) ;
#8357=VERTEX_POINT ( 'NONE', #7135 ) ;
#8358=ORIENTED_EDGE ( 'NONE', *, *, #998, .T. ) ;
#8359=DIRECTION ( 'NONE',  ( -1.000000000000000000, -0.000000000000000000, -0.000000000000000000 ) ) ;
#8361=CYLINDRICAL_SURFACE ( 'NONE', #6996, 22.99899999999999878 ) ;
#8362=CARTESIAN_POINT ( 'NONE',  ( 0.000000000000000000, 8.645255683529009971, 23.24434456306328300 ) ) ;
#8364=AXIS2_PLACEMENT_3D ( 'NONE', #5732, #3093, #11418 ) ;
#8366=VECTOR ( 'NONE', #2586, 1000.000000000000000 ) ;
#8367=CARTESIAN_POINT ( 'NONE',  ( 3.000000000000000888, 20.78471918669860941, 8.753070780933226658 ) ) ;
#8369=VERTEX_POINT ( 'NONE', #10254 ) ;
#8370=ORIENTED_EDGE ( 'NONE', *, *, #5338, .T. ) ;
#8371=ORIENTED_EDGE ( 'NONE', *, *, #3143, .F. ) ;
#8372=CARTESIAN_POINT ( 'NONE',  ( 3.000000000000000888, -16.45023496161675780, 15.42759117534379953 ) ) ;
#8374=VECTOR ( 'NONE', #10636, 1000.000000000000000 ) ;
#8375=DIRECTION ( 'NONE',  ( 1.000000000000000000, 0.000000000000000000, 0.000000000000000000 ) ) ;
#8376=CYLINDRICAL_SURFACE ( 'NONE', #9738, 9.599999999999997868 ) ;
#8377=CIRCLE ( 'NONE', #6423, 9.599999999999997868 ) ;
#8378=EDGE_CURVE ( 'NONE', #5811, #6304, #9334, .T. ) ;
#8379=DIRECTION ( 'NONE',  ( -1.000000000000000000, -0.000000000000000000, 0.000000000000000000 ) ) ;
#8380=EDGE_CURVE ( 'NONE', #10824, #1101, #11515, .T. ) ;
#8383=EDGE_CURVE ( 'NONE', #6456, #622, #173, .T. ) ;
#8384=CARTESIAN_POINT ( 'NONE',  ( 3.000000000000000888, 1.901833551798254973, 22.47229024614977888 ) ) ;
#8385=AXIS2_PLACEMENT_3D ( 'NONE', #7888, #476, #8873 ) ;
#8386=ORIENTED_EDGE ( 'NONE', *, *, #3518, .T. ) ;
#8387=ORIENTED_EDGE ( 'NONE', *, *, #7114, .F. ) ;
#8388=CYLINDRICAL_SURFACE ( 'NONE', #2358, 24.80000000000000071 ) ;
#8390=FACE_OUTER_BOUND ( 'NONE', #7494, .T. ) ;
#8391=CARTESIAN_POINT ( 'NONE',  ( 0.000000000000000000, 9.667200211210106531, -20.86861857134724474 ) ) ;
#8394=AXIS2_PLACEMENT_3D ( 'NONE', #9544, #6838, #1224 ) ;
#8396=DIRECTION ( 'NONE',  ( -1.000000000000000000, 0.000000000000000000, 0.000000000000000000 ) ) ;
#8398=DIRECTION ( 'NONE',  ( -1.000000000000000000, 0.000000000000000000, 0.000000000000000000 ) ) ;
#8399=CARTESIAN_POINT ( 'NONE',  ( 3.000000000000000888, 0.000000000000000000, 0.000000000000000000 ) ) ;
#8400=CARTESIAN_POINT ( 'NONE',  ( 0.000000000000000000, 0.000000000000000000, 0.000000000000000000 ) ) ;
#8401=DIRECTION ( 'NONE',  ( -1.000000000000000000, 0.000000000000000000, 0.000000000000000000 ) ) ;
#8402=ORIENTED_EDGE ( 'NONE', *, *, #5843, .T. ) ;
#8403=AXIS2_PLACEMENT_3D ( 'NONE', #1282, #5015, #8751 ) ;
#8404=CIRCLE ( 'NONE', #6823, 22.99900000000000233 ) ;
#8405=EDGE_CURVE ( 'NONE', #246, #8841, #2439, .T. ) ;
#8407=AXIS2_PLACEMENT_3D ( 'NONE', #10936, #10134, #1986 ) ;
#8408=LINE ( 'NONE', #5718, #4620 ) ;
#8410=DIRECTION ( 'NONE',  ( -1.000000000000000000, -0.000000000000000000, 0.000000000000000000 ) ) ;
#8411=CARTESIAN_POINT ( 'NONE',  ( 3.000000000000000888, -5.117118920208643118, 22.42251312757878168 ) ) ;
#8413=AXIS2_PLACEMENT_3D ( 'NONE', #3164, #5796, #2059 ) ;
#8415=CARTESIAN_POINT ( 'NONE',  ( 0.000000000000000000, 22.83456483164692941, -2.745295967525760439 ) ) ;
#8416=CIRCLE ( 'NONE', #6831, 9.599999999999997868 ) ;
#8419=EDGE_CURVE ( 'NONE', #429, #7212, #8787, .T. ) ;
#8421=VERTEX_POINT ( 'NONE', #2395 ) ;
#8422=EDGE_LOOP ( 'NONE', ( #11439, #6005, #10628, #4170 ) ) ;
#8424=DIRECTION ( 'NONE',  ( -1.000000000000000000, -0.000000000000000000, -0.000000000000000000 ) ) ;
#8425=AXIS2_PLACEMENT_3D ( 'NONE', #6061, #8010, #7897 ) ;
#8427=CIRCLE ( 'NONE', #1573, 9.599999999999997868 ) ;
#8428=CARTESIAN_POINT ( 'NONE',  ( 3.000000000000000888, 15.80756504416717334, -19.10918332567941746 ) ) ;
#8429=DIRECTION ( 'NONE',  ( -1.000000000000000000, 0.000000000000000000, 0.000000000000000000 ) ) ;
#8432=CARTESIAN_POINT ( 'NONE',  ( 0.000000000000000000, -20.08719549084857192, -11.20082935824096459 ) ) ;
#8433=AXIS2_PLACEMENT_3D ( 'NONE', #991, #5402, #4548 ) ;
#8434=DIRECTION ( 'NONE',  ( -1.000000000000000000, 0.000000000000000000, 0.000000000000000000 ) ) ;
#8435=CIRCLE ( 'NONE', #4520, 9.600000000000001421 ) ;
#8436=ORIENTED_EDGE ( 'NONE', *, *, #5368, .T. ) ;
#8437=ADVANCED_FACE ( 'NONE', ( #909 ), #5563, .T. ) ;
#8438=EDGE_CURVE ( 'NONE', #2943, #6856, #7400, .T. ) ;
#8439=AXIS2_PLACEMENT_3D ( 'NONE', #8328, #3554, #11021 ) ;
#8440=EDGE_LOOP ( 'NONE', ( #747, #9046, #676, #5146 ) ) ;
#8441=EDGE_LOOP ( 'NONE', ( #10909, #4602, #1655, #7620 ) ) ;
#8442=CARTESIAN_POINT ( 'NONE',  ( 0.000000000000000000, -22.42251312757876036, -5.117118920208720390 ) ) ;
#8443=CARTESIAN_POINT ( 'NONE',  ( 0.000000000000000000, 3.623565124517433400, -24.53384959170453783 ) ) ;
#8445=DIRECTION ( 'NONE',  ( -1.000000000000000000, 0.000000000000000000, 0.000000000000000000 ) ) ;
#8447=CIRCLE ( 'NONE', #7642, 22.99899999999999523 ) ;
#8448=DIRECTION ( 'NONE',  ( 0.000000000000000000, 0.000000000000000000, -1.000000000000000000 ) ) ;
#8451=AXIS2_PLACEMENT_3D ( 'NONE', #1122, #3879, #2100 ) ;
#8452=DIRECTION ( 'NONE',  ( -1.000000000000000000, -0.000000000000000000, -0.000000000000000000 ) ) ;
#8453=ORIENTED_EDGE ( 'NONE', *, *, #9789, .T. ) ;
#8454=ORIENTED_EDGE ( 'NONE', *, *, #2993, .F. ) ;
#8455=CARTESIAN_POINT ( 'NONE',  ( 0.000000000000000000, 0.000000000000000000, 0.000000000000000000 ) ) ;
#8456=CIRCLE ( 'NONE', #3173, 9.599999999999996092 ) ;
#8457=EDGE_LOOP ( 'NONE', ( #8326, #7327, #1952, #2577 ) ) ;
#8458=VERTEX_POINT ( 'NONE', #8317 ) ;
#8459=DIRECTION ( 'NONE',  ( 1.000000000000000000, 0.000000000000000000, 0.000000000000000000 ) ) ;
#8460=DIRECTION ( 'NONE',  ( 0.000000000000000000, 0.000000000000000000, 1.000000000000000000 ) ) ;
#8461=ORIENTED_EDGE ( 'NONE', *, *, #8616, .F. ) ;
#8462=EDGE_CURVE ( 'NONE', #6967, #3076, #8087, .T. ) ;
#8464=CIRCLE ( 'NONE', #4543, 9.599999999999997868 ) ;
#8465=CARTESIAN_POINT ( 'NONE',  ( 3.000000000000000888, 0.000000000000000000, 0.000000000000000000 ) ) ;
#8466=LINE ( 'NONE', #925, #10602 ) ;
#8469=DIRECTION ( 'NONE',  ( 0.000000000000000000, -0.5877852522924630341, -0.8090169943749546677 ) ) ;
#8470=ORIENTED_EDGE ( 'NONE', *, *, #771, .F. ) ;
#8471=CARTESIAN_POINT ( 'NONE',  ( 1.500000000000000444, -19.43515443678412780, 15.40502424595139530 ) ) ;
#8472=ORIENTED_EDGE ( 'NONE', *, *, #1342, .F. ) ;
#8473=EDGE_CURVE ( 'NONE', #11218, #3365, #3700, .T. ) ;
#8474=AXIS2_PLACEMENT_3D ( 'NONE', #1674, #1551, #2653 ) ;
#8476=EDGE_CURVE ( 'NONE', #11323, #12055, #8598, .T. ) ;
#8477=AXIS2_PLACEMENT_3D ( 'NONE', #11589, #7729, #8838 ) ;
#8478=CYLINDRICAL_SURFACE ( 'NONE', #1095, 9.599999999999996092 ) ;
#8480=DIRECTION ( 'NONE',  ( 1.000000000000000000, -0.000000000000000000, 0.000000000000000000 ) ) ;
#8482=AXIS2_PLACEMENT_3D ( 'NONE', #10228, #7646, #4780 ) ;
#8484=CYLINDRICAL_SURFACE ( 'NONE', #1760, 9.599999999999997868 ) ;
#8485=AXIS2_PLACEMENT_3D ( 'NONE', #6839, #4274, #10701 ) ;
#8486=VERTEX_POINT ( 'NONE', #3380 ) ;
#8487=FACE_OUTER_BOUND ( 'NONE', #7009, .T. ) ;
#8488=ORIENTED_EDGE ( 'NONE', *, *, #6499, .F. ) ;
#8489=AXIS2_PLACEMENT_3D ( 'NONE', #10891, #5199, #11016 ) ;
#8494=DIRECTION ( 'NONE',  ( 1.000000000000000000, -0.000000000000000000, -0.000000000000000000 ) ) ;
#8495=AXIS2_PLACEMENT_3D ( 'NONE', #9934, #2992, #10451 ) ;
#8496=CARTESIAN_POINT ( 'NONE',  ( 3.000000000000000888, 13.23915371906955052, 18.80635025205174671 ) ) ;
#8497=ORIENTED_EDGE ( 'NONE', *, *, #5552, .F. ) ;
#8498=EDGE_CURVE ( 'NONE', #10826, #10797, #10534, .T. ) ;
#8500=VERTEX_POINT ( 'NONE', #6194 ) ;
#8501=ORIENTED_EDGE ( 'NONE', *, *, #5312, .T. ) ;
#8502=LINE ( 'NONE', #7621, #59 ) ;
#8503=CARTESIAN_POINT ( 'NONE',  ( 1.500000000000000444, -23.05871956130128808, 9.128825345752947129 ) ) ;
#8504=CIRCLE ( 'NONE', #9273, 22.99900000000000233 ) ;
#8505=DIRECTION ( 'NONE',  ( 0.000000000000000000, 0.000000000000000000, 1.000000000000000000 ) ) ;
#8506=CARTESIAN_POINT ( 'NONE',  ( 3.000000000000000888, 0.000000000000000000, 0.000000000000000000 ) ) ;
#8507=EDGE_CURVE ( 'NONE', #5406, #10107, #1534, .T. ) ;
#8508=DIRECTION ( 'NONE',  ( 0.000000000000000000, 0.000000000000000000, 1.000000000000000000 ) ) ;
#8511=VERTEX_POINT ( 'NONE', #11979 ) ;
#8512=VERTEX_POINT ( 'NONE', #3608 ) ;
#8514=EDGE_LOOP ( 'NONE', ( #4696, #8141, #9970, #8527 ) ) ;
#8515=DIRECTION ( 'NONE',  ( -1.000000000000000000, -0.000000000000000000, -0.000000000000000000 ) ) ;
#8518=DIRECTION ( 'NONE',  ( -1.000000000000000000, 0.000000000000000000, 0.000000000000000000 ) ) ;
#8519=AXIS2_PLACEMENT_3D ( 'NONE', #9818, #5165, #3327 ) ;
#8520=CARTESIAN_POINT ( 'NONE',  ( 3.000000000000000888, 16.45023496161686438, -15.42759117534368407 ) ) ;
#8522=LINE ( 'NONE', #5126, #3371 ) ;
#8523=DIRECTION ( 'NONE',  ( 0.000000000000000000, 0.000000000000000000, 1.000000000000000000 ) ) ;
#8524=ORIENTED_EDGE ( 'NONE', *, *, #5798, .T. ) ;
#8525=ORIENTED_EDGE ( 'NONE', *, *, #1092, .F. ) ;
#8526=DIRECTION ( 'NONE',  ( 0.000000000000000000, 0.000000000000000000, 1.000000000000000000 ) ) ;
#8527=ORIENTED_EDGE ( 'NONE', *, *, #8473, .T. ) ;
#8528=AXIS2_PLACEMENT_3D ( 'NONE', #10962, #2640, #10158 ) ;
#8530=EDGE_CURVE ( 'NONE', #4684, #2848, #5260, .T. ) ;
#8532=DIRECTION ( 'NONE',  ( -1.000000000000000000, 0.000000000000000000, 0.000000000000000000 ) ) ;
#8533=CYLINDRICAL_SURFACE ( 'NONE', #673, 9.599999999999997868 ) ;
#8537=CARTESIAN_POINT ( 'NONE',  ( 3.000000000000000888, 11.67026512804572924, -19.29833442572348190 ) ) ;
#8538=DIRECTION ( 'NONE',  ( 0.000000000000000000, 0.8660254037844363761, 0.5000000000000039968 ) ) ;
#8539=EDGE_CURVE ( 'NONE', #5263, #505, #7204, .T. ) ;
#8540=CARTESIAN_POINT ( 'NONE',  ( 3.000000000000000888, -16.85990652506889376, -15.64281154287614584 ) ) ;
#8541=VERTEX_POINT ( 'NONE', #6473 ) ;
#8542=EDGE_CURVE ( 'NONE', #8125, #10492, #4482, .T. ) ;
#8543=CARTESIAN_POINT ( 'NONE',  ( -10.00000000000000000, 0.000000000000000000, 0.000000000000000000 ) ) ;
#8544=ORIENTED_EDGE ( 'NONE', *, *, #11382, .F. ) ;
#8548=CARTESIAN_POINT ( 'NONE',  ( 3.000000000000000888, 22.54798042742718067, -0.4575788569252652871 ) ) ;
#8551=DIRECTION ( 'NONE',  ( -1.000000000000000000, 0.000000000000000000, 0.000000000000000000 ) ) ;
#8552=ORIENTED_EDGE ( 'NONE', *, *, #4492, .T. ) ;
#8554=ORIENTED_EDGE ( 'NONE', *, *, #10555, .T. ) ;
#8555=CARTESIAN_POINT ( 'NONE',  ( 3.000000000000000888, 0.000000000000000000, 0.000000000000000000 ) ) ;
#8556=EDGE_CURVE ( 'NONE', #900, #2329, #6648, .T. ) ;
#8557=DIRECTION ( 'NONE',  ( -1.000000000000000000, 0.000000000000000000, -0.000000000000000000 ) ) ;
#8559=DIRECTION ( 'NONE',  ( -1.000000000000000000, 0.000000000000000000, 0.000000000000000000 ) ) ;
#8560=EDGE_CURVE ( 'NONE', #1454, #8857, #11324, .T. ) ;
#8561=AXIS2_PLACEMENT_3D ( 'NONE', #4489, #8220, #2654 ) ;
#8564=EDGE_CURVE ( 'NONE', #7059, #2212, #765, .T. ) ;
#8565=DIRECTION ( 'NONE',  ( -1.000000000000000000, -0.000000000000000000, 0.000000000000000000 ) ) ;
#8566=VERTEX_POINT ( 'NONE', #3847 ) ;
#8567=ORIENTED_EDGE ( 'NONE', *, *, #148, .T. ) ;
#8570=ADVANCED_FACE ( 'NONE', ( #5750 ), #6590, .T. ) ;
#8571=EDGE_LOOP ( 'NONE', ( #5117, #310, #8753, #11647 ) ) ;
#8572=AXIS2_PLACEMENT_3D ( 'NONE', #4386, #4442, #8118 ) ;
#8573=CARTESIAN_POINT ( 'NONE',  ( 0.000000000000000000, -11.02759168516760013, 22.21333432029560129 ) ) ;
#8574=CYLINDRICAL_SURFACE ( 'NONE', #11465, 22.99899999999999878 ) ;
#8575=ORIENTED_EDGE ( 'NONE', *, *, #8507, .T. ) ;
#8576=DIRECTION ( 'NONE',  ( 0.000000000000000000, 0.2079116908177597312, -0.9781476007338056888 ) ) ;
#8580=AXIS2_PLACEMENT_3D ( 'NONE', #12084, #4441, #652 ) ;
#8581=LINE ( 'NONE', #9770, #7640 ) ;
#8582=EDGE_CURVE ( 'NONE', #2749, #5671, #6250, .T. ) ;
#8583=LINE ( 'NONE', #9676, #1606 ) ;
#8584=EDGE_LOOP ( 'NONE', ( #2957, #1338, #11541, #10462 ) ) ;
#8585=ORIENTED_EDGE ( 'NONE', *, *, #7139, .F. ) ;
#8586=FACE_OUTER_BOUND ( 'NONE', #10382, .T. ) ;
#8587=ORIENTED_EDGE ( 'NONE', *, *, #2946, .F. ) ;
#8589=AXIS2_PLACEMENT_3D ( 'NONE', #1506, #5423, #4506 ) ;
#8592=CARTESIAN_POINT ( 'NONE',  ( 1.500000000000000444, 17.35216073792440739, 17.71842311621535870 ) ) ;
#8593=CARTESIAN_POINT ( 'NONE',  ( 3.000000000000000888, 0.000000000000000000, 0.000000000000000000 ) ) ;
#8595=DIRECTION ( 'NONE',  ( -1.000000000000000000, -0.000000000000000000, 0.000000000000000000 ) ) ;
#8596=LINE ( 'NONE', #10541, #5342 ) ;
#8597=AXIS2_PLACEMENT_3D ( 'NONE', #2440, #7315, #6236 ) ;
#8598=CIRCLE ( 'NONE', #3308, 24.80000000000000071 ) ;
#8599=DIRECTION ( 'NONE',  ( -1.000000000000000000, -0.000000000000000000, 0.000000000000000000 ) ) ;
#8600=CARTESIAN_POINT ( 'NONE',  ( 1.499999999999999556, 23.05871956130122413, 9.128825345753105225 ) ) ;
#8601=EDGE_LOOP ( 'NONE', ( #6328, #2510, #4381, #10832 ) ) ;
#8602=ORIENTED_EDGE ( 'NONE', *, *, #2825, .T. ) ;
#8603=AXIS2_PLACEMENT_3D ( 'NONE', #7735, #11473, #5907 ) ;
#8607=CARTESIAN_POINT ( 'NONE',  ( -10.00000000000000000, 0.000000000000000000, 0.000000000000000000 ) ) ;
#8608=ADVANCED_FACE ( 'NONE', ( #10325 ), #1944, .T. ) ;
#8609=CIRCLE ( 'NONE', #1566, 9.599999999999997868 ) ;
#8612=FACE_OUTER_BOUND ( 'NONE', #5771, .T. ) ;
#8613=VERTEX_POINT ( 'NONE', #2868 ) ;
#8614=VECTOR ( 'NONE', #3020, 1000.000000000000000 ) ;
#8615=ORIENTED_EDGE ( 'NONE', *, *, #7814, .T. ) ;
#8616=EDGE_CURVE ( 'NONE', #11379, #8825, #8404, .T. ) ;
#8617=CYLINDRICAL_SURFACE ( 'NONE', #2295, 24.80000000000000071 ) ;
#8618=DIRECTION ( 'NONE',  ( 1.000000000000000000, 0.000000000000000000, 0.000000000000000000 ) ) ;
#8619=ADVANCED_FACE ( 'NONE', ( #2121 ), #1212, .T. ) ;
#8621=CARTESIAN_POINT ( 'NONE',  ( 3.000000000000000888, 0.000000000000000000, 0.000000000000000000 ) ) ;
#8622=CARTESIAN_POINT ( 'NONE',  ( 1.499999999999999556, 23.05871956130134492, -9.128825345752797915 ) ) ;
#8624=VECTOR ( 'NONE', #11205, 1000.000000000000000 ) ;
#8626=EDGE_CURVE ( 'NONE', #8200, #10186, #4949, .T. ) ;
#8627=CYLINDRICAL_SURFACE ( 'NONE', #1356, 22.99899999999999878 ) ;
#8629=VERTEX_POINT ( 'NONE', #7567 ) ;
#8631=ORIENTED_EDGE ( 'NONE', *, *, #5449, .F. ) ;
#8632=AXIS2_PLACEMENT_3D ( 'NONE', #5768, #9491, #178 ) ;
#8633=ADVANCED_FACE ( 'NONE', ( #2186 ), #11309, .T. ) ;
#8634=DIRECTION ( 'NONE',  ( -1.000000000000000000, 0.000000000000000000, -0.000000000000000000 ) ) ;
#8635=DIRECTION ( 'NONE',  ( 1.000000000000000000, 0.000000000000000000, -0.000000000000000000 ) ) ;
#8636=CIRCLE ( 'NONE', #1403, 9.599999999999996092 ) ;
#8638=ORIENTED_EDGE ( 'NONE', *, *, #3898, .F. ) ;
#8639=DIRECTION ( 'NONE',  ( 0.000000000000000000, 0.000000000000000000, 1.000000000000000000 ) ) ;
#8640=CARTESIAN_POINT ( 'NONE',  ( 3.000000000000000888, 0.000000000000000000, 0.000000000000000000 ) ) ;
#8642=PRODUCT ( 'spring holder_ISO - Spur gear 0.8M 60T 20PA 3FW ---S60A75H50L8.0N', 'spring holder_ISO - Spur gear 0.8M 60T 20PA 3FW ---S60A75H50L8.0N', '', ( #10016 ) ) ;
#8644=ORIENTED_EDGE ( 'NONE', *, *, #10053, .F. ) ;
#8645=CIRCLE ( 'NONE', #7058, 9.599999999999997868 ) ;
#8646=FACE_OUTER_BOUND ( 'NONE', #10235, .T. ) ;
#8647=VERTEX_POINT ( 'NONE', #3903 ) ;
#8648=CARTESIAN_POINT ( 'NONE',  ( 0.000000000000000000, 0.000000000000000000, 0.000000000000000000 ) ) ;
#8649=ORIENTED_EDGE ( 'NONE', *, *, #2927, .T. ) ;
#8650=EDGE_CURVE ( 'NONE', #2737, #6263, #574, .T. ) ;
#8653=CIRCLE ( 'NONE', #10398, 24.80000000000000071 ) ;
#8654=DIRECTION ( 'NONE',  ( -1.000000000000000000, 0.000000000000000000, 0.000000000000000000 ) ) ;
#8655=ORIENTED_EDGE ( 'NONE', *, *, #1429, .T. ) ;
#8658=EDGE_CURVE ( 'NONE', #6529, #8051, #7412, .T. ) ;
#8661=FILL_AREA_STYLE_COLOUR ( '', #1995 ) ;
#8664=COLOUR_RGB ( '', 0.09019608, 0.27058824, 0.51372549) ;
#8665=ORIENTED_EDGE ( 'NONE', *, *, #10289, .T. ) ;
#8666=CARTESIAN_POINT ( 'NONE',  ( 3.000000000000000888, 0.000000000000000000, 0.000000000000000000 ) ) ;
#8667=ORIENTED_EDGE ( 'NONE', *, *, #11682, .F. ) ;
#8668=DIRECTION ( 'NONE',  ( 0.000000000000000000, 0.4067366430758009299, -0.9135454576426005335 ) ) ;
#8670=AXIS2_PLACEMENT_3D ( 'NONE', #11390, #6551, #10285 ) ;
#8671=LINE ( 'NONE', #271, #5252 ) ;
#8675=DIRECTION ( 'NONE',  ( -1.000000000000000000, -0.000000000000000000, 0.000000000000000000 ) ) ;
#8676=ORIENTED_EDGE ( 'NONE', *, *, #9508, .T. ) ;
#8678=EDGE_CURVE ( 'NONE', #2346, #2635, #1556, .T. ) ;
#8680=DIRECTION ( 'NONE',  ( -1.000000000000000000, -0.000000000000000000, -0.000000000000000000 ) ) ;
#8681=CARTESIAN_POINT ( 'NONE',  ( 3.000000000000000888, 9.667200211210106531, -20.86861857134724474 ) ) ;
#8682=EDGE_CURVE ( 'NONE', #10975, #8500, #3708, .T. ) ;
#8683=DIRECTION ( 'NONE',  ( 1.000000000000000000, 0.000000000000000000, 0.000000000000000000 ) ) ;
#8684=DIRECTION ( 'NONE',  ( 0.000000000000000000, -1.000000000000000000, -1.048062100069321321E-14 ) ) ;
#8685=CIRCLE ( 'NONE', #3410, 9.599999999999997868 ) ;
#8686=AXIS2_PLACEMENT_3D ( 'NONE', #8849, #10735, #1437 ) ;
#8688=EDGE_CURVE ( 'NONE', #9879, #8749, #7751, .T. ) ;
#8689=EDGE_CURVE ( 'NONE', #5268, #7198, #11430, .T. ) ;
#8691=ORIENTED_EDGE ( 'NONE', *, *, #6297, .F. ) ;
#8692=ORIENTED_EDGE ( 'NONE', *, *, #9569, .F. ) ;
#8693=EDGE_CURVE ( 'NONE', #5028, #1910, #5982, .T. ) ;
#8696=VERTEX_POINT ( 'NONE', #9893 ) ;
#8697=AXIS2_PLACEMENT_3D ( 'NONE', #9740, #5090, #8835 ) ;
#8699=CARTESIAN_POINT ( 'NONE',  ( 1.500000000000000444, 1.556492618230968628, -24.75110766671650708 ) ) ;
#8700=CARTESIAN_POINT ( 'NONE',  ( 3.000000000000000888, 13.28910708463127932, 20.93895013827586027 ) ) ;
#8702=EDGE_LOOP ( 'NONE', ( #5977, #2192, #4368, #10150 ) ) ;
#8703=CYLINDRICAL_SURFACE ( 'NONE', #844, 9.599999999999997868 ) ;
#8704=CARTESIAN_POINT ( 'NONE',  ( 1.500000000000000444, -15.80756504416703656, 19.10918332567953115 ) ) ;
#8706=VERTEX_POINT ( 'NONE', #2425 ) ;
#8707=DIRECTION ( 'NONE',  ( -1.000000000000000000, 0.000000000000000000, -0.000000000000000000 ) ) ;
#8708=CARTESIAN_POINT ( 'NONE',  ( 0.000000000000000000, 20.86861857134747567, -9.667200211209610927 ) ) ;
#8712=CARTESIAN_POINT ( 'NONE',  ( 3.000000000000000888, 22.42251312757886339, -5.117118920208268307 ) ) ;
#8713=ORIENTED_EDGE ( 'NONE', *, *, #145, .F. ) ;
#8714=DIRECTION ( 'NONE',  ( 0.000000000000000000, 0.000000000000000000, 1.000000000000000000 ) ) ;
#8715=CARTESIAN_POINT ( 'NONE',  ( 3.000000000000000888, -4.135161237383403687, -24.45282072769605364 ) ) ;
#8717=ADVANCED_FACE ( 'NONE', ( #9654 ), #10816, .T. ) ;
#8718=LINE ( 'NONE', #11409, #2184 ) ;
#8720=FACE_OUTER_BOUND ( 'NONE', #5543, .T. ) ;
#8721=CIRCLE ( 'NONE', #3829, 24.80000000000000071 ) ;
#8722=CYLINDRICAL_SURFACE ( 'NONE', #9582, 9.599999999999997868 ) ;
#8723=ORIENTED_EDGE ( 'NONE', *, *, #998, .F. ) ;
#8724=EDGE_CURVE ( 'NONE', #3881, #11808, #10327, .T. ) ;
#8725=ORIENTED_EDGE ( 'NONE', *, *, #6144, .F. ) ;
#8726=FACE_OUTER_BOUND ( 'NONE', #3328, .T. ) ;
#8728=DIRECTION ( 'NONE',  ( 0.000000000000000000, 0.000000000000000000, -1.000000000000000000 ) ) ;
#8729=CIRCLE ( 'NONE', #7335, 9.599999999999997868 ) ;
#8730=CARTESIAN_POINT ( 'NONE',  ( 3.000000000000000888, 17.97274125076074114, 13.62355943574025652 ) ) ;
#8735=VERTEX_POINT ( 'NONE', #11609 ) ;
#8736=CIRCLE ( 'NONE', #12041, 9.599999999999997868 ) ;
#8737=EDGE_LOOP ( 'NONE', ( #5525, #3685, #10627, #5314 ) ) ;
#8738=CYLINDRICAL_SURFACE ( 'NONE', #3576, 24.80000000000000071 ) ;
#8739=DIRECTION ( 'NONE',  ( -1.000000000000000000, -0.000000000000000000, 0.000000000000000000 ) ) ;
#8740=CARTESIAN_POINT ( 'NONE',  ( 0.000000000000000000, 19.75591328264886215, 10.87771529938168946 ) ) ;
#8741=CARTESIAN_POINT ( 'NONE',  ( 0.000000000000000000, -19.10918332567968037, 15.80756504416684649 ) ) ;
#8744=DIRECTION ( 'NONE',  ( 0.000000000000000000, -0.9945218953682721796, -0.1045284632676635878 ) ) ;
#8745=VERTEX_POINT ( 'NONE', #1322 ) ;
#8746=VERTEX_POINT ( 'NONE', #7124 ) ;
#8748=CARTESIAN_POINT ( 'NONE',  ( 3.000000000000000888, 21.30300407174352983, 7.402892494506653875 ) ) ;
#8749=VERTEX_POINT ( 'NONE', #7000 ) ;
#8750=CARTESIAN_POINT ( 'NONE',  ( 3.000000000000000888, -17.71842311621541555, 17.35216073792435054 ) ) ;
#8751=DIRECTION ( 'NONE',  ( 0.000000000000000000, 0.000000000000000000, 1.000000000000000000 ) ) ;
#8752=DIRECTION ( 'NONE',  ( 0.000000000000000000, -0.8660254037844431485, 0.4999999999999920619 ) ) ;
#8753=ORIENTED_EDGE ( 'NONE', *, *, #4582, .T. ) ;
#8755=DIRECTION ( 'NONE',  ( -1.000000000000000000, 0.000000000000000000, -0.000000000000000000 ) ) ;
#8757=EDGE_CURVE ( 'NONE', #277, #7198, #9930, .T. ) ;
#8758=DIRECTION ( 'NONE',  ( -1.000000000000000000, 0.000000000000000000, 0.000000000000000000 ) ) ;
#8760=ORIENTED_EDGE ( 'NONE', *, *, #3169, .F. ) ;
#8762=VECTOR ( 'NONE', #2097, 1000.000000000000000 ) ;
#8763=DIRECTION ( 'NONE',  ( 0.000000000000000000, 0.000000000000000000, 1.000000000000000000 ) ) ;
#8764=ORIENTED_EDGE ( 'NONE', *, *, #5860, .F. ) ;
#8766=ADVANCED_FACE ( 'NONE', ( #4149, #7063 ), #11549, .F. ) ;
#8767=DIRECTION ( 'NONE',  ( 0.000000000000000000, 0.000000000000000000, 1.000000000000000000 ) ) ;
#8772=DIRECTION ( 'NONE',  ( -1.000000000000000000, -0.000000000000000000, 0.000000000000000000 ) ) ;
#8775=DIRECTION ( 'NONE',  ( 0.000000000000000000, 0.3090169943749416781, 0.9510565162951555296 ) ) ;
#8777=DIRECTION ( 'NONE',  ( -1.000000000000000000, -0.000000000000000000, 0.000000000000000000 ) ) ;
#8778=VERTEX_POINT ( 'NONE', #3226 ) ;
#8779=AXIS2_PLACEMENT_3D ( 'NONE', #3120, #11563, #2133 ) ;
#8780=ORIENTED_EDGE ( 'NONE', *, *, #4086, .F. ) ;
#8781=EDGE_CURVE ( 'NONE', #9635, #2061, #3884, .T. ) ;
#8782=DIRECTION ( 'NONE',  ( -1.000000000000000000, -0.000000000000000000, -0.000000000000000000 ) ) ;
#8786=AXIS2_PLACEMENT_3D ( 'NONE', #10208, #1144, #6711 ) ;
#8787=CIRCLE ( 'NONE', #10930, 9.599999999999997868 ) ;
#8790=EDGE_CURVE ( 'NONE', #6967, #8912, #6224, .T. ) ;
#8791=DIRECTION ( 'NONE',  ( -1.000000000000000000, 0.000000000000000000, 0.000000000000000000 ) ) ;
#8792=ORIENTED_EDGE ( 'NONE', *, *, #8247, .F. ) ;
#8793=ORIENTED_EDGE ( 'NONE', *, *, #10247, .T. ) ;
#8794=ORIENTED_EDGE ( 'NONE', *, *, #9908, .T. ) ;
#8795=CARTESIAN_POINT ( 'NONE',  ( 0.000000000000000000, -7.432877647175055280, -21.76479567747249533 ) ) ;
#8797=VECTOR ( 'NONE', #8923, 1000.000000000000000 ) ;
#8798=CARTESIAN_POINT ( 'NONE',  ( 1.500000000000000444, 8.645255683529310176, -23.24434456306316577 ) ) ;
#8799=EDGE_CURVE ( 'NONE', #3556, #4581, #2362, .T. ) ;
#8801=AXIS2_PLACEMENT_3D ( 'NONE', #2607, #10923, #9827 ) ;
#8802=AXIS2_PLACEMENT_3D ( 'NONE', #198, #1305, #7733 ) ;
#8803=CARTESIAN_POINT ( 'NONE',  ( 0.000000000000000000, 18.80635025205187816, -13.23915371906935867 ) ) ;
#8804=ORIENTED_EDGE ( 'NONE', *, *, #3890, .T. ) ;
#8808=VERTEX_POINT ( 'NONE', #1633 ) ;
#8809=LINE ( 'NONE', #2198, #956 ) ;
#8811=AXIS2_PLACEMENT_3D ( 'NONE', #9744, #8840, #8896 ) ;
#8813=CARTESIAN_POINT ( 'NONE',  ( 3.000000000000000888, 0.000000000000000000, 0.000000000000000000 ) ) ;
#8814=AXIS2_PLACEMENT_3D ( 'NONE', #858, #1832, #5625 ) ;
#8816=AXIS2_PLACEMENT_3D ( 'NONE', #10169, #9319, #10236 ) ;
#8817=CARTESIAN_POINT ( 'NONE',  ( 3.000000000000000888, 0.000000000000000000, 0.000000000000000000 ) ) ;
#8818=FACE_OUTER_BOUND ( 'NONE', #4699, .T. ) ;
#8820=VERTEX_POINT ( 'NONE', #8240 ) ;
#8822=CARTESIAN_POINT ( 'NONE',  ( 0.000000000000000000, 20.86861857134734421, 9.667200211209893368 ) ) ;
#8823=VECTOR ( 'NONE', #6612, 1000.000000000000000 ) ;
#8824=DIRECTION ( 'NONE',  ( 0.000000000000000000, 0.000000000000000000, -1.000000000000000000 ) ) ;
#8825=VERTEX_POINT ( 'NONE', #8117 ) ;
#8826=EDGE_CURVE ( 'NONE', #9539, #532, #2909, .T. ) ;
#8828=ORIENTED_EDGE ( 'NONE', *, *, #10507, .T. ) ;
#8829=CARTESIAN_POINT ( 'NONE',  ( 3.000000000000000888, 14.74749645580011226, 17.06259499759949705 ) ) ;
#8830=ORIENTED_EDGE ( 'NONE', *, *, #904, .F. ) ;
#8831=CIRCLE ( 'NONE', #4915, 22.99899999999999523 ) ;
#8832=EDGE_CURVE ( 'NONE', #2073, #7721, #7182, .T. ) ;
#8835=DIRECTION ( 'NONE',  ( 0.000000000000000000, 0.000000000000000000, 1.000000000000000000 ) ) ;
#8837=DIRECTION ( 'NONE',  ( 0.000000000000000000, 0.9510565162951521989, 0.3090169943749515036 ) ) ;
#8838=DIRECTION ( 'NONE',  ( 0.000000000000000000, 0.000000000000000000, 1.000000000000000000 ) ) ;
#8840=DIRECTION ( 'NONE',  ( -1.000000000000000000, -0.000000000000000000, -0.000000000000000000 ) ) ;
#8841=VERTEX_POINT ( 'NONE', #6348 ) ;
#8842=DIRECTION ( 'NONE',  ( 0.000000000000000000, 0.7431448254773954654, -0.6691306063588569053 ) ) ;
#8843=EDGE_CURVE ( 'NONE', #11556, #916, #4630, .T. ) ;
#8844=( GEOMETRIC_REPRESENTATION_CONTEXT ( 3 ) GLOBAL_UNCERTAINTY_ASSIGNED_CONTEXT ( ( #8932 ) ) GLOBAL_UNIT_ASSIGNED_CONTEXT ( ( #5960, #9687, #5037 ) ) REPRESENTATION_CONTEXT ( 'NONE', 'WORKASPACE' ) );
#8845=ORIENTED_EDGE ( 'NONE', *, *, #7057, .T. ) ;
#8846=AXIS2_PLACEMENT_3D ( 'NONE', #358, #4100, #7833 ) ;
#8847=CARTESIAN_POINT ( 'NONE',  ( 3.000000000000000888, 14.74749645580034496, -17.06259499759930165 ) ) ;
#8848=DIRECTION ( 'NONE',  ( 0.000000000000000000, 0.000000000000000000, 1.000000000000000000 ) ) ;
#8849=CARTESIAN_POINT ( 'NONE',  ( 3.000000000000000888, 0.000000000000000000, 0.000000000000000000 ) ) ;
#8851=STYLED_ITEM ( 'NONE', ( #4487 ), #323 ) ;
#8853=DIRECTION ( 'NONE',  ( -1.000000000000000000, 0.000000000000000000, 0.000000000000000000 ) ) ;
#8854=DIRECTION ( 'NONE',  ( 0.000000000000000000, 0.000000000000000000, -1.000000000000000000 ) ) ;
#8856=ORIENTED_EDGE ( 'NONE', *, *, #2587, .F. ) ;
#8857=VERTEX_POINT ( 'NONE', #5480 ) ;
#8858=AXIS2_PLACEMENT_3D ( 'NONE', #4965, #6846, #7831 ) ;
#8859=LINE ( 'NONE', #4081, #2180 ) ;
#8860=CARTESIAN_POINT ( 'NONE',  ( 3.000000000000000888, 0.000000000000000000, 0.000000000000000000 ) ) ;
#8861=CIRCLE ( 'NONE', #2206, 24.80000000000000071 ) ;
#8862=FACE_OUTER_BOUND ( 'NONE', #4265, .T. ) ;
#8864=EDGE_CURVE ( 'NONE', #11729, #8857, #2123, .T. ) ;
#8865=AXIS2_PLACEMENT_3D ( 'NONE', #2627, #2443, #7140 ) ;
#8866=FACE_OUTER_BOUND ( 'NONE', #3688, .T. ) ;
#8867=CARTESIAN_POINT ( 'NONE',  ( 3.000000000000000888, 10.87771529938162196, 19.75591328264889768 ) ) ;
#8868=ORIENTED_EDGE ( 'NONE', *, *, #7934, .F. ) ;
#8869=EDGE_LOOP ( 'NONE', ( #9425, #7455, #2906, #10339 ) ) ;
#8870=VECTOR ( 'NONE', #1225, 1000.000000000000000 ) ;
#8872=ORIENTED_EDGE ( 'NONE', *, *, #8008, .T. ) ;
#8873=DIRECTION ( 'NONE',  ( 0.000000000000000000, 0.000000000000000000, 1.000000000000000000 ) ) ;
#8874=DIRECTION ( 'NONE',  ( -1.000000000000000000, -0.000000000000000000, 0.000000000000000000 ) ) ;
#8875=ADVANCED_FACE ( 'NONE', ( #9216 ), #8361, .T. ) ;
#8877=DIRECTION ( 'NONE',  ( -1.000000000000000000, 0.000000000000000000, 0.000000000000000000 ) ) ;
#8878=ORIENTED_EDGE ( 'NONE', *, *, #7814, .F. ) ;
#8882=EDGE_LOOP ( 'NONE', ( #164, #10614, #2405, #3167 ) ) ;
#8883=DIRECTION ( 'NONE',  ( -1.000000000000000000, 0.000000000000000000, 0.000000000000000000 ) ) ;
#8884=AXIS2_PLACEMENT_3D ( 'NONE', #10423, #5837, #10357 ) ;
#8885=DIRECTION ( 'NONE',  ( -1.000000000000000000, 0.000000000000000000, 0.000000000000000000 ) ) ;
#8886=VERTEX_POINT ( 'NONE', #10070 ) ;
#8888=CARTESIAN_POINT ( 'NONE',  ( 0.000000000000000000, -11.79560690673886292, 19.74380051311536022 ) ) ;
#8889=EDGE_LOOP ( 'NONE', ( #1686, #5634, #1547, #8934 ) ) ;
#8890=AXIS2_PLACEMENT_3D ( 'NONE', #1421, #8772, #5153 ) ;
#8892=CYLINDRICAL_SURFACE ( 'NONE', #7906, 22.99899999999999878 ) ;
#8894=CARTESIAN_POINT ( 'NONE',  ( 1.500000000000000444, 19.43515443678423793, -15.40502424595126030 ) ) ;
#8896=DIRECTION ( 'NONE',  ( 0.000000000000000000, 0.000000000000000000, 1.000000000000000000 ) ) ;
#8897=VERTEX_POINT ( 'NONE', #1567 ) ;
#8898=CARTESIAN_POINT ( 'NONE',  ( 3.000000000000000888, -1.901833551798098876, -22.47229024614979309 ) ) ;
#8899=EDGE_LOOP ( 'NONE', ( #6454, #3413, #3481, #6974 ) ) ;
#8900=ADVANCED_FACE ( 'NONE', ( #5304 ), #1690, .T. ) ;
#8902=VERTEX_POINT ( 'NONE', #9040 ) ;
#8903=DIRECTION ( 'NONE',  ( 0.000000000000000000, 0.8090169943749446757, 0.5877852522924770229 ) ) ;
#8904=EDGE_CURVE ( 'NONE', #1329, #9017, #3291, .T. ) ;
#8905=FACE_OUTER_BOUND ( 'NONE', #7548, .T. ) ;
#8909=CYLINDRICAL_SURFACE ( 'NONE', #11176, 24.80000000000000071 ) ;
#8912=VERTEX_POINT ( 'NONE', #7366 ) ;
#8913=ORIENTED_EDGE ( 'NONE', *, *, #8179, .T. ) ;
#8915=AXIS2_PLACEMENT_3D ( 'NONE', #11460, #1064, #4794 ) ;
#8917=EDGE_CURVE ( 'NONE', #2390, #1768, #9351, .T. ) ;
#8919=CARTESIAN_POINT ( 'NONE',  ( 3.000000000000000888, 13.62355943574019435, 17.97274125076078732 ) ) ;
#8921=CARTESIAN_POINT ( 'NONE',  ( 0.000000000000000000, 16.85990652506900389, 15.64281154287603215 ) ) ;
#8922=VECTOR ( 'NONE', #9722, 1000.000000000000000 ) ;
#8923=DIRECTION ( 'NONE',  ( -1.000000000000000000, 0.000000000000000000, -0.000000000000000000 ) ) ;
#8924=ORIENTED_EDGE ( 'NONE', *, *, #4834, .F. ) ;
#8925=ORIENTED_EDGE ( 'NONE', *, *, #5461, .T. ) ;
#8927=VERTEX_POINT ( 'NONE', #835 ) ;
#8928=DIRECTION ( 'NONE',  ( 0.000000000000000000, -0.9781476007338079093, 0.2079116908177492118 ) ) ;
#8929=DIRECTION ( 'NONE',  ( -1.000000000000000000, 0.000000000000000000, -0.000000000000000000 ) ) ;
#8930=DIRECTION ( 'NONE',  ( -1.000000000000000000, -0.000000000000000000, 0.000000000000000000 ) ) ;
#8931=EDGE_CURVE ( 'NONE', #9548, #7191, #2710, .T. ) ;
#8932=UNCERTAINTY_MEASURE_WITH_UNIT (LENGTH_MEASURE( 1.000000000000000082E-05 ), #5960, 'distance_accuracy_value', 'NONE');
#8933=CARTESIAN_POINT ( 'NONE',  ( 3.000000000000000888, 22.99643626497956816, 0.3433949777332492848 ) ) ;
#8934=ORIENTED_EDGE ( 'NONE', *, *, #11197, .T. ) ;
#8935=PLANE ( 'NONE',  #11606 ) ;
#8936=CARTESIAN_POINT ( 'NONE',  ( 3.000000000000000888, 22.56530478845649057, 4.445336973060936891 ) ) ;
#8938=EDGE_CURVE ( 'NONE', #3562, #10640, #9097, .T. ) ;
#8939=CARTESIAN_POINT ( 'NONE',  ( 3.000000000000000888, -12.88318129270191825, 18.51065745848373822 ) ) ;
#8940=CARTESIAN_POINT ( 'NONE',  ( 3.000000000000000888, 17.31945870441167301, -15.13242714128102406 ) ) ;
#8941=ORIENTED_EDGE ( 'NONE', *, *, #4492, .F. ) ;
#8943=ORIENTED_EDGE ( 'NONE', *, *, #7185, .F. ) ;
#8944=CARTESIAN_POINT ( 'NONE',  ( 3.000000000000000888, 20.08719549084880640, -11.20082935824054182 ) ) ;
#8945=CYLINDRICAL_SURFACE ( 'NONE', #6603, 9.599999999999997868 ) ;
#8946=DIRECTION ( 'NONE',  ( -1.000000000000000000, 0.000000000000000000, -0.000000000000000000 ) ) ;
#8948=EDGE_CURVE ( 'NONE', #7092, #1140, #11110, .T. ) ;
#8949=CIRCLE ( 'NONE', #3274, 9.599999999999996092 ) ;
#8950=CARTESIAN_POINT ( 'NONE',  ( 3.000000000000000888, -15.42759117534397006, 16.45023496161660148 ) ) ;
#8952=CARTESIAN_POINT ( 'NONE',  ( 3.000000000000000888, 22.37663021667340146, 2.811977935938166695 ) ) ;
#8953=ORIENTED_EDGE ( 'NONE', *, *, #5019, .T. ) ;
#8954=CARTESIAN_POINT ( 'NONE',  ( 0.000000000000000000, 0.000000000000000000, 0.000000000000000000 ) ) ;
#8955=ORIENTED_EDGE ( 'NONE', *, *, #9947, .F. ) ;
#8956=CARTESIAN_POINT ( 'NONE',  ( -10.00000000000000000, 0.000000000000000000, 0.000000000000000000 ) ) ;
#8957=ORIENTED_EDGE ( 'NONE', *, *, #9496, .T. ) ;
#8958=CARTESIAN_POINT ( 'NONE',  ( 3.000000000000000888, -22.54798042742718422, 0.4575788569251160731 ) ) ;
#8959=DIRECTION ( 'NONE',  ( -1.000000000000000000, 0.000000000000000000, 0.000000000000000000 ) ) ;
#8960=FACE_OUTER_BOUND ( 'NONE', #5588, .T. ) ;
#8961=LINE ( 'NONE', #572, #7047 ) ;
#8963=DIRECTION ( 'NONE',  ( 0.000000000000000000, 0.000000000000000000, 1.000000000000000000 ) ) ;
#8964=VECTOR ( 'NONE', #836, 1000.000000000000000 ) ;
#8965=DIRECTION ( 'NONE',  ( 0.000000000000000000, 0.8090169943749485615, -0.5877852522924714718 ) ) ;
#8966=VERTEX_POINT ( 'NONE', #10125 ) ;
#8967=CIRCLE ( 'NONE', #10911, 24.80000000000000071 ) ;
#8969=EDGE_CURVE ( 'NONE', #4541, #7118, #6611, .T. ) ;
#8970=VERTEX_POINT ( 'NONE', #3649 ) ;
#8972=EDGE_CURVE ( 'NONE', #4987, #3516, #8377, .T. ) ;
#8973=CIRCLE ( 'NONE', #7801, 22.99899999999999878 ) ;
#8974=CARTESIAN_POINT ( 'NONE',  ( 3.000000000000000000, 0.000000000000000000, 0.000000000000000000 ) ) ;
#8976=DIRECTION ( 'NONE',  ( 0.000000000000000000, 0.000000000000000000, 1.000000000000000000 ) ) ;
#8977=CIRCLE ( 'NONE', #10737, 22.99900000000000233 ) ;
#8978=ADVANCED_FACE ( 'NONE', ( #5666 ), #3954, .T. ) ;
#8979=CARTESIAN_POINT ( 'NONE',  ( 0.000000000000000000, -23.05871956130128808, 9.128825345752948905 ) ) ;
#8980=VECTOR ( 'NONE', #11370, 1000.000000000000000 ) ;
#8981=ORIENTED_EDGE ( 'NONE', *, *, #587, .T. ) ;
#8983=EDGE_CURVE ( 'NONE', #6466, #7118, #8967, .T. ) ;
#8984=VECTOR ( 'NONE', #2555, 1000.000000000000000 ) ;
#8985=ORIENTED_EDGE ( 'NONE', *, *, #3326, .T. ) ;
#8987=CARTESIAN_POINT ( 'NONE',  ( 0.000000000000000000, -21.97817939804047427, 11.48910920600676100 ) ) ;
#8988=CARTESIAN_POINT ( 'NONE',  ( 1.500000000000000444, -13.72351598154883412, -20.65684170206505499 ) ) ;
#8989=DIRECTION ( 'NONE',  ( 0.000000000000000000, 0.000000000000000000, 1.000000000000000000 ) ) ;
#8990=ORIENTED_EDGE ( 'NONE', *, *, #3594, .F. ) ;
#8991=DIRECTION ( 'NONE',  ( -1.000000000000000000, 0.000000000000000000, 0.000000000000000000 ) ) ;
#8992=AXIS2_PLACEMENT_3D ( 'NONE', #5405, #563, #9989 ) ;
#8993=DIRECTION ( 'NONE',  ( -1.000000000000000000, 0.000000000000000000, 0.000000000000000000 ) ) ;
#8995=DIRECTION ( 'NONE',  ( -1.000000000000000000, 0.000000000000000000, -0.000000000000000000 ) ) ;
#8996=ORIENTED_EDGE ( 'NONE', *, *, #4943, .T. ) ;
#8997=CARTESIAN_POINT ( 'NONE',  ( 3.000000000000000888, -4.445336973060693531, -22.56530478845653676 ) ) ;
#8999=ORIENTED_EDGE ( 'NONE', *, *, #3214, .T. ) ;
#9000=AXIS2_PLACEMENT_3D ( 'NONE', #5261, #9858, #9969 ) ;
#9002=CIRCLE ( 'NONE', #2745, 9.599999999999999645 ) ;
#9003=ORIENTED_EDGE ( 'NONE', *, *, #1873, .F. ) ;
#9004=CARTESIAN_POINT ( 'NONE',  ( 3.000000000000000888, -1.039229259764315128, -24.77821629063822684 ) ) ;
#9007=CARTESIAN_POINT ( 'NONE',  ( 3.000000000000000888, 0.000000000000000000, 0.000000000000000000 ) ) ;
#9008=CARTESIAN_POINT ( 'NONE',  ( 3.000000000000000888, -21.14796121233190362, -9.039786367039052806 ) ) ;
#9010=CIRCLE ( 'NONE', #3545, 9.599999999999996092 ) ;
#9011=DIRECTION ( 'NONE',  ( -1.000000000000000000, 0.000000000000000000, -0.000000000000000000 ) ) ;
#9013=CIRCLE ( 'NONE', #8439, 22.99899999999999523 ) ;
#9014=ADVANCED_FACE ( 'NONE', ( #5605 ), #2856, .T. ) ;
#9015=DIRECTION ( 'NONE',  ( -1.000000000000000000, 0.000000000000000000, -0.000000000000000000 ) ) ;
#9016=ORIENTED_EDGE ( 'NONE', *, *, #8380, .F. ) ;
#9017=VERTEX_POINT ( 'NONE', #4690 ) ;
#9018=CARTESIAN_POINT ( 'NONE',  ( 3.000000000000000888, -17.06259499759954679, 14.74749645580005364 ) ) ;
#9019=VERTEX_POINT ( 'NONE', #7610 ) ;
#9021=AXIS2_PLACEMENT_3D ( 'NONE', #7171, #11889, #5466 ) ;
#9023=DIRECTION ( 'NONE',  ( 0.000000000000000000, -0.9510565162951503115, -0.3090169943749572767 ) ) ;
#9024=ORIENTED_EDGE ( 'NONE', *, *, #5338, .F. ) ;
#9026=AXIS2_PLACEMENT_3D ( 'NONE', #7516, #4938, #3099 ) ;
#9028=DIRECTION ( 'NONE',  ( 0.000000000000000000, 0.000000000000000000, -1.000000000000000000 ) ) ;
#9029=CARTESIAN_POINT ( 'NONE',  ( 0.000000000000000000, 0.000000000000000000, 0.000000000000000000 ) ) ;
#9031=DIRECTION ( 'NONE',  ( 1.000000000000000000, 0.000000000000000000, 0.000000000000000000 ) ) ;
#9032=CARTESIAN_POINT ( 'NONE',  ( 1.499999999999999556, -22.21333432029571142, 11.02759168516737276 ) ) ;
#9033=ORIENTED_EDGE ( 'NONE', *, *, #10061, .T. ) ;
#9034=CIRCLE ( 'NONE', #8425, 9.599999999999997868 ) ;
#9036=ORIENTED_EDGE ( 'NONE', *, *, #904, .T. ) ;
#9038=VECTOR ( 'NONE', #11087, 1000.000000000000000 ) ;
#9039=CIRCLE ( 'NONE', #41, 22.99899999999999878 ) ;
#9040=CARTESIAN_POINT ( 'NONE',  ( 0.000000000000000000, -15.64281154287608722, 16.85990652506894705 ) ) ;
#9041=DIRECTION ( 'NONE',  ( -1.000000000000000000, -0.000000000000000000, -0.000000000000000000 ) ) ;
#9043=DIRECTION ( 'NONE',  ( 0.000000000000000000, 0.000000000000000000, 1.000000000000000000 ) ) ;
#9044=CARTESIAN_POINT ( 'NONE',  ( 0.000000000000000000, -24.75110766671653195, 1.556492618230558289 ) ) ;
#9045=EDGE_LOOP ( 'NONE', ( #3928, #3674, #2835, #597 ) ) ;
#9046=ORIENTED_EDGE ( 'NONE', *, *, #11809, .T. ) ;
#9047=EDGE_LOOP ( 'NONE', ( #6383, #10251, #4044, #10956 ) ) ;
#9048=CARTESIAN_POINT ( 'NONE',  ( -10.00000000000000000, 0.000000000000000000, 0.000000000000000000 ) ) ;
#9049=ADVANCED_FACE ( 'NONE', ( #89 ), #9517, .T. ) ;
#9050=CIRCLE ( 'NONE', #3780, 24.80000000000000071 ) ;
#9051=CARTESIAN_POINT ( 'NONE',  ( 3.000000000000000888, -21.97817939804047427, 11.48910920600676100 ) ) ;
#9052=CARTESIAN_POINT ( 'NONE',  ( 1.500000000000000444, -17.71842311621518462, -17.35216073792458857 ) ) ;
#9053=ORIENTED_EDGE ( 'NONE', *, *, #11773, .F. ) ;
#9055=CIRCLE ( 'NONE', #6120, 22.99899999999999878 ) ;
#9056=LINE ( 'NONE', #8004, #3589 ) ;
#9057=EDGE_CURVE ( 'NONE', #215, #4173, #4462, .T. ) ;
#9058=CARTESIAN_POINT ( 'NONE',  ( 3.000000000000000888, 0.000000000000000000, 0.000000000000000000 ) ) ;
#9060=AXIS2_PLACEMENT_3D ( 'NONE', #1086, #3899, #9229 ) ;
#9061=CIRCLE ( 'NONE', #6516, 22.99899999999999878 ) ;
#9062=ADVANCED_FACE ( 'NONE', ( #10257 ), #6523, .T. ) ;
#9063=CARTESIAN_POINT ( 'NONE',  ( 3.000000000000000888, 21.96011696265484403, 5.135568396240393518 ) ) ;
#9064=VERTEX_POINT ( 'NONE', #7681 ) ;
#9065=CARTESIAN_POINT ( 'NONE',  ( 3.000000000000000888, 0.000000000000000000, 0.000000000000000000 ) ) ;
#9066=ORIENTED_EDGE ( 'NONE', *, *, #8157, .F. ) ;
#9067=AXIS2_PLACEMENT_3D ( 'NONE', #4458, #11067, #9476 ) ;
#9068=ORIENTED_EDGE ( 'NONE', *, *, #6404, .T. ) ;
#9070=CARTESIAN_POINT ( 'NONE',  ( 0.000000000000000000, 17.06259499759944021, 14.74749645580017088 ) ) ;
#9071=VERTEX_POINT ( 'NONE', #205 ) ;
#9072=CARTESIAN_POINT ( 'NONE',  ( 3.000000000000002665, 0.000000000000000000, 0.000000000000000000 ) ) ;
#9073=DIRECTION ( 'NONE',  ( -1.000000000000000000, 0.000000000000000000, 0.000000000000000000 ) ) ;
#9075=VECTOR ( 'NONE', #7628, 1000.000000000000000 ) ;
#9076=CYLINDRICAL_SURFACE ( 'NONE', #1216, 9.599999999999997868 ) ;
#9077=LINE ( 'NONE', #7158, #790 ) ;
#9078=VERTEX_POINT ( 'NONE', #1870 ) ;
#9079=EDGE_LOOP ( 'NONE', ( #2515, #3150, #10005, #9158 ) ) ;
#9080=CYLINDRICAL_SURFACE ( 'NONE', #5479, 22.99899999999999878 ) ;
#9081=VERTEX_POINT ( 'NONE', #2913 ) ;
#9082=EDGE_CURVE ( 'NONE', #3896, #4836, #5851, .T. ) ;
#9084=LINE ( 'NONE', #2652, #4402 ) ;
#9085=ORIENTED_EDGE ( 'NONE', *, *, #5642, .F. ) ;
#9086=EDGE_CURVE ( 'NONE', #9844, #2082, #10437, .T. ) ;
#9087=CARTESIAN_POINT ( 'NONE',  ( -10.00000000000000000, 0.000000000000000000, 0.000000000000000000 ) ) ;
#9088=CARTESIAN_POINT ( 'NONE',  ( 3.000000000000000888, -8.645255683528844770, -23.24434456306333985 ) ) ;
#9091=DIRECTION ( 'NONE',  ( 0.000000000000000000, 0.000000000000000000, 1.000000000000000000 ) ) ;
#9092=CYLINDRICAL_SURFACE ( 'NONE', #416, 22.99899999999999878 ) ;
#9093=EDGE_LOOP ( 'NONE', ( #9274, #4010, #12076, #7659 ) ) ;
#9094=EDGE_CURVE ( 'NONE', #6369, #4549, #9361, .T. ) ;
#9095=ORIENTED_EDGE ( 'NONE', *, *, #7632, .T. ) ;
#9097=LINE ( 'NONE', #5422, #4863 ) ;
#9098=DIRECTION ( 'NONE',  ( 0.000000000000000000, 0.000000000000000000, 1.000000000000000000 ) ) ;
#9099=AXIS2_PLACEMENT_3D ( 'NONE', #7227, #693, #635 ) ;
#9101=DIRECTION ( 'NONE',  ( 1.000000000000000000, 0.000000000000000000, 0.000000000000000000 ) ) ;
#9103=ORIENTED_EDGE ( 'NONE', *, *, #6805, .F. ) ;
#9104=ORIENTED_EDGE ( 'NONE', *, *, #10715, .F. ) ;
#9105=AXIS2_PLACEMENT_3D ( 'NONE', #3080, #6798, #5030 ) ;
#9107=ORIENTED_EDGE ( 'NONE', *, *, #4255, .F. ) ;
#9109=DIRECTION ( 'NONE',  ( 0.000000000000000000, 0.000000000000000000, -1.000000000000000000 ) ) ;
#9111=DIRECTION ( 'NONE',  ( 0.000000000000000000, 0.1045284632676470038, 0.9945218953682740670 ) ) ;
#9113=DIRECTION ( 'NONE',  ( -1.000000000000000000, 0.000000000000000000, -0.000000000000000000 ) ) ;
#9115=DIRECTION ( 'NONE',  ( 1.000000000000000000, -0.000000000000000000, 0.000000000000000000 ) ) ;
#9116=CARTESIAN_POINT ( 'NONE',  ( 3.000000000000000888, 0.000000000000000000, 0.000000000000000000 ) ) ;
#9117=ORIENTED_EDGE ( 'NONE', *, *, #11747, .T. ) ;
#9118=VERTEX_POINT ( 'NONE', #10373 ) ;
#9119=VECTOR ( 'NONE', #5322, 1000.000000000000000 ) ;
#9121=EDGE_CURVE ( 'NONE', #7873, #6662, #8671, .T. ) ;
#9122=ORIENTED_EDGE ( 'NONE', *, *, #4570, .F. ) ;
#9123=DIRECTION ( 'NONE',  ( 0.000000000000000000, -0.9781476007338034684, -0.2079116908177699174 ) ) ;
#9124=ORIENTED_EDGE ( 'NONE', *, *, #1670, .F. ) ;
#9125=EDGE_CURVE ( 'NONE', #8629, #2147, #957, .T. ) ;
#9126=DIRECTION ( 'NONE',  ( 0.000000000000000000, -0.5877852522924797984, 0.8090169943749425663 ) ) ;
#9127=DIRECTION ( 'NONE',  ( -1.000000000000000000, 0.000000000000000000, 0.000000000000000000 ) ) ;
#9129=CARTESIAN_POINT ( 'NONE',  ( 3.000000000000000888, -22.15038895030651744, 4.240409074144028345 ) ) ;
#9130=CYLINDRICAL_SURFACE ( 'NONE', #11935, 22.99899999999999878 ) ;
#9131=EDGE_LOOP ( 'NONE', ( #732, #9753, #12061, #7872 ) ) ;
#9132=CARTESIAN_POINT ( 'NONE',  ( 0.000000000000000000, -19.29833442572367375, 11.67026512804540950 ) ) ;
#9133=ORIENTED_EDGE ( 'NONE', *, *, #2305, .T. ) ;
#9134=EDGE_CURVE ( 'NONE', #117, #1630, #7194, .T. ) ;
#9136=CARTESIAN_POINT ( 'NONE',  ( -10.00000000000000000, 0.000000000000000000, 0.000000000000000000 ) ) ;
#9137=VERTEX_POINT ( 'NONE', #8428 ) ;
#9138=CARTESIAN_POINT ( 'NONE',  ( 0.000000000000000000, 22.56530478845654386, -4.445336973060635799 ) ) ;
#9139=CARTESIAN_POINT ( 'NONE',  ( 1.500000000000000444, 22.21333432029563681, 11.02759168516753085 ) ) ;
#9143=CARTESIAN_POINT ( 'NONE',  ( 3.000000000000000888, 0.000000000000000000, 0.000000000000000000 ) ) ;
#9144=CARTESIAN_POINT ( 'NONE',  ( 3.000000000000000888, -17.97274125076083351, 13.62355943574013750 ) ) ;
#9145=ORIENTED_EDGE ( 'NONE', *, *, #7699, .T. ) ;
#9147=ORIENTED_EDGE ( 'NONE', *, *, #4216, .T. ) ;
#9148=ORIENTED_EDGE ( 'NONE', *, *, #5873, .T. ) ;
#9150=DIRECTION ( 'NONE',  ( -1.000000000000000000, -0.000000000000000000, 0.000000000000000000 ) ) ;
#9151=LINE ( 'NONE', #9838, #1146 ) ;
#9154=DIRECTION ( 'NONE',  ( 0.000000000000000000, 0.000000000000000000, -1.000000000000000000 ) ) ;
#9155=LINE ( 'NONE', #6227, #9178 ) ;
#9156=ADVANCED_FACE ( 'NONE', ( #9697 ), #5104, .T. ) ;
#9157=ORIENTED_EDGE ( 'NONE', *, *, #11682, .T. ) ;
#9158=ORIENTED_EDGE ( 'NONE', *, *, #6131, .T. ) ;
#9159=ORIENTED_EDGE ( 'NONE', *, *, #5107, .T. ) ;
#9160=CYLINDRICAL_SURFACE ( 'NONE', #3585, 9.599999999999997868 ) ;
#9161=DIRECTION ( 'NONE',  ( -1.000000000000000000, 0.000000000000000000, 0.000000000000000000 ) ) ;
#9163=DIRECTION ( 'NONE',  ( -1.000000000000000000, 0.000000000000000000, 0.000000000000000000 ) ) ;
#9164=EDGE_CURVE ( 'NONE', #3509, #9866, #7169, .T. ) ;
#9165=FACE_OUTER_BOUND ( 'NONE', #8422, .T. ) ;
#9166=CARTESIAN_POINT ( 'NONE',  ( 3.000000000000000888, 15.64281154287620446, -16.85990652506883691 ) ) ;
#9167=DIRECTION ( 'NONE',  ( -1.000000000000000000, 0.000000000000000000, -0.000000000000000000 ) ) ;
#9169=AXIS2_PLACEMENT_3D ( 'NONE', #8068, #6521, #6177 ) ;
#9171=ORIENTED_EDGE ( 'NONE', *, *, #8948, .F. ) ;
#9172=ORIENTED_EDGE ( 'NONE', *, *, #5274, .F. ) ;
#9173=DIRECTION ( 'NONE',  ( 0.000000000000000000, 0.000000000000000000, -1.000000000000000000 ) ) ;
#9174=ORIENTED_EDGE ( 'NONE', *, *, #8972, .T. ) ;
#9176=DIRECTION ( 'NONE',  ( 0.000000000000000000, 0.000000000000000000, 1.000000000000000000 ) ) ;
#9177=ORIENTED_EDGE ( 'NONE', *, *, #2318, .T. ) ;
#9178=VECTOR ( 'NONE', #658, 1000.000000000000000 ) ;
#9179=CARTESIAN_POINT ( 'NONE',  ( 0.000000000000000000, -16.45023496161654819, -15.42759117534402513 ) ) ;
#9180=DIRECTION ( 'NONE',  ( -1.000000000000000000, -0.000000000000000000, 0.000000000000000000 ) ) ;
#9182=DIRECTION ( 'NONE',  ( -1.000000000000000000, 0.000000000000000000, 0.000000000000000000 ) ) ;
#9183=DIRECTION ( 'NONE',  ( -1.000000000000000000, 0.000000000000000000, -0.000000000000000000 ) ) ;
#9185=EDGE_CURVE ( 'NONE', #2061, #9879, #6014, .T. ) ;
#9186=CARTESIAN_POINT ( 'NONE',  ( 3.000000000000000888, 0.000000000000000000, 0.000000000000000000 ) ) ;
#9187=AXIS2_PLACEMENT_3D ( 'NONE', #9677, #4047, #4973 ) ;
#9188=EDGE_LOOP ( 'NONE', ( #11281, #569, #3788, #9177 ) ) ;
#9191=EDGE_CURVE ( 'NONE', #1430, #532, #6809, .T. ) ;
#9193=VERTEX_POINT ( 'NONE', #1260 ) ;
#9194=AXIS2_PLACEMENT_3D ( 'NONE', #381, #10544, #2163 ) ;
#9195=FACE_OUTER_BOUND ( 'NONE', #8334, .T. ) ;
#9196=CIRCLE ( 'NONE', #399, 9.599999999999997868 ) ;
#9197=CIRCLE ( 'NONE', #6664, 9.599999999999997868 ) ;
#9198=LINE ( 'NONE', #8288, #3347 ) ;
#9199=CARTESIAN_POINT ( 'NONE',  ( 3.000000000000000888, 13.72351598154924979, -20.65684170206477788 ) ) ;
#9201=CIRCLE ( 'NONE', #204, 9.599999999999997868 ) ;
#9202=EDGE_CURVE ( 'NONE', #219, #1419, #6154, .T. ) ;
#9206=ADVANCED_FACE ( 'NONE', ( #7799 ), #5167, .T. ) ;
#9207=DIRECTION ( 'NONE',  ( 0.000000000000000000, 0.000000000000000000, 1.000000000000000000 ) ) ;
#9208=ORIENTED_EDGE ( 'NONE', *, *, #5032, .T. ) ;
#9210=CIRCLE ( 'NONE', #1977, 24.80000000000000071 ) ;
#9212=AXIS2_PLACEMENT_3D ( 'NONE', #9383, #5468, #11951 ) ;
#9213=VERTEX_POINT ( 'NONE', #11597 ) ;
#9216=FACE_OUTER_BOUND ( 'NONE', #11512, .T. ) ;
#9217=CARTESIAN_POINT ( 'NONE',  ( 0.000000000000000000, 0.000000000000000000, 0.000000000000000000 ) ) ;
#9218=EDGE_CURVE ( 'NONE', #1936, #7518, #3866, .T. ) ;
#9219=CIRCLE ( 'NONE', #9410, 24.80000000000000071 ) ;
#9223=ORIENTED_EDGE ( 'NONE', *, *, #7588, .T. ) ;
#9224=CYLINDRICAL_SURFACE ( 'NONE', #8207, 24.80000000000000071 ) ;
#9225=ORIENTED_EDGE ( 'NONE', *, *, #10555, .F. ) ;
#9228=ORIENTED_EDGE ( 'NONE', *, *, #8790, .T. ) ;
#9229=DIRECTION ( 'NONE',  ( 0.000000000000000000, -0.8660254037844328234, -0.5000000000000101030 ) ) ;
#9230=CIRCLE ( 'NONE', #3956, 24.80000000000000071 ) ;
#9231=CARTESIAN_POINT ( 'NONE',  ( 3.000000000000000888, 21.97817939804039611, 11.48910920600691554 ) ) ;
#9232=DIRECTION ( 'NONE',  ( -1.000000000000000000, -0.000000000000000000, 0.000000000000000000 ) ) ;
#9234=ADVANCED_FACE ( 'NONE', ( #4305 ), #11475, .T. ) ;
#9235=CARTESIAN_POINT ( 'NONE',  ( 0.000000000000000000, -0.3433949777333296094, 22.99643626497956816 ) ) ;
#9238=CIRCLE ( 'NONE', #5337, 22.99899999999999523 ) ;
#9239=DIRECTION ( 'NONE',  ( 0.000000000000000000, 0.2079116908177532641, 0.9781476007338070211 ) ) ;
#9240=VERTEX_POINT ( 'NONE', #11649 ) ;
#9241=ORIENTED_EDGE ( 'NONE', *, *, #8560, .F. ) ;
#9243=EDGE_CURVE ( 'NONE', #11379, #2984, #4056, .T. ) ;
#9244=EDGE_LOOP ( 'NONE', ( #2150, #4144, #3980, #10559 ) ) ;
#9246=VECTOR ( 'NONE', #3861, 1000.000000000000000 ) ;
#9247=DIRECTION ( 'NONE',  ( 0.000000000000000000, 0.000000000000000000, 1.000000000000000000 ) ) ;
#9248=EDGE_LOOP ( 'NONE', ( #3091, #10455, #4361, #294 ) ) ;
#9249=AXIS2_PLACEMENT_3D ( 'NONE', #11306, #10321, #1755 ) ;
#9250=FACE_OUTER_BOUND ( 'NONE', #2955, .T. ) ;
#9251=AXIS2_PLACEMENT_3D ( 'NONE', #11170, #1070, #3825 ) ;
#9252=DIRECTION ( 'NONE',  ( -1.000000000000000000, 0.000000000000000000, -0.000000000000000000 ) ) ;
#9254=CYLINDRICAL_SURFACE ( 'NONE', #2584, 9.599999999999997868 ) ;
#9256=AXIS2_PLACEMENT_3D ( 'NONE', #1465, #11916, #10766 ) ;
#9257=ORIENTED_EDGE ( 'NONE', *, *, #8917, .T. ) ;
#9258=LINE ( 'NONE', #11037, #7430 ) ;
#9259=ORIENTED_EDGE ( 'NONE', *, *, #10289, .F. ) ;
#9261=DIRECTION ( 'NONE',  ( 0.000000000000000000, 0.000000000000000000, 1.000000000000000000 ) ) ;
#9263=AXIS2_PLACEMENT_3D ( 'NONE', #2533, #2716, #6508 ) ;
#9264=CARTESIAN_POINT ( 'NONE',  ( 0.000000000000000000, -12.88318129270191825, 18.51065745848373822 ) ) ;
#9265=CARTESIAN_POINT ( 'NONE',  ( 3.000000000000000888, 0.000000000000000000, 0.000000000000000000 ) ) ;
#9268=CARTESIAN_POINT ( 'NONE',  ( -10.00000000000000000, 0.000000000000000000, 0.000000000000000000 ) ) ;
#9269=CARTESIAN_POINT ( 'NONE',  ( 3.000000000000000888, 10.87771529938188486, -19.75591328264875202 ) ) ;
#9271=APPLICATION_CONTEXT ( 'automotive_design' ) ;
#9273=AXIS2_PLACEMENT_3D ( 'NONE', #1778, #9127, #9982 ) ;
#9274=ORIENTED_EDGE ( 'NONE', *, *, #10698, .F. ) ;
#9276=CARTESIAN_POINT ( 'NONE',  ( 3.000000000000000888, -20.86861857134741172, 9.667200211209745930 ) ) ;
#9279=DIRECTION ( 'NONE',  ( 0.000000000000000000, 0.000000000000000000, -1.000000000000000000 ) ) ;
#9280=CARTESIAN_POINT ( 'NONE',  ( 3.000000000000000888, -10.87771529938174808, 19.75591328264882662 ) ) ;
#9281=EDGE_CURVE ( 'NONE', #5271, #1630, #9640, .T. ) ;
#9283=CIRCLE ( 'NONE', #1856, 9.599999999999999645 ) ;
#9284=DIRECTION ( 'NONE',  ( 0.000000000000000000, 0.000000000000000000, 1.000000000000000000 ) ) ;
#9285=LINE ( 'NONE', #1877, #7438 ) ;
#9286=ORIENTED_EDGE ( 'NONE', *, *, #4723, .T. ) ;
#9287=ORIENTED_EDGE ( 'NONE', *, *, #8826, .F. ) ;
#9288=ORIENTED_EDGE ( 'NONE', *, *, #8405, .T. ) ;
#9289=EDGE_CURVE ( 'NONE', #5671, #5364, #508, .T. ) ;
#9290=DIRECTION ( 'NONE',  ( -1.000000000000000000, 0.000000000000000000, 0.000000000000000000 ) ) ;
#9291=DIRECTION ( 'NONE',  ( -1.000000000000000000, 0.000000000000000000, 0.000000000000000000 ) ) ;
#9292=DIRECTION ( 'NONE',  ( 0.000000000000000000, 0.000000000000000000, 1.000000000000000000 ) ) ;
#9293=UNCERTAINTY_MEASURE_WITH_UNIT (LENGTH_MEASURE( 1.000000000000000082E-05 ), #5409, 'distance_accuracy_value', 'NONE');
#9294=DIRECTION ( 'NONE',  ( -1.000000000000000000, 0.000000000000000000, -0.000000000000000000 ) ) ;
#9295=FACE_OUTER_BOUND ( 'NONE', #2451, .T. ) ;
#9298=EDGE_CURVE ( 'NONE', #6260, #5789, #7794, .T. ) ;
#9299=CARTESIAN_POINT ( 'NONE',  ( 1.499999999999999556, -1.556492618230804759, 24.75110766671651774 ) ) ;
#9300=EDGE_LOOP ( 'NONE', ( #9208, #3868, #199, #4579 ) ) ;
#9301=ORIENTED_EDGE ( 'NONE', *, *, #8476, .T. ) ;
#9302=DIRECTION ( 'NONE',  ( 1.000000000000000000, 0.000000000000000000, 0.000000000000000000 ) ) ;
#9303=ORIENTED_EDGE ( 'NONE', *, *, #3898, .T. ) ;
#9304=EDGE_CURVE ( 'NONE', #8343, #2229, #4085, .T. ) ;
#9305=ORIENTED_EDGE ( 'NONE', *, *, #6208, .T. ) ;
#9306=CARTESIAN_POINT ( 'NONE',  ( 0.000000000000000000, -19.29833442572351743, -11.67026512804567062 ) ) ;
#9308=ADVANCED_FACE ( 'NONE', ( #7049 ), #2233, .T. ) ;
#9310=CARTESIAN_POINT ( 'NONE',  ( -10.00000000000000000, 0.000000000000000000, 0.000000000000000000 ) ) ;
#9311=ADVANCED_FACE ( 'NONE', ( #9195 ), #8162, .T. ) ;
#9312=DIRECTION ( 'NONE',  ( -1.000000000000000000, 0.000000000000000000, 0.000000000000000000 ) ) ;
#9315=FACE_OUTER_BOUND ( 'NONE', #2542, .T. ) ;
#9316=VERTEX_POINT ( 'NONE', #883 ) ;
#9317=AXIS2_PLACEMENT_3D ( 'NONE', #721, #11014, #1463 ) ;
#9318=VERTEX_POINT ( 'NONE', #1622 ) ;
#9319=DIRECTION ( 'NONE',  ( -1.000000000000000000, -0.000000000000000000, -0.000000000000000000 ) ) ;
#9320=ORIENTED_EDGE ( 'NONE', *, *, #5198, .F. ) ;
#9322=DIRECTION ( 'NONE',  ( 1.000000000000000000, 0.000000000000000000, 0.000000000000000000 ) ) ;
#9323=DIRECTION ( 'NONE',  ( -1.000000000000000000, 0.000000000000000000, 0.000000000000000000 ) ) ;
#9324=ADVANCED_FACE ( 'NONE', ( #3461 ), #2601, .T. ) ;
#9325=CARTESIAN_POINT ( 'NONE',  ( 3.000000000000000888, -22.54798042742717357, -0.4575788569254196636 ) ) ;
#9326=CARTESIAN_POINT ( 'NONE',  ( 8.000000000000000000, 2.265596578422603002E-15, -18.49999999999999645 ) ) ;
#9328=DIRECTION ( 'NONE',  ( -1.000000000000000000, -0.000000000000000000, -0.000000000000000000 ) ) ;
#9329=DIRECTION ( 'NONE',  ( -1.000000000000000000, -0.000000000000000000, 0.000000000000000000 ) ) ;
#9330=CYLINDRICAL_SURFACE ( 'NONE', #9603, 9.599999999999997868 ) ;
#9331=EDGE_LOOP ( 'NONE', ( #3655, #7861, #10203, #1464 ) ) ;
#9332=ORIENTED_EDGE ( 'NONE', *, *, #2048, .F. ) ;
#9333=VERTEX_POINT ( 'NONE', #3403 ) ;
#9334=LINE ( 'NONE', #1866, #12094 ) ;
#9336=DIRECTION ( 'NONE',  ( 0.000000000000000000, 0.000000000000000000, 1.000000000000000000 ) ) ;
#9337=CARTESIAN_POINT ( 'NONE',  ( 0.000000000000000000, 0.000000000000000000, 0.000000000000000000 ) ) ;
#9338=CARTESIAN_POINT ( 'NONE',  ( 3.000000000000000888, 0.000000000000000000, 0.000000000000000000 ) ) ;
#9340=DIRECTION ( 'NONE',  ( 1.000000000000000000, -0.000000000000000000, -0.000000000000000000 ) ) ;
#9342=ORIENTED_EDGE ( 'NONE', *, *, #2415, .F. ) ;
#9343=ORIENTED_EDGE ( 'NONE', *, *, #3530, .F. ) ;
#9344=EDGE_CURVE ( 'NONE', #4720, #7859, #2917, .T. ) ;
#9345=EDGE_LOOP ( 'NONE', ( #8249, #11637, #10599, #7072 ) ) ;
#9346=CARTESIAN_POINT ( 'NONE',  ( 3.000000000000000888, -20.78471918669854901, -8.753070780933368766 ) ) ;
#9347=DIRECTION ( 'NONE',  ( 1.000000000000000000, -0.000000000000000000, -0.000000000000000000 ) ) ;
#9348=CIRCLE ( 'NONE', #4075, 24.80000000000000071 ) ;
#9349=CARTESIAN_POINT ( 'NONE',  ( 3.000000000000000888, 0.000000000000000000, 0.000000000000000000 ) ) ;
#9350=DIRECTION ( 'NONE',  ( -1.000000000000000000, 0.000000000000000000, 0.000000000000000000 ) ) ;
#9351=CIRCLE ( 'NONE', #5441, 9.599999999999997868 ) ;
#9352=CARTESIAN_POINT ( 'NONE',  ( 0.000000000000000000, -11.67026512804560134, 19.29833442572355651 ) ) ;
#9355=EDGE_CURVE ( 'NONE', #1694, #1049, #8189, .T. ) ;
#9356=EDGE_CURVE ( 'NONE', #2393, #277, #9749, .T. ) ;
#9357=CARTESIAN_POINT ( 'NONE',  ( 0.000000000000000000, 21.97702544527767188, -6.779701584702504391 ) ) ;
#9358=AXIS2_PLACEMENT_3D ( 'NONE', #2363, #10999, #768 ) ;
#9359=VERTEX_POINT ( 'NONE', #5289 ) ;
#9360=VERTEX_POINT ( 'NONE', #9996 ) ;
#9361=CIRCLE ( 'NONE', #7762, 9.599999999999997868 ) ;
#9363=VERTEX_POINT ( 'NONE', #5358 ) ;
#9364=VERTEX_POINT ( 'NONE', #7111 ) ;
#9365=CARTESIAN_POINT ( 'NONE',  ( 1.499999999999999556, 21.97817939804055598, -11.48910920600660468 ) ) ;
#9366=CARTESIAN_POINT ( 'NONE',  ( 3.000000000000000888, -16.85990652506910692, 15.64281154287591669 ) ) ;
#9367=ORIENTED_EDGE ( 'NONE', *, *, #10888, .F. ) ;
#9370=CARTESIAN_POINT ( 'NONE',  ( -10.00000000000000000, 0.000000000000000000, 0.000000000000000000 ) ) ;
#9372=DIRECTION ( 'NONE',  ( -1.000000000000000000, -0.000000000000000000, 0.000000000000000000 ) ) ;
#9373=FACE_OUTER_BOUND ( 'NONE', #10431, .T. ) ;
#9374=ORIENTED_EDGE ( 'NONE', *, *, #3908, .T. ) ;
#9375=DIRECTION ( 'NONE',  ( -1.000000000000000000, 0.000000000000000000, 0.000000000000000000 ) ) ;
#9376=ORIENTED_EDGE ( 'NONE', *, *, #3195, .T. ) ;
#9377=CIRCLE ( 'NONE', #8786, 9.599999999999997868 ) ;
#9379=CIRCLE ( 'NONE', #6048, 24.80000000000000071 ) ;
#9380=DIRECTION ( 'NONE',  ( 0.000000000000000000, 0.000000000000000000, 1.000000000000000000 ) ) ;
#9381=DIRECTION ( 'NONE',  ( 0.000000000000000000, -0.4067366430757886619, -0.9135454576426060846 ) ) ;
#9382=CYLINDRICAL_SURFACE ( 'NONE', #11238, 9.599999999999997868 ) ;
#9383=CARTESIAN_POINT ( 'NONE',  ( 3.000000000000000888, 8.753070780933430939, -20.78471918669851703 ) ) ;
#9384=VECTOR ( 'NONE', #6214, 1000.000000000000000 ) ;
#9385=ADVANCED_FACE ( 'NONE', ( #5411 ), #3636, .T. ) ;
#9387=DIRECTION ( 'NONE',  ( -1.000000000000000000, 0.000000000000000000, -0.000000000000000000 ) ) ;
#9388=AXIS2_PLACEMENT_3D ( 'NONE', #5428, #2620, #3599 ) ;
#9389=DIRECTION ( 'NONE',  ( -1.000000000000000000, 0.000000000000000000, 0.000000000000000000 ) ) ;
#9390=ORIENTED_EDGE ( 'NONE', *, *, #7340, .T. ) ;
#9391=ADVANCED_FACE ( 'NONE', ( #10914 ), #10983, .T. ) ;
#9392=EDGE_LOOP ( 'NONE', ( #7407, #9557 ) ) ;
#9393=CARTESIAN_POINT ( 'NONE',  ( 1.499999999999999556, -24.02068490260616329, 6.168200451485678748 ) ) ;
#9394=AXIS2_PLACEMENT_3D ( 'NONE', #11131, #10031, #11201 ) ;
#9396=AXIS2_PLACEMENT_3D ( 'NONE', #5587, #11154, #878 ) ;
#9397=DIRECTION ( 'NONE',  ( 0.000000000000000000, 0.000000000000000000, 1.000000000000000000 ) ) ;
#9400=CARTESIAN_POINT ( 'NONE',  ( 3.000000000000000888, 16.45023496161665122, 15.42759117534391322 ) ) ;
#9401=CIRCLE ( 'NONE', #8233, 9.599999999999997868 ) ;
#9402=CARTESIAN_POINT ( 'NONE',  ( 3.000000000000000888, -1.901833551798412847, 22.47229024614976822 ) ) ;
#9403=VECTOR ( 'NONE', #1934, 1000.000000000000000 ) ;
#9404=VERTEX_POINT ( 'NONE', #9138 ) ;
#9406=VERTEX_POINT ( 'NONE', #818 ) ;
#9407=ORIENTED_EDGE ( 'NONE', *, *, #71, .F. ) ;
#9408=DIRECTION ( 'NONE',  ( 0.000000000000000000, -0.6691306063588644548, 0.7431448254773885820 ) ) ;
#9409=DIRECTION ( 'NONE',  ( 1.000000000000000000, -0.000000000000000000, -0.000000000000000000 ) ) ;
#9410=AXIS2_PLACEMENT_3D ( 'NONE', #3824, #10540, #11344 ) ;
#9412=CARTESIAN_POINT ( 'NONE',  ( 1.500000000000000444, -15.40502424595158537, 19.43515443678397148 ) ) ;
#9413=DIRECTION ( 'NONE',  ( -1.000000000000000000, 0.000000000000000000, -0.000000000000000000 ) ) ;
#9414=CIRCLE ( 'NONE', #4142, 24.80000000000000071 ) ;
#9415=LINE ( 'NONE', #11198, #260 ) ;
#9417=DIRECTION ( 'NONE',  ( -1.000000000000000000, 0.000000000000000000, 0.000000000000000000 ) ) ;
#9418=CIRCLE ( 'NONE', #5716, 9.599999999999997868 ) ;
#9419=DIRECTION ( 'NONE',  ( 0.000000000000000000, 0.6691306063588594588, -0.7431448254773932449 ) ) ;
#9420=CARTESIAN_POINT ( 'NONE',  ( 0.000000000000000000, 0.000000000000000000, 0.000000000000000000 ) ) ;
#9421=EDGE_CURVE ( 'NONE', #2308, #4256, #5621, .T. ) ;
#9423=VERTEX_POINT ( 'NONE', #11044 ) ;
#9425=ORIENTED_EDGE ( 'NONE', *, *, #9839, .T. ) ;
#9426=DIRECTION ( 'NONE',  ( 0.000000000000000000, -0.5877852522924633671, -0.8090169943749546677 ) ) ;
#9428=DIRECTION ( 'NONE',  ( -1.000000000000000000, 0.000000000000000000, 0.000000000000000000 ) ) ;
#9429=ORIENTED_EDGE ( 'NONE', *, *, #9057, .F. ) ;
#9431=CIRCLE ( 'NONE', #6889, 9.599999999999996092 ) ;
#9432=FACE_OUTER_BOUND ( 'NONE', #2559, .T. ) ;
#9433=CYLINDRICAL_SURFACE ( 'NONE', #2585, 9.599999999999997868 ) ;
#9435=LINE ( 'NONE', #121, #407 ) ;
#9436=DIRECTION ( 'NONE',  ( -1.000000000000000000, 0.000000000000000000, 0.000000000000000000 ) ) ;
#9437=ORIENTED_EDGE ( 'NONE', *, *, #969, .T. ) ;
#9439=CARTESIAN_POINT ( 'NONE',  ( 3.000000000000000888, 18.51065745848377730, 12.88318129270185430 ) ) ;
#9440=ORIENTED_EDGE ( 'NONE', *, *, #5345, .T. ) ;
#9441=AXIS2_PLACEMENT_3D ( 'NONE', #6254, #9980, #1605 ) ;
#9443=AXIS2_PLACEMENT_3D ( 'NONE', #10303, #3699, #7601 ) ;
#9444=CARTESIAN_POINT ( 'NONE',  ( 0.000000000000000000, 17.97274125076092233, -13.62355943574001671 ) ) ;
#9445=VERTEX_POINT ( 'NONE', #637 ) ;
#9446=LINE ( 'NONE', #76, #5826 ) ;
#9447=DIRECTION ( 'NONE',  ( 0.000000000000000000, 0.000000000000000000, 1.000000000000000000 ) ) ;
#9449=CIRCLE ( 'NONE', #9832, 9.599999999999997868 ) ;
#9450=CARTESIAN_POINT ( 'NONE',  ( 3.000000000000000888, -19.74380051311532114, -11.79560690673893042 ) ) ;
#9452=LINE ( 'NONE', #8540, #4706 ) ;
#9454=ORIENTED_EDGE ( 'NONE', *, *, #6618, .F. ) ;
#9455=DIRECTION ( 'NONE',  ( -1.000000000000000000, -0.000000000000000000, -0.000000000000000000 ) ) ;
#9456=ORIENTED_EDGE ( 'NONE', *, *, #8279, .T. ) ;
#9457=EDGE_CURVE ( 'NONE', #679, #9776, #9721, .T. ) ;
#9458=AXIS2_PLACEMENT_3D ( 'NONE', #2681, #8320, #5622 ) ;
#9464=ADVANCED_FACE ( 'NONE', ( #11097 ), #2714, .T. ) ;
#9465=AXIS2_PLACEMENT_3D ( 'NONE', #8163, #10113, #1730 ) ;
#9466=CARTESIAN_POINT ( 'NONE',  ( 0.000000000000000000, -22.99643626497957172, 0.3433949777330864706 ) ) ;
#9467=VERTEX_POINT ( 'NONE', #10112 ) ;
#9468=ORIENTED_EDGE ( 'NONE', *, *, #5353, .F. ) ;
#9469=ORIENTED_EDGE ( 'NONE', *, *, #5924, .T. ) ;
#9470=CARTESIAN_POINT ( 'NONE',  ( 3.000000000000000888, -8.753070780933015271, -20.78471918669869467 ) ) ;
#9471=DIRECTION ( 'NONE',  ( -1.000000000000000000, -0.000000000000000000, 0.000000000000000000 ) ) ;
#9472=ORIENTED_EDGE ( 'NONE', *, *, #10564, .T. ) ;
#9473=CIRCLE ( 'NONE', #9859, 24.80000000000000071 ) ;
#9474=DIRECTION ( 'NONE',  ( -1.000000000000000000, 0.000000000000000000, 0.000000000000000000 ) ) ;
#9475=CYLINDRICAL_SURFACE ( 'NONE', #2702, 22.99899999999999878 ) ;
#9476=DIRECTION ( 'NONE',  ( 0.000000000000000000, 0.000000000000000000, 1.000000000000000000 ) ) ;
#9478=DIRECTION ( 'NONE',  ( -1.000000000000000000, -0.000000000000000000, -0.000000000000000000 ) ) ;
#9479=VERTEX_POINT ( 'NONE', #10178 ) ;
#9480=VERTEX_POINT ( 'NONE', #1728 ) ;
#9483=ORIENTED_EDGE ( 'NONE', *, *, #11448, .T. ) ;
#9484=LINE ( 'NONE', #7578, #8275 ) ;
#9486=ORIENTED_EDGE ( 'NONE', *, *, #10581, .F. ) ;
#9488=AXIS2_PLACEMENT_3D ( 'NONE', #1727, #10056, #9023 ) ;
#9489=CARTESIAN_POINT ( 'NONE',  ( 0.000000000000000000, 0.000000000000000000, 0.000000000000000000 ) ) ;
#9491=DIRECTION ( 'NONE',  ( -1.000000000000000000, -0.000000000000000000, 0.000000000000000000 ) ) ;
#9492=CYLINDRICAL_SURFACE ( 'NONE', #5321, 22.99899999999999878 ) ;
#9493=ORIENTED_EDGE ( 'NONE', *, *, #5721, .F. ) ;
#9494=ORIENTED_EDGE ( 'NONE', *, *, #2962, .F. ) ;
#9495=DIRECTION ( 'NONE',  ( 0.000000000000000000, 0.9510565162951544194, -0.3090169943749450088 ) ) ;
#9496=EDGE_CURVE ( 'NONE', #2749, #3541, #6507, .T. ) ;
#9497=ORIENTED_EDGE ( 'NONE', *, *, #866, .F. ) ;
#9498=CIRCLE ( 'NONE', #9105, 9.599999999999997868 ) ;
#9499=EDGE_CURVE ( 'NONE', #8125, #10279, #9502, .T. ) ;
#9501=CARTESIAN_POINT ( 'NONE',  ( 0.000000000000000000, -6.532525787310825116, -21.58580335785683246 ) ) ;
#9502=LINE ( 'NONE', #11227, #9731 ) ;
#9505=AXIS2_PLACEMENT_3D ( 'NONE', #8813, #10761, #6842 ) ;
#9506=DIRECTION ( 'NONE',  ( -1.000000000000000000, 0.000000000000000000, 0.000000000000000000 ) ) ;
#9508=EDGE_CURVE ( 'NONE', #5848, #1491, #4455, .T. ) ;
#9509=DIRECTION ( 'NONE',  ( 1.000000000000000000, 0.000000000000000000, 0.000000000000000000 ) ) ;
#9510=ORIENTED_EDGE ( 'NONE', *, *, #8564, .F. ) ;
#9511=CARTESIAN_POINT ( 'NONE',  ( 3.000000000000000888, -21.96011696265495061, 5.135568396239952982 ) ) ;
#9512=EDGE_CURVE ( 'NONE', #12091, #2865, #5433, .T. ) ;
#9513=ORIENTED_EDGE ( 'NONE', *, *, #2639, .F. ) ;
#9514=ORIENTED_EDGE ( 'NONE', *, *, #2734, .T. ) ;
#9515=DIRECTION ( 'NONE',  ( -1.000000000000000000, -0.000000000000000000, -0.000000000000000000 ) ) ;
#9517=CYLINDRICAL_SURFACE ( 'NONE', #4272, 24.80000000000000071 ) ;
#9518=EDGE_CURVE ( 'NONE', #11239, #3932, #8949, .T. ) ;
#9521=EDGE_CURVE ( 'NONE', #992, #10871, #7963, .T. ) ;
#9522=DIRECTION ( 'NONE',  ( -1.000000000000000000, -0.000000000000000000, -0.000000000000000000 ) ) ;
#9523=EDGE_CURVE ( 'NONE', #6489, #2943, #9446, .T. ) ;
#9524=ORIENTED_EDGE ( 'NONE', *, *, #4126, .F. ) ;
#9525=EDGE_LOOP ( 'NONE', ( #5626, #4998, #11482, #3247 ) ) ;
#9526=ORIENTED_EDGE ( 'NONE', *, *, #10878, .T. ) ;
#9527=DIRECTION ( 'NONE',  ( -1.000000000000000000, 0.000000000000000000, 0.000000000000000000 ) ) ;
#9528=CARTESIAN_POINT ( 'NONE',  ( 3.000000000000000888, 0.000000000000000000, 0.000000000000000000 ) ) ;
#9529=VERTEX_POINT ( 'NONE', #6564 ) ;
#9531=DIRECTION ( 'NONE',  ( 1.000000000000000000, -0.000000000000000000, -0.000000000000000000 ) ) ;
#9532=DIRECTION ( 'NONE',  ( 0.000000000000000000, 0.000000000000000000, 1.000000000000000000 ) ) ;
#9533=VECTOR ( 'NONE', #2156, 1000.000000000000000 ) ;
#9534=LINE ( 'NONE', #1150, #5366 ) ;
#9537=CARTESIAN_POINT ( 'NONE',  ( 0.000000000000000000, -17.06259499759935139, -14.74749645580028101 ) ) ;
#9538=ORIENTED_EDGE ( 'NONE', *, *, #10793, .T. ) ;
#9539=VERTEX_POINT ( 'NONE', #11339 ) ;
#9542=ORIENTED_EDGE ( 'NONE', *, *, #8378, .T. ) ;
#9543=AXIS2_PLACEMENT_3D ( 'NONE', #3227, #1213, #8684 ) ;
#9544=CARTESIAN_POINT ( 'NONE',  ( 3.000000000000000888, 0.000000000000000000, 0.000000000000000000 ) ) ;
#9545=DIRECTION ( 'NONE',  ( -1.000000000000000000, 0.000000000000000000, -0.000000000000000000 ) ) ;
#9546=EDGE_CURVE ( 'NONE', #1896, #10351, #4796, .T. ) ;
#9548=VERTEX_POINT ( 'NONE', #7597 ) ;
#9549=DIRECTION ( 'NONE',  ( 1.000000000000000000, 0.000000000000000000, 0.000000000000000000 ) ) ;
#9550=CARTESIAN_POINT ( 'NONE',  ( 3.000000000000000888, 16.85990652506900389, 15.64281154287603215 ) ) ;
#9552=CIRCLE ( 'NONE', #3691, 9.599999999999996092 ) ;
#9553=AXIS2_PLACEMENT_3D ( 'NONE', #2055, #2978, #9397 ) ;
#9555=ORIENTED_EDGE ( 'NONE', *, *, #2022, .F. ) ;
#9556=DIRECTION ( 'NONE',  ( 0.000000000000000000, 0.000000000000000000, -1.000000000000000000 ) ) ;
#9557=ORIENTED_EDGE ( 'NONE', *, *, #4269, .F. ) ;
#9558=ORIENTED_EDGE ( 'NONE', *, *, #5264, .T. ) ;
#9559=DIRECTION ( 'NONE',  ( -1.000000000000000000, -0.000000000000000000, 0.000000000000000000 ) ) ;
#9560=ORIENTED_EDGE ( 'NONE', *, *, #9523, .F. ) ;
#9562=AXIS2_PLACEMENT_3D ( 'NONE', #5253, #8359, #4333 ) ;
#9563=DIRECTION ( 'NONE',  ( 0.000000000000000000, 0.000000000000000000, 1.000000000000000000 ) ) ;
#9564=DIRECTION ( 'NONE',  ( 0.000000000000000000, 0.000000000000000000, 1.000000000000000000 ) ) ;
#9565=DIRECTION ( 'NONE',  ( -1.000000000000000000, 0.000000000000000000, 0.000000000000000000 ) ) ;
#9567=PRESENTATION_STYLE_ASSIGNMENT (( #7728 ) ) ;
#9569=EDGE_CURVE ( 'NONE', #3234, #11531, #4066, .T. ) ;
#9570=CARTESIAN_POINT ( 'NONE',  ( 3.000000000000000888, 0.000000000000000000, 0.000000000000000000 ) ) ;
#9572=CARTESIAN_POINT ( 'NONE',  ( 0.000000000000000000, -11.48910920600699193, 21.97817939804034992 ) ) ;
#9573=AXIS2_PLACEMENT_3D ( 'NONE', #4155, #11667, #11612 ) ;
#9574=ADVANCED_FACE ( 'NONE', ( #11404 ), #2963, .T. ) ;
#9575=VERTEX_POINT ( 'NONE', #10422 ) ;
#9579=EDGE_CURVE ( 'NONE', #8886, #3221, #740, .T. ) ;
#9580=DIRECTION ( 'NONE',  ( 0.000000000000000000, 0.000000000000000000, -1.000000000000000000 ) ) ;
#9581=ADVANCED_FACE ( 'NONE', ( #5780 ), #10481, .T. ) ;
#9582=AXIS2_PLACEMENT_3D ( 'NONE', #4006, #5902, #446 ) ;
#9585=EDGE_CURVE ( 'NONE', #5072, #7710, #7577, .T. ) ;
#9586=LINE ( 'NONE', #7870, #1957 ) ;
#9587=EDGE_LOOP ( 'NONE', ( #3489, #4244, #1878, #11456 ) ) ;
#9588=CIRCLE ( 'NONE', #3723, 9.599999999999997868 ) ;
#9589=CIRCLE ( 'NONE', #10960, 9.599999999999996092 ) ;
#9590=ORIENTED_EDGE ( 'NONE', *, *, #368, .F. ) ;
#9591=DIRECTION ( 'NONE',  ( 0.000000000000000000, 0.000000000000000000, 1.000000000000000000 ) ) ;
#9593=DIRECTION ( 'NONE',  ( -1.000000000000000000, 0.000000000000000000, 0.000000000000000000 ) ) ;
#9594=CARTESIAN_POINT ( 'NONE',  ( 3.000000000000000888, 13.62355943574019435, 17.97274125076078732 ) ) ;
#9596=AXIS2_PLACEMENT_3D ( 'NONE', #1529, #428, #9860 ) ;
#9598=DIRECTION ( 'NONE',  ( 0.000000000000000000, -0.7431448254773999063, 0.6691306063588520203 ) ) ;
#9599=ORIENTED_EDGE ( 'NONE', *, *, #12079, .F. ) ;
#9603=AXIS2_PLACEMENT_3D ( 'NONE', #7547, #10364, #6309 ) ;
#9604=ORIENTED_EDGE ( 'NONE', *, *, #2664, .F. ) ;
#9605=CIRCLE ( 'NONE', #5886, 24.80000000000000071 ) ;
#9606=FACE_OUTER_BOUND ( 'NONE', #12047, .T. ) ;
#9607=DIRECTION ( 'NONE',  ( 0.000000000000000000, 0.000000000000000000, 1.000000000000000000 ) ) ;
#9608=AXIS2_PLACEMENT_3D ( 'NONE', #1321, #9764, #6100 ) ;
#9609=EDGE_CURVE ( 'NONE', #8613, #11921, #6216, .T. ) ;
#9610=CARTESIAN_POINT ( 'NONE',  ( 3.000000000000000888, 0.000000000000000000, 0.000000000000000000 ) ) ;
#9611=EDGE_LOOP ( 'NONE', ( #11388, #4760, #7536, #9975 ) ) ;
#9612=CARTESIAN_POINT ( 'NONE',  ( 3.000000000000000888, 22.42251312757879234, 5.117118920208566735 ) ) ;
#9613=DIRECTION ( 'NONE',  ( -1.000000000000000000, -0.000000000000000000, -0.000000000000000000 ) ) ;
#9615=AXIS2_PLACEMENT_3D ( 'NONE', #3319, #7039, #10790 ) ;
#9616=ORIENTED_EDGE ( 'NONE', *, *, #227, .T. ) ;
#9617=EDGE_CURVE ( 'NONE', #9915, #3995, #11164, .T. ) ;
#9619=CARTESIAN_POINT ( 'NONE',  ( 0.000000000000000000, -24.53384959170454849, -3.623565124517358793 ) ) ;
#9620=VERTEX_POINT ( 'NONE', #2778 ) ;
#9621=CARTESIAN_POINT ( 'NONE',  ( 0.000000000000000000, 11.79560690673899970, -19.74380051311527495 ) ) ;
#9622=ORIENTED_EDGE ( 'NONE', *, *, #8155, .F. ) ;
#9625=DIRECTION ( 'NONE',  ( -1.000000000000000000, 0.000000000000000000, -0.000000000000000000 ) ) ;
#9627=LINE ( 'NONE', #9685, #1074 ) ;
#9629=DIRECTION ( 'NONE',  ( -1.000000000000000000, 0.000000000000000000, -0.000000000000000000 ) ) ;
#9630=DIRECTION ( 'NONE',  ( -1.000000000000000000, 0.000000000000000000, -0.000000000000000000 ) ) ;
#9631=FACE_OUTER_BOUND ( 'NONE', #10704, .T. ) ;
#9632=VECTOR ( 'NONE', #1815, 1000.000000000000000 ) ;
#9633=CARTESIAN_POINT ( 'NONE',  ( 3.000000000000000888, -17.35216073792428659, -17.71842311621547950 ) ) ;
#9634=AXIS2_PLACEMENT_3D ( 'NONE', #3467, #944, #8538 ) ;
#9635=VERTEX_POINT ( 'NONE', #7540 ) ;
#9636=ORIENTED_EDGE ( 'NONE', *, *, #9761, .T. ) ;
#9637=DIRECTION ( 'NONE',  ( -1.000000000000000000, -0.000000000000000000, 0.000000000000000000 ) ) ;
#9639=VECTOR ( 'NONE', #118, 1000.000000000000000 ) ;
#9640=LINE ( 'NONE', #7973, #9942 ) ;
#9644=DIRECTION ( 'NONE',  ( -1.000000000000000000, 0.000000000000000000, -0.000000000000000000 ) ) ;
#9645=FACE_OUTER_BOUND ( 'NONE', #5334, .T. ) ;
#9646=VERTEX_POINT ( 'NONE', #11285 ) ;
#9647=AXIS2_PLACEMENT_3D ( 'NONE', #5020, #11446, #5880 ) ;
#9648=EDGE_CURVE ( 'NONE', #4550, #2557, #2900, .T. ) ;
#9649=ORIENTED_EDGE ( 'NONE', *, *, #11974, .T. ) ;
#9650=DIRECTION ( 'NONE',  ( 0.000000000000000000, 0.6691306063588593478, -0.7431448254773931339 ) ) ;
#9652=EDGE_CURVE ( 'NONE', #139, #6466, #1978, .T. ) ;
#9654=FACE_OUTER_BOUND ( 'NONE', #6313, .T. ) ;
#9655=FACE_OUTER_BOUND ( 'NONE', #10938, .T. ) ;
#9659=CARTESIAN_POINT ( 'NONE',  ( 0.000000000000000000, 7.432877647175207159, 21.76479567747244204 ) ) ;
#9660=ORIENTED_EDGE ( 'NONE', *, *, #8305, .T. ) ;
#9664=ORIENTED_EDGE ( 'NONE', *, *, #2645, .T. ) ;
#9665=CIRCLE ( 'NONE', #8884, 24.80000000000000071 ) ;
#9667=DIRECTION ( 'NONE',  ( 0.000000000000000000, 0.000000000000000000, 1.000000000000000000 ) ) ;
#9668=CARTESIAN_POINT ( 'NONE',  ( 1.499999999999999556, 24.02068490260612776, 6.168200451485841285 ) ) ;
#9669=VERTEX_POINT ( 'NONE', #9805 ) ;
#9670=CARTESIAN_POINT ( 'NONE',  ( 3.000000000000000888, -18.51065745848386968, 12.88318129270172818 ) ) ;
#9671=ADVANCED_FACE ( 'NONE', ( #437 ), #4916, .T. ) ;
#9672=DIRECTION ( 'NONE',  ( 0.000000000000000000, -0.2079116908177664480, 0.9781476007338040235 ) ) ;
#9674=ORIENTED_EDGE ( 'NONE', *, *, #6288, .T. ) ;
#9676=CARTESIAN_POINT ( 'NONE',  ( 3.000000000000000888, -5.117118920208326038, -22.42251312757885273 ) ) ;
#9677=CARTESIAN_POINT ( 'NONE',  ( 3.000000000000000888, 0.000000000000000000, 0.000000000000000000 ) ) ;
#9678=ORIENTED_EDGE ( 'NONE', *, *, #609, .T. ) ;
#9680=DIRECTION ( 'NONE',  ( -1.000000000000000000, 0.000000000000000000, 0.000000000000000000 ) ) ;
#9683=EDGE_CURVE ( 'NONE', #2943, #4581, #10710, .T. ) ;
#9685=CARTESIAN_POINT ( 'NONE',  ( 1.500000000000000444, -6.168200451485581048, -24.02068490260619171 ) ) ;
#9687=( NAMED_UNIT ( * ) PLANE_ANGLE_UNIT ( ) SI_UNIT ( $, .RADIAN. ) );
#9690=CIRCLE ( 'NONE', #4412, 22.99899999999999523 ) ;
#9691=ORIENTED_EDGE ( 'NONE', *, *, #2282, .T. ) ;
#9692=CARTESIAN_POINT ( 'NONE',  ( 0.000000000000000000, 0.000000000000000000, 0.000000000000000000 ) ) ;
#9693=ORIENTED_EDGE ( 'NONE', *, *, #5367, .F. ) ;
#9694=VERTEX_POINT ( 'NONE', #5089 ) ;
#9695=DIRECTION ( 'NONE',  ( 0.000000000000000000, -0.4067366430757887730, -0.9135454576426059736 ) ) ;
#9696=ADVANCED_FACE ( 'NONE', ( #257 ), #9739, .T. ) ;
#9697=FACE_OUTER_BOUND ( 'NONE', #3539, .T. ) ;
#9698=CIRCLE ( 'NONE', #9891, 22.99900000000000233 ) ;
#9699=LINE ( 'NONE', #2412, #10187 ) ;
#9702=LINE ( 'NONE', #10441, #6640 ) ;
#9703=ORIENTED_EDGE ( 'NONE', *, *, #10475, .F. ) ;
#9704=ORIENTED_EDGE ( 'NONE', *, *, #4862, .T. ) ;
#9707=DIRECTION ( 'NONE',  ( -1.000000000000000000, 0.000000000000000000, 0.000000000000000000 ) ) ;
#9708=DIRECTION ( 'NONE',  ( 0.000000000000000000, 0.000000000000000000, -1.000000000000000000 ) ) ;
#9709=DIRECTION ( 'NONE',  ( -0.000000000000000000, 0.000000000000000000, 1.000000000000000000 ) ) ;
#9710=DIRECTION ( 'NONE',  ( -1.000000000000000000, -0.000000000000000000, -0.000000000000000000 ) ) ;
#9712=EDGE_CURVE ( 'NONE', #348, #3644, #10904, .T. ) ;
#9713=FACE_OUTER_BOUND ( 'NONE', #6869, .T. ) ;
#9714=EDGE_LOOP ( 'NONE', ( #7161, #1141, #1413, #9927 ) ) ;
#9718=ORIENTED_EDGE ( 'NONE', *, *, #1828, .T. ) ;
#9719=DIRECTION ( 'NONE',  ( -1.000000000000000000, 0.000000000000000000, 0.000000000000000000 ) ) ;
#9720=LINE ( 'NONE', #5940, #7491 ) ;
#9721=CIRCLE ( 'NONE', #4445, 9.599999999999997868 ) ;
#9722=DIRECTION ( 'NONE',  ( 1.000000000000000000, -0.000000000000000000, -0.000000000000000000 ) ) ;
#9723=ORIENTED_EDGE ( 'NONE', *, *, #11915, .T. ) ;
#9724=ADVANCED_FACE ( 'NONE', ( #7724 ), #3083, .T. ) ;
#9726=EDGE_CURVE ( 'NONE', #11027, #5571, #10719, .T. ) ;
#9727=CARTESIAN_POINT ( 'NONE',  ( 0.000000000000000000, -21.97702544527753332, -6.779701584702958250 ) ) ;
#9729=ORIENTED_EDGE ( 'NONE', *, *, #288, .F. ) ;
#9731=VECTOR ( 'NONE', #9323, 1000.000000000000000 ) ;
#9732=ORIENTED_EDGE ( 'NONE', *, *, #11625, .T. ) ;
#9733=CARTESIAN_POINT ( 'NONE',  ( 0.000000000000000000, -2.811977935937933104, 22.37663021667342989 ) ) ;
#9734=VERTEX_POINT ( 'NONE', #6920 ) ;
#9736=DIRECTION ( 'NONE',  ( -1.000000000000000000, -0.000000000000000000, 0.000000000000000000 ) ) ;
#9738=AXIS2_PLACEMENT_3D ( 'NONE', #1886, #2869, #6474 ) ;
#9739=CYLINDRICAL_SURFACE ( 'NONE', #4253, 24.80000000000000071 ) ;
#9740=CARTESIAN_POINT ( 'NONE',  ( 0.000000000000000000, 0.000000000000000000, 0.000000000000000000 ) ) ;
#9742=CARTESIAN_POINT ( 'NONE',  ( 3.000000000000000888, -17.31945870441157354, 15.13242714128113775 ) ) ;
#9744=CARTESIAN_POINT ( 'NONE',  ( -10.00000000000000000, 0.000000000000000000, 0.000000000000000000 ) ) ;
#9745=ORIENTED_EDGE ( 'NONE', *, *, #11527, .F. ) ;
#9747=ORIENTED_EDGE ( 'NONE', *, *, #5161, .T. ) ;
#9748=CIRCLE ( 'NONE', #1931, 22.99899999999999878 ) ;
#9749=CIRCLE ( 'NONE', #11317, 22.99900000000000233 ) ;
#9751=EDGE_CURVE ( 'NONE', #1049, #5811, #3875, .T. ) ;
#9752=DIRECTION ( 'NONE',  ( -1.000000000000000000, 0.000000000000000000, -0.000000000000000000 ) ) ;
#9753=ORIENTED_EDGE ( 'NONE', *, *, #5158, .F. ) ;
#9754=CARTESIAN_POINT ( 'NONE',  ( 3.000000000000000888, 0.000000000000000000, 0.000000000000000000 ) ) ;
#9756=CIRCLE ( 'NONE', #4880, 22.99899999999999523 ) ;
#9759=DIRECTION ( 'NONE',  ( 0.000000000000000000, 0.000000000000000000, 1.000000000000000000 ) ) ;
#9761=EDGE_CURVE ( 'NONE', #1309, #8897, #7784, .T. ) ;
#9762=ORIENTED_EDGE ( 'NONE', *, *, #4154, .T. ) ;
#9763=VERTEX_POINT ( 'NONE', #315 ) ;
#9764=DIRECTION ( 'NONE',  ( -1.000000000000000000, 0.000000000000000000, 0.000000000000000000 ) ) ;
#9765=CIRCLE ( 'NONE', #8802, 9.599999999999997868 ) ;
#9766=CARTESIAN_POINT ( 'NONE',  ( 1.500000000000000444, -3.623565124516942237, -24.53384959170461599 ) ) ;
#9767=DIRECTION ( 'NONE',  ( 0.000000000000000000, 0.000000000000000000, 1.000000000000000000 ) ) ;
#9769=AXIS2_PLACEMENT_3D ( 'NONE', #335, #2114, #6884 ) ;
#9770=CARTESIAN_POINT ( 'NONE',  ( 1.499999999999999556, -24.53384959170460178, 3.623565124517029279 ) ) ;
#9771=VECTOR ( 'NONE', #7772, 1000.000000000000000 ) ;
#9772=FACE_OUTER_BOUND ( 'NONE', #3816, .T. ) ;
#9773=ORIENTED_EDGE ( 'NONE', *, *, #2846, .T. ) ;
#9774=ORIENTED_EDGE ( 'NONE', *, *, #4040, .T. ) ;
#9776=VERTEX_POINT ( 'NONE', #10604 ) ;
#9777=DIRECTION ( 'NONE',  ( 0.000000000000000000, -0.9510565162951503115, -0.3090169943749572767 ) ) ;
#9778=CARTESIAN_POINT ( 'NONE',  ( 3.000000000000000888, 21.76479567747241717, 7.432877647175279101 ) ) ;
#9781=DIRECTION ( 'NONE',  ( 0.000000000000000000, 0.000000000000000000, 1.000000000000000000 ) ) ;
#9782=AXIS2_PLACEMENT_3D ( 'NONE', #5568, #11862, #2685 ) ;
#9784=AXIS2_PLACEMENT_3D ( 'NONE', #6792, #2149, #366 ) ;
#9785=CARTESIAN_POINT ( 'NONE',  ( 3.000000000000000888, -9.039786367038701087, -21.14796121233205284 ) ) ;
#9787=DIRECTION ( 'NONE',  ( 0.000000000000000000, 0.000000000000000000, 1.000000000000000000 ) ) ;
#9789=EDGE_CURVE ( 'NONE', #6735, #11676, #10508, .T. ) ;
#9790=ORIENTED_EDGE ( 'NONE', *, *, #11659, .F. ) ;
#9792=DIRECTION ( 'NONE',  ( 0.000000000000000000, 0.8660254037844397068, -0.4999999999999980016 ) ) ;
#9793=CIRCLE ( 'NONE', #5498, 24.80000000000000071 ) ;
#9794=DIRECTION ( 'NONE',  ( -1.000000000000000000, 0.000000000000000000, -0.000000000000000000 ) ) ;
#9795=VECTOR ( 'NONE', #8079, 1000.000000000000000 ) ;
#9796=VERTEX_POINT ( 'NONE', #6975 ) ;
#9799=ORIENTED_EDGE ( 'NONE', *, *, #11523, .T. ) ;
#9800=CARTESIAN_POINT ( 'NONE',  ( 3.000000000000000888, 21.76479567747252020, -7.432877647174977120 ) ) ;
#9802=EDGE_LOOP ( 'NONE', ( #8341, #12117, #12006, #9847 ) ) ;
#9803=EDGE_CURVE ( 'NONE', #11729, #10656, #12068, .T. ) ;
#9805=CARTESIAN_POINT ( 'NONE',  ( 0.000000000000000000, 21.97817939804055598, -11.48910920600660646 ) ) ;
#9806=AXIS2_PLACEMENT_3D ( 'NONE', #2661, #8229, #3522 ) ;
#9807=DIRECTION ( 'NONE',  ( -1.000000000000000000, -0.000000000000000000, -0.000000000000000000 ) ) ;
#9809=CARTESIAN_POINT ( 'NONE',  ( 0.000000000000000000, -17.97274125076064877, -13.62355943574037731 ) ) ;
#9811=DIRECTION ( 'NONE',  ( 1.000000000000000000, 0.000000000000000000, 0.000000000000000000 ) ) ;
#9812=EDGE_LOOP ( 'NONE', ( #151, #6282, #8804, #2837 ) ) ;
#9813=CARTESIAN_POINT ( 'NONE',  ( 0.000000000000000000, 0.000000000000000000, 0.000000000000000000 ) ) ;
#9814=CIRCLE ( 'NONE', #10796, 9.599999999999996092 ) ;
#9815=ORIENTED_EDGE ( 'NONE', *, *, #9134, .T. ) ;
#9817=CIRCLE ( 'NONE', #10798, 22.99899999999999878 ) ;
#9818=CARTESIAN_POINT ( 'NONE',  ( 0.000000000000000000, 0.000000000000000000, 0.000000000000000000 ) ) ;
#9819=VERTEX_POINT ( 'NONE', #2276 ) ;
#9820=CARTESIAN_POINT ( 'NONE',  ( -10.00000000000000000, 0.000000000000000000, 0.000000000000000000 ) ) ;
#9823=AXIS2_PLACEMENT_3D ( 'NONE', #1876, #958, #4694 ) ;
#9824=EDGE_CURVE ( 'NONE', #2472, #3273, #8090, .T. ) ;
#9826=CARTESIAN_POINT ( 'NONE',  ( 3.000000000000000888, 0.000000000000000000, 0.000000000000000000 ) ) ;
#9827=DIRECTION ( 'NONE',  ( 0.000000000000000000, 0.000000000000000000, 1.000000000000000000 ) ) ;
#9828=ORIENTED_EDGE ( 'NONE', *, *, #11105, .F. ) ;
#9829=EDGE_CURVE ( 'NONE', #6927, #7251, #3383, .T. ) ;
#9830=ORIENTED_EDGE ( 'NONE', *, *, #3456, .T. ) ;
#9831=ORIENTED_EDGE ( 'NONE', *, *, #9121, .T. ) ;
#9832=AXIS2_PLACEMENT_3D ( 'NONE', #1229, #9549, #4901 ) ;
#9833=EDGE_CURVE ( 'NONE', #9318, #9844, #10314, .T. ) ;
#9836=CARTESIAN_POINT ( 'NONE',  ( -10.00000000000000000, 0.000000000000000000, 0.000000000000000000 ) ) ;
#9837=CIRCLE ( 'NONE', #7084, 24.80000000000000071 ) ;
#9838=CARTESIAN_POINT ( 'NONE',  ( 1.499999999999999556, 4.135161237383580435, 24.45282072769602166 ) ) ;
#9839=EDGE_CURVE ( 'NONE', #10975, #9118, #1536, .T. ) ;
#9841=CIRCLE ( 'NONE', #11791, 9.599999999999997868 ) ;
#9842=CYLINDRICAL_SURFACE ( 'NONE', #210, 22.99899999999999878 ) ;
#9843=CARTESIAN_POINT ( 'NONE',  ( 0.000000000000000000, 4.445336973060856955, 22.56530478845650123 ) ) ;
#9844=VERTEX_POINT ( 'NONE', #11758 ) ;
#9845=VERTEX_POINT ( 'NONE', #6321 ) ;
#9847=ORIENTED_EDGE ( 'NONE', *, *, #11442, .T. ) ;
#9848=CARTESIAN_POINT ( 'NONE',  ( 0.000000000000000000, 0.000000000000000000, 0.000000000000000000 ) ) ;
#9849=DIRECTION ( 'NONE',  ( -1.000000000000000000, 0.000000000000000000, 0.000000000000000000 ) ) ;
#9850=CARTESIAN_POINT ( 'NONE',  ( 3.000000000000000888, -3.623565124516938685, -24.53384959170461244 ) ) ;
#9851=ADVANCED_FACE ( 'NONE', ( #3622 ), #8945, .T. ) ;
#9853=DIRECTION ( 'NONE',  ( -1.000000000000000000, -0.000000000000000000, -0.000000000000000000 ) ) ;
#9854=ORIENTED_EDGE ( 'NONE', *, *, #4424, .F. ) ;
#9855=CARTESIAN_POINT ( 'NONE',  ( 0.000000000000000000, 20.41249101028211754, 9.589108953447965433 ) ) ;
#9856=DIRECTION ( 'NONE',  ( -1.000000000000000000, -0.000000000000000000, 0.000000000000000000 ) ) ;
#9858=DIRECTION ( 'NONE',  ( -1.000000000000000000, 0.000000000000000000, -0.000000000000000000 ) ) ;
#9859=AXIS2_PLACEMENT_3D ( 'NONE', #7850, #11586, #10666 ) ;
#9860=DIRECTION ( 'NONE',  ( 0.000000000000000000, 0.000000000000000000, 1.000000000000000000 ) ) ;
#9861=ORIENTED_EDGE ( 'NONE', *, *, #9499, .T. ) ;
#9863=VERTEX_POINT ( 'NONE', #5450 ) ;
#9864=CARTESIAN_POINT ( 'NONE',  ( 3.000000000000000888, 0.000000000000000000, 0.000000000000000000 ) ) ;
#9866=VERTEX_POINT ( 'NONE', #2698 ) ;
#9868=DIRECTION ( 'NONE',  ( -1.000000000000000000, 0.000000000000000000, -0.000000000000000000 ) ) ;
#9870=DIRECTION ( 'NONE',  ( 0.000000000000000000, -0.3090169943749545012, 0.9510565162951513107 ) ) ;
#9873=CARTESIAN_POINT ( 'NONE',  ( 0.000000000000000000, -23.05871956130116018, -9.128825345753257992 ) ) ;
#9874=EDGE_CURVE ( 'NONE', #10068, #1657, #2498, .T. ) ;
#9875=CARTESIAN_POINT ( 'NONE',  ( 3.000000000000000888, -0.3433949777333296094, 22.99643626497956816 ) ) ;
#9876=ORIENTED_EDGE ( 'NONE', *, *, #7929, .T. ) ;
#9877=DIRECTION ( 'NONE',  ( -1.000000000000000000, 0.000000000000000000, 0.000000000000000000 ) ) ;
#9879=VERTEX_POINT ( 'NONE', #1663 ) ;
#9880=DIRECTION ( 'NONE',  ( -1.000000000000000000, -0.000000000000000000, -0.000000000000000000 ) ) ;
#9883=ADVANCED_FACE ( 'NONE', ( #5273 ), #11998, .T. ) ;
#9886=EDGE_CURVE ( 'NONE', #7518, #9078, #251, .T. ) ;
#9887=DIRECTION ( 'NONE',  ( -1.000000000000000000, 0.000000000000000000, 0.000000000000000000 ) ) ;
#9889=ORIENTED_EDGE ( 'NONE', *, *, #2846, .F. ) ;
#9891=AXIS2_PLACEMENT_3D ( 'NONE', #4848, #128, #3024 ) ;
#9893=CARTESIAN_POINT ( 'NONE',  ( 0.000000000000000000, 22.56530478845649057, 4.445336973060936891 ) ) ;
#9894=DIRECTION ( 'NONE',  ( 0.000000000000000000, -6.866613759074863256E-15, 1.000000000000000000 ) ) ;
#9896=CARTESIAN_POINT ( 'NONE',  ( 1.500000000000000444, 17.71842311621552923, -17.35216073792423330 ) ) ;
#9897=AXIS2_PLACEMENT_3D ( 'NONE', #9610, #1226, #9781 ) ;
#9898=DIRECTION ( 'NONE',  ( -1.000000000000000000, -0.000000000000000000, -0.000000000000000000 ) ) ;
#9899=ORIENTED_EDGE ( 'NONE', *, *, #6168, .T. ) ;
#9902=ORIENTED_EDGE ( 'NONE', *, *, #10856, .T. ) ;
#9904=CYLINDRICAL_SURFACE ( 'NONE', #10340, 9.599999999999997868 ) ;
#9905=DIRECTION ( 'NONE',  ( -1.000000000000000000, 0.000000000000000000, -0.000000000000000000 ) ) ;
#9906=CARTESIAN_POINT ( 'NONE',  ( 3.000000000000000888, -4.240409074144249502, 22.15038895030647836 ) ) ;
#9907=ORIENTED_EDGE ( 'NONE', *, *, #6655, .T. ) ;
#9908=EDGE_CURVE ( 'NONE', #4202, #8369, #10416, .T. ) ;
#9909=CARTESIAN_POINT ( 'NONE',  ( 3.000000000000000888, 22.15038895030649257, 4.240409074144170454 ) ) ;
#9910=DIRECTION ( 'NONE',  ( -1.000000000000000000, 0.000000000000000000, 0.000000000000000000 ) ) ;
#9912=DIRECTION ( 'NONE',  ( 1.000000000000000000, 0.000000000000000000, 0.000000000000000000 ) ) ;
#9913=CARTESIAN_POINT ( 'NONE',  ( 3.000000000000000888, -0.3433949777333296094, 22.99643626497956816 ) ) ;
#9914=EDGE_CURVE ( 'NONE', #2253, #1383, #8072, .T. ) ;
#9915=VERTEX_POINT ( 'NONE', #801 ) ;
#9918=DIRECTION ( 'NONE',  ( 0.000000000000000000, -0.4067366430757888285, -0.9135454576426059736 ) ) ;
#9919=DIRECTION ( 'NONE',  ( -1.000000000000000000, -0.000000000000000000, -0.000000000000000000 ) ) ;
#9920=DIRECTION ( 'NONE',  ( -1.000000000000000000, -0.000000000000000000, -0.000000000000000000 ) ) ;
#9921=DIRECTION ( 'NONE',  ( 0.000000000000000000, -0.2079116908177468526, -0.9781476007338083534 ) ) ;
#9923=DIRECTION ( 'NONE',  ( 0.000000000000000000, -0.1045284632676607012, 0.9945218953682726237 ) ) ;
#9925=CARTESIAN_POINT ( 'NONE',  ( 3.000000000000000888, -2.062268319295719632, 22.90635393027945454 ) ) ;
#9926=LINE ( 'NONE', #9875, #4709 ) ;
#9927=ORIENTED_EDGE ( 'NONE', *, *, #3739, .T. ) ;
#9928=FACE_OUTER_BOUND ( 'NONE', #4819, .T. ) ;
#9929=VECTOR ( 'NONE', #4150, 1000.000000000000000 ) ;
#9930=CIRCLE ( 'NONE', #5242, 9.599999999999996092 ) ;
#9931=CARTESIAN_POINT ( 'NONE',  ( 3.000000000000000888, -20.78471918669854901, -8.753070780933368766 ) ) ;
#9932=ORIENTED_EDGE ( 'NONE', *, *, #1715, .F. ) ;
#9933=CARTESIAN_POINT ( 'NONE',  ( -10.00000000000000000, 0.000000000000000000, 0.000000000000000000 ) ) ;
#9934=CARTESIAN_POINT ( 'NONE',  ( 0.000000000000000000, 0.000000000000000000, 0.000000000000000000 ) ) ;
#9935=DIRECTION ( 'NONE',  ( 1.000000000000000000, -0.000000000000000000, 0.000000000000000000 ) ) ;
#9937=CARTESIAN_POINT ( 'NONE',  ( 0.000000000000000000, -15.42759117534397006, 16.45023496161660148 ) ) ;
#9939=CARTESIAN_POINT ( 'NONE',  ( 0.000000000000000000, -3.623565124517270419, 24.53384959170456270 ) ) ;
#9940=ADVANCED_FACE ( 'NONE', ( #4354 ), #736, .T. ) ;
#9941=ORIENTED_EDGE ( 'NONE', *, *, #6830, .T. ) ;
#9942=VECTOR ( 'NONE', #11708, 1000.000000000000000 ) ;
#9943=VERTEX_POINT ( 'NONE', #5341 ) ;
#9944=EDGE_LOOP ( 'NONE', ( #385, #11716, #6751, #2298 ) ) ;
#9945=EDGE_CURVE ( 'NONE', #11132, #1751, #6699, .T. ) ;
#9947=EDGE_CURVE ( 'NONE', #5671, #2749, #11786, .T. ) ;
#9948=AXIS2_PLACEMENT_3D ( 'NONE', #7447, #8020, #10843 ) ;
#9949=CARTESIAN_POINT ( 'NONE',  ( 0.000000000000000000, 21.58580335785685378, -6.532525787310757615 ) ) ;
#9950=DIRECTION ( 'NONE',  ( 0.000000000000000000, -0.7431448254773863615, -0.6691306063588672304 ) ) ;
#9951=EDGE_CURVE ( 'NONE', #219, #10824, #5348, .T. ) ;
#9953=DIRECTION ( 'NONE',  ( 0.000000000000000000, 0.000000000000000000, 1.000000000000000000 ) ) ;
#9954=CARTESIAN_POINT ( 'NONE',  ( 0.000000000000000000, -15.42759117534374447, -16.45023496161680754 ) ) ;
#9955=AXIS2_PLACEMENT_3D ( 'NONE', #5804, #4022, #1147 ) ;
#9957=ORIENTED_EDGE ( 'NONE', *, *, #2250, .F. ) ;
#9958=AXIS2_PLACEMENT_3D ( 'NONE', #1096, #11491, #9598 ) ;
#9959=VERTEX_POINT ( 'NONE', #11028 ) ;
#9961=CARTESIAN_POINT ( 'NONE',  ( 3.000000000000000888, 19.29833442572375546, -11.67026512804527272 ) ) ;
#9962=CYLINDRICAL_SURFACE ( 'NONE', #1528, 9.599999999999997868 ) ;
#9964=CARTESIAN_POINT ( 'NONE',  ( 3.000000000000000888, -17.06259499759954679, 14.74749645580005364 ) ) ;
#9965=AXIS2_PLACEMENT_3D ( 'NONE', #8543, #2673, #7549 ) ;
#9966=CARTESIAN_POINT ( 'NONE',  ( 3.000000000000000888, 21.14796121233209192, -9.039786367038628256 ) ) ;
#9968=ADVANCED_FACE ( 'NONE', ( #4544 ), #8274, .T. ) ;
#9969=DIRECTION ( 'NONE',  ( 0.000000000000000000, 0.3090169943749479509, -0.9510565162951534202 ) ) ;
#9970=ORIENTED_EDGE ( 'NONE', *, *, #6755, .F. ) ;
#9971=FACE_OUTER_BOUND ( 'NONE', #10924, .T. ) ;
#9972=AXIS2_PLACEMENT_3D ( 'NONE', #6926, #5842, #7790 ) ;
#9975=ORIENTED_EDGE ( 'NONE', *, *, #9951, .T. ) ;
#9976=AXIS2_PLACEMENT_3D ( 'NONE', #7264, #8325, #3729 ) ;
#9978=CIRCLE ( 'NONE', #9187, 24.80000000000000071 ) ;
#9979=DIRECTION ( 'NONE',  ( -1.000000000000000000, 0.000000000000000000, -0.000000000000000000 ) ) ;
#9980=DIRECTION ( 'NONE',  ( -1.000000000000000000, 0.000000000000000000, 0.000000000000000000 ) ) ;
#9981=EDGE_CURVE ( 'NONE', #8199, #6260, #10341, .T. ) ;
#9982=DIRECTION ( 'NONE',  ( 0.000000000000000000, 0.1045284632676471287, 0.9945218953682740670 ) ) ;
#9984=CIRCLE ( 'NONE', #3938, 24.80000000000000071 ) ;
#9985=VECTOR ( 'NONE', #3782, 1000.000000000000000 ) ;
#9987=LINE ( 'NONE', #3449, #586 ) ;
#9988=ORIENTED_EDGE ( 'NONE', *, *, #633, .F. ) ;
#9989=DIRECTION ( 'NONE',  ( 0.000000000000000000, 0.000000000000000000, 1.000000000000000000 ) ) ;
#9990=VERTEX_POINT ( 'NONE', #2945 ) ;
#9992=CIRCLE ( 'NONE', #10359, 22.99899999999999523 ) ;
#9994=VERTEX_POINT ( 'NONE', #60 ) ;
#9995=AXIS2_PLACEMENT_3D ( 'NONE', #5687, #10740, #47 ) ;
#9996=CARTESIAN_POINT ( 'NONE',  ( 3.000000000000000888, 19.10918332567978695, -15.80756504416672215 ) ) ;
#10000=CARTESIAN_POINT ( 'NONE',  ( 3.000000000000000888, 24.77821629063821973, 1.039229259764575364 ) ) ;
#10001=AXIS2_PLACEMENT_3D ( 'NONE', #4666, #8398, #3746 ) ;
#10002=DIRECTION ( 'NONE',  ( -1.000000000000000000, 0.000000000000000000, -0.000000000000000000 ) ) ;
#10003=ORIENTED_EDGE ( 'NONE', *, *, #1272, .F. ) ;
#10005=ORIENTED_EDGE ( 'NONE', *, *, #7162, .F. ) ;
#10007=AXIS2_PLACEMENT_3D ( 'NONE', #6785, #3068, #4221 ) ;
#10012=ADVANCED_FACE ( 'NONE', ( #9250 ), #6607, .T. ) ;
#10013=CARTESIAN_POINT ( 'NONE',  ( 1.500000000000000444, -23.24434456306319419, -8.645255683529244450 ) ) ;
#10014=ORIENTED_EDGE ( 'NONE', *, *, #4192, .F. ) ;
#10016=PRODUCT_CONTEXT ( 'NONE', #5124, 'mechanical' ) ;
#10017=ADVANCED_FACE ( 'NONE', ( #9432 ), #11271, .T. ) ;
#10018=ORIENTED_EDGE ( 'NONE', *, *, #6624, .F. ) ;
#10020=AXIS2_PLACEMENT_3D ( 'NONE', #4721, #5698, #9426 ) ;
#10021=DIRECTION ( 'NONE',  ( 0.000000000000000000, 0.000000000000000000, 1.000000000000000000 ) ) ;
#10023=FACE_OUTER_BOUND ( 'NONE', #8899, .T. ) ;
#10024=ORIENTED_EDGE ( 'NONE', *, *, #6762, .F. ) ;
#10025=AXIS2_PLACEMENT_3D ( 'NONE', #6434, #1902, #8576 ) ;
#10026=DIRECTION ( 'NONE',  ( 0.000000000000000000, 0.000000000000000000, 1.000000000000000000 ) ) ;
#10027=CARTESIAN_POINT ( 'NONE',  ( 3.000000000000000888, -10.87771529938148518, -19.75591328264897228 ) ) ;
#10030=AXIS2_PLACEMENT_3D ( 'NONE', #6724, #11267, #4833 ) ;
#10031=DIRECTION ( 'NONE',  ( -1.000000000000000000, -0.000000000000000000, 0.000000000000000000 ) ) ;
#10032=ORIENTED_EDGE ( 'NONE', *, *, #8781, .F. ) ;
#10033=DIRECTION ( 'NONE',  ( -1.000000000000000000, 0.000000000000000000, 0.000000000000000000 ) ) ;
#10034=ORIENTED_EDGE ( 'NONE', *, *, #10417, .F. ) ;
#10035=CIRCLE ( 'NONE', #854, 9.599999999999999645 ) ;
#10036=ORIENTED_EDGE ( 'NONE', *, *, #9726, .T. ) ;
#10038=VERTEX_POINT ( 'NONE', #10406 ) ;
#10040=CARTESIAN_POINT ( 'NONE',  ( 3.000000000000000888, 0.000000000000000000, 0.000000000000000000 ) ) ;
#10041=ORIENTED_EDGE ( 'NONE', *, *, #10692, .T. ) ;
#10042=DIRECTION ( 'NONE',  ( -1.000000000000000000, 0.000000000000000000, 0.000000000000000000 ) ) ;
#10043=CARTESIAN_POINT ( 'NONE',  ( 3.000000000000000888, -7.402892494506152943, -21.30300407174369681 ) ) ;
#10045=EDGE_CURVE ( 'NONE', #7806, #6896, #2023, .T. ) ;
#10046=CIRCLE ( 'NONE', #4972, 22.99900000000000588 ) ;
#10047=CARTESIAN_POINT ( 'NONE',  ( 3.000000000000000888, 1.556492618230968628, -24.75110766671650353 ) ) ;
#10048=DIRECTION ( 'NONE',  ( 0.000000000000000000, -6.866613759074863256E-15, 1.000000000000000000 ) ) ;
#10049=ORIENTED_EDGE ( 'NONE', *, *, #11369, .F. ) ;
#10050=ORIENTED_EDGE ( 'NONE', *, *, #4814, .F. ) ;
#10051=CARTESIAN_POINT ( 'NONE',  ( 3.000000000000000888, -19.43515443678392529, -15.40502424595165110 ) ) ;
#10052=EDGE_LOOP ( 'NONE', ( #7769, #11412, #10683, #6530 ) ) ;
#10053=EDGE_CURVE ( 'NONE', #5516, #8808, #4166, .T. ) ;
#10055=VECTOR ( 'NONE', #5958, 1000.000000000000000 ) ;
#10056=DIRECTION ( 'NONE',  ( -1.000000000000000000, -0.000000000000000000, 0.000000000000000000 ) ) ;
#10057=EDGE_LOOP ( 'NONE', ( #6251, #1187, #2971, #5222 ) ) ;
#10058=DIRECTION ( 'NONE',  ( -1.000000000000000000, 0.000000000000000000, -0.000000000000000000 ) ) ;
#10059=DIRECTION ( 'NONE',  ( -1.000000000000000000, 0.000000000000000000, 0.000000000000000000 ) ) ;
#10061=EDGE_CURVE ( 'NONE', #11676, #10279, #5138, .T. ) ;
#10063=DIRECTION ( 'NONE',  ( -1.000000000000000000, -0.000000000000000000, -0.000000000000000000 ) ) ;
#10064=CYLINDRICAL_SURFACE ( 'NONE', #983, 9.599999999999996092 ) ;
#10066=VERTEX_POINT ( 'NONE', #5579 ) ;
#10068=VERTEX_POINT ( 'NONE', #7401 ) ;
#10070=CARTESIAN_POINT ( 'NONE',  ( 3.000000000000000888, 16.85990652506920995, -15.64281154287580655 ) ) ;
#10071=CARTESIAN_POINT ( 'NONE',  ( 3.000000000000000888, 0.000000000000000000, 0.000000000000000000 ) ) ;
#10072=CIRCLE ( 'NONE', #7132, 9.599999999999999645 ) ;
#10074=CARTESIAN_POINT ( 'NONE',  ( 3.000000000000000888, 0.000000000000000000, 0.000000000000000000 ) ) ;
#10075=DIRECTION ( 'NONE',  ( -1.000000000000000000, -0.000000000000000000, -0.000000000000000000 ) ) ;
#10076=ORIENTED_EDGE ( 'NONE', *, *, #1115, .T. ) ;
#10077=VERTEX_POINT ( 'NONE', #924 ) ;
#10078=ORIENTED_EDGE ( 'NONE', *, *, #11320, .T. ) ;
#10080=DIRECTION ( 'NONE',  ( 0.000000000000000000, 0.9510565162951523099, 0.3090169943749513370 ) ) ;
#10081=FACE_OUTER_BOUND ( 'NONE', #7120, .T. ) ;
#10083=VECTOR ( 'NONE', #6906, 1000.000000000000000 ) ;
#10084=EDGE_CURVE ( 'NONE', #8696, #9118, #2611, .T. ) ;
#10085=DIRECTION ( 'NONE',  ( 1.000000000000000000, -0.000000000000000000, -0.000000000000000000 ) ) ;
#10087=DIRECTION ( 'NONE',  ( -1.000000000000000000, 0.000000000000000000, 0.000000000000000000 ) ) ;
#10088=EDGE_LOOP ( 'NONE', ( #7222, #1072, #4297, #10981 ) ) ;
#10089=LINE ( 'NONE', #4654, #1588 ) ;
#10090=ORIENTED_EDGE ( 'NONE', *, *, #9585, .F. ) ;
#10093=EDGE_CURVE ( 'NONE', #10640, #5406, #2995, .T. ) ;
#10095=FACE_OUTER_BOUND ( 'NONE', #5137, .T. ) ;
#10096=EDGE_LOOP ( 'NONE', ( #8644, #8497, #235, #3305 ) ) ;
#10097=EDGE_CURVE ( 'NONE', #5247, #10333, #7271, .T. ) ;
#10098=CARTESIAN_POINT ( 'NONE',  ( 3.000000000000000888, 5.135568396240338451, -21.96011696265485824 ) ) ;
#10099=ADVANCED_FACE ( 'NONE', ( #11213 ), #4727, .T. ) ;
#10100=LINE ( 'NONE', #871, #7706 ) ;
#10103=CYLINDRICAL_SURFACE ( 'NONE', #1388, 22.99899999999999878 ) ;
#10104=ORIENTED_EDGE ( 'NONE', *, *, #11527, .T. ) ;
#10105=ORIENTED_EDGE ( 'NONE', *, *, #11812, .T. ) ;
#10106=DIRECTION ( 'NONE',  ( -1.000000000000000000, 0.000000000000000000, -0.000000000000000000 ) ) ;
#10107=VERTEX_POINT ( 'NONE', #6908 ) ;
#10110=CARTESIAN_POINT ( 'NONE',  ( 0.000000000000000000, -22.37663021667341923, 6.788022064061986605 ) ) ;
#10111=AXIS2_PLACEMENT_3D ( 'NONE', #2840, #2042, #7482 ) ;
#10112=CARTESIAN_POINT ( 'NONE',  ( 0.000000000000000000, 6.168200451485757796, 24.02068490260614908 ) ) ;
#10113=DIRECTION ( 'NONE',  ( -1.000000000000000000, 0.000000000000000000, -0.000000000000000000 ) ) ;
#10116=FACE_OUTER_BOUND ( 'NONE', #4651, .T. ) ;
#10117=DIRECTION ( 'NONE',  ( -1.000000000000000000, 0.000000000000000000, -0.000000000000000000 ) ) ;
#10118=ORIENTED_EDGE ( 'NONE', *, *, #1982, .T. ) ;
#10119=AXIS2_PLACEMENT_3D ( 'NONE', #222, #9710, #9532 ) ;
#10120=VERTEX_POINT ( 'NONE', #2140 ) ;
#10121=ORIENTED_EDGE ( 'NONE', *, *, #4485, .T. ) ;
#10122=EDGE_CURVE ( 'NONE', #9694, #4337, #9449, .T. ) ;
#10123=DIRECTION ( 'NONE',  ( 0.000000000000000000, 0.000000000000000000, 1.000000000000000000 ) ) ;
#10125=CARTESIAN_POINT ( 'NONE',  ( 0.000000000000000000, -11.20082935824061110, -20.08719549084876732 ) ) ;
#10126=CARTESIAN_POINT ( 'NONE',  ( 3.000000000000000888, -13.79477846460783574, -18.40266524480602683 ) ) ;
#10128=AXIS2_PLACEMENT_3D ( 'NONE', #9280, #7302, #1871 ) ;
#10129=AXIS2_PLACEMENT_3D ( 'NONE', #2548, #12024, #7431 ) ;
#10130=EDGE_CURVE ( 'NONE', #3750, #10107, #6511, .T. ) ;
#10132=DIRECTION ( 'NONE',  ( 0.000000000000000000, 0.000000000000000000, 1.000000000000000000 ) ) ;
#10133=ORIENTED_EDGE ( 'NONE', *, *, #8254, .T. ) ;
#10134=DIRECTION ( 'NONE',  ( -1.000000000000000000, 0.000000000000000000, 0.000000000000000000 ) ) ;
#10135=EDGE_LOOP ( 'NONE', ( #2359, #6375, #5954, #3354 ) ) ;
#10137=CARTESIAN_POINT ( 'NONE',  ( 0.000000000000000000, -18.40266524480598065, 13.79477846460790502 ) ) ;
#10138=AXIS2_PLACEMENT_3D ( 'NONE', #1691, #9041, #9098 ) ;
#10139=CARTESIAN_POINT ( 'NONE',  ( 3.000000000000000888, -20.08719549084872824, 11.20082935824068038 ) ) ;
#10140=DIRECTION ( 'NONE',  ( 0.000000000000000000, -0.1045284632676401204, -0.9945218953682746221 ) ) ;
#10142=CARTESIAN_POINT ( 'NONE',  ( 0.000000000000000000, -24.02068490260616329, 6.168200451485676972 ) ) ;
#10143=DIRECTION ( 'NONE',  ( -1.000000000000000000, -0.000000000000000000, -0.000000000000000000 ) ) ;
#10144=CARTESIAN_POINT ( 'NONE',  ( 0.000000000000000000, 0.000000000000000000, 0.000000000000000000 ) ) ;
#10145=CARTESIAN_POINT ( 'NONE',  ( 3.000000000000000888, -13.23915371906942440, -18.80635025205183197 ) ) ;
#10146=CIRCLE ( 'NONE', #10928, 9.599999999999996092 ) ;
#10147=VECTOR ( 'NONE', #6135, 1000.000000000000000 ) ;
#10148=CIRCLE ( 'NONE', #11130, 9.599999999999997868 ) ;
#10149=CARTESIAN_POINT ( 'NONE',  ( 3.000000000000000888, 22.83456483164692585, -2.745295967525759995 ) ) ;
#10150=ORIENTED_EDGE ( 'NONE', *, *, #10951, .T. ) ;
#10151=ORIENTED_EDGE ( 'NONE', *, *, #4649, .T. ) ;
#10152=CARTESIAN_POINT ( 'NONE',  ( 1.500000000000000444, 17.35216073792464897, -17.71842311621511712 ) ) ;
#10153=EDGE_LOOP ( 'NONE', ( #9889, #7819 ) ) ;
#10154=ORIENTED_EDGE ( 'NONE', *, *, #2406, .T. ) ;
#10157=ORIENTED_EDGE ( 'NONE', *, *, #6208, .F. ) ;
#10158=DIRECTION ( 'NONE',  ( 0.000000000000000000, 0.000000000000000000, 1.000000000000000000 ) ) ;
#10159=EDGE_LOOP ( 'NONE', ( #7459, #3772, #1172, #7891 ) ) ;
#10160=AXIS2_PLACEMENT_3D ( 'NONE', #3089, #5788, #6928 ) ;
#10161=ADVANCED_FACE ( 'NONE', ( #3126 ), #8703, .T. ) ;
#10162=CARTESIAN_POINT ( 'NONE',  ( 0.000000000000000000, 0.000000000000000000, 0.000000000000000000 ) ) ;
#10163=CARTESIAN_POINT ( 'NONE',  ( 3.000000000000000888, -9.589108953448036488, 20.41249101028208202 ) ) ;
#10165=VECTOR ( 'NONE', #10117, 1000.000000000000000 ) ;
#10166=CARTESIAN_POINT ( 'NONE',  ( 3.000000000000000888, 8.753070780933159156, 20.78471918669863427 ) ) ;
#10167=VERTEX_POINT ( 'NONE', #4219 ) ;
#10168=VERTEX_POINT ( 'NONE', #5819 ) ;
#10169=CARTESIAN_POINT ( 'NONE',  ( -10.00000000000000000, 0.000000000000000000, 0.000000000000000000 ) ) ;
#10170=EDGE_CURVE ( 'NONE', #3469, #6885, #9055, .T. ) ;
#10171=AXIS2_PLACEMENT_3D ( 'NONE', #10294, #3629, #11280 ) ;
#10173=EDGE_CURVE ( 'NONE', #139, #4299, #7680, .T. ) ;
#10177=AXIS2_PLACEMENT_3D ( 'NONE', #7102, #10726, #2462 ) ;
#10178=CARTESIAN_POINT ( 'NONE',  ( 0.000000000000000000, -21.97817939804031795, -11.48910920600707186 ) ) ;
#10179=AXIS2_PLACEMENT_3D ( 'NONE', #5510, #6368, #2751 ) ;
#10180=CARTESIAN_POINT ( 'NONE',  ( 0.000000000000000000, 0.000000000000000000, 0.000000000000000000 ) ) ;
#10183=CARTESIAN_POINT ( 'NONE',  ( 0.000000000000000000, 0.000000000000000000, 0.000000000000000000 ) ) ;
#10184=EDGE_CURVE ( 'NONE', #9575, #8512, #2403, .T. ) ;
#10185=FACE_OUTER_BOUND ( 'NONE', #2333, .T. ) ;
#10186=VERTEX_POINT ( 'NONE', #1340 ) ;
#10187=VECTOR ( 'NONE', #4933, 1000.000000000000000 ) ;
#10188=VECTOR ( 'NONE', #7067, 1000.000000000000000 ) ;
#10189=AXIS2_PLACEMENT_3D ( 'NONE', #1948, #1314, #2176 ) ;
#10190=ORIENTED_EDGE ( 'NONE', *, *, #9521, .F. ) ;
#10191=DIRECTION ( 'NONE',  ( 0.000000000000000000, 0.000000000000000000, 1.000000000000000000 ) ) ;
#10193=DIRECTION ( 'NONE',  ( 0.000000000000000000, 0.000000000000000000, -1.000000000000000000 ) ) ;
#10194=ADVANCED_FACE ( 'NONE', ( #422 ), #10522, .T. ) ;
#10195=DIRECTION ( 'NONE',  ( 0.000000000000000000, -0.1045284632676605485, 0.9945218953682725127 ) ) ;
#10196=CIRCLE ( 'NONE', #11954, 24.80000000000000071 ) ;
#10198=CIRCLE ( 'NONE', #4928, 9.599999999999997868 ) ;
#10199=DIRECTION ( 'NONE',  ( -1.000000000000000000, 0.000000000000000000, -0.000000000000000000 ) ) ;
#10200=EDGE_CURVE ( 'NONE', #8183, #1245, #7079, .T. ) ;
#10201=CARTESIAN_POINT ( 'NONE',  ( 3.000000000000000888, 0.000000000000000000, 0.000000000000000000 ) ) ;
#10202=ORIENTED_EDGE ( 'NONE', *, *, #6441, .F. ) ;
#10203=ORIENTED_EDGE ( 'NONE', *, *, #11661, .F. ) ;
#10204=AXIS2_PLACEMENT_3D ( 'NONE', #7280, #7405, #11937 ) ;
#10205=ORIENTED_EDGE ( 'NONE', *, *, #5397, .F. ) ;
#10206=DIRECTION ( 'NONE',  ( 0.000000000000000000, 0.3090169943749415671, 0.9510565162951555296 ) ) ;
#10207=AXIS2_PLACEMENT_3D ( 'NONE', #7894, #9613, #1230 ) ;
#10208=CARTESIAN_POINT ( 'NONE',  ( 0.000000000000000000, 2.811977935938088535, -22.37663021667340857 ) ) ;
#10210=AXIS2_PLACEMENT_3D ( 'NONE', #1142, #1267, #1208 ) ;
#10211=DIRECTION ( 'NONE',  ( -1.000000000000000000, -0.000000000000000000, -0.000000000000000000 ) ) ;
#10212=CARTESIAN_POINT ( 'NONE',  ( 1.499999999999999556, 24.75110766671654616, -1.556492618230384872 ) ) ;
#10213=DIRECTION ( 'NONE',  ( 0.000000000000000000, 0.000000000000000000, -1.000000000000000000 ) ) ;
#10214=CIRCLE ( 'NONE', #11800, 9.599999999999996092 ) ;
#10217=CIRCLE ( 'NONE', #2604, 9.599999999999997868 ) ;
#10218=CARTESIAN_POINT ( 'NONE',  ( 1.499999999999999556, 24.45282072769606430, -4.135161237383341515 ) ) ;
#10219=ORIENTED_EDGE ( 'NONE', *, *, #5486, .T. ) ;
#10220=EDGE_LOOP ( 'NONE', ( #9145, #2687, #2032, #3751 ) ) ;
#10221=VECTOR ( 'NONE', #8110, 1000.000000000000000 ) ;
#10222=CARTESIAN_POINT ( 'NONE',  ( 0.000000000000000000, 24.75110766671654616, -1.556492618230386649 ) ) ;
#10223=ORIENTED_EDGE ( 'NONE', *, *, #4340, .F. ) ;
#10224=EDGE_LOOP ( 'NONE', ( #10937, #11089, #9599, #1561 ) ) ;
#10226=DIRECTION ( 'NONE',  ( -1.000000000000000000, 0.000000000000000000, 0.000000000000000000 ) ) ;
#10227=ORIENTED_EDGE ( 'NONE', *, *, #549, .F. ) ;
#10228=CARTESIAN_POINT ( 'NONE',  ( 3.000000000000000888, 7.402892494506291499, 21.30300407174365063 ) ) ;
#10229=DIRECTION ( 'NONE',  ( 0.000000000000000000, 0.000000000000000000, 1.000000000000000000 ) ) ;
#10233=CIRCLE ( 'NONE', #4962, 24.80000000000000071 ) ;
#10234=ORIENTED_EDGE ( 'NONE', *, *, #4639, .T. ) ;
#10235=EDGE_LOOP ( 'NONE', ( #3309, #2230, #6206, #326 ) ) ;
#10236=DIRECTION ( 'NONE',  ( 0.000000000000000000, 0.000000000000000000, 1.000000000000000000 ) ) ;
#10237=ORIENTED_EDGE ( 'NONE', *, *, #523, .F. ) ;
#10239=CARTESIAN_POINT ( 'NONE',  ( 1.500000000000000444, -11.02759168516760013, 22.21333432029560129 ) ) ;
#10241=AXIS2_PLACEMENT_3D ( 'NONE', #7231, #8225, #6389 ) ;
#10242=CARTESIAN_POINT ( 'NONE',  ( 8.000000000000000000, 0.000000000000000000, 19.99999999999999645 ) ) ;
#10243=EDGE_CURVE ( 'NONE', #3895, #11729, #4098, .T. ) ;
#10247=EDGE_CURVE ( 'NONE', #9423, #7806, #3786, .T. ) ;
#10248=EDGE_CURVE ( 'NONE', #1013, #6911, #11015, .T. ) ;
#10249=LINE ( 'NONE', #760, #10165 ) ;
#10250=ORIENTED_EDGE ( 'NONE', *, *, #9886, .F. ) ;
#10251=ORIENTED_EDGE ( 'NONE', *, *, #846, .F. ) ;
#10252=AXIS2_PLACEMENT_3D ( 'NONE', #5896, #7037, #2337 ) ;
#10253=VERTEX_POINT ( 'NONE', #11503 ) ;
#10254=CARTESIAN_POINT ( 'NONE',  ( 0.000000000000000000, -23.24434456306319419, -8.645255683529242674 ) ) ;
#10256=EDGE_CURVE ( 'NONE', #8647, #6529, #5744, .T. ) ;
#10257=FACE_OUTER_BOUND ( 'NONE', #2530, .T. ) ;
#10258=CYLINDRICAL_SURFACE ( 'NONE', #4082, 24.80000000000000071 ) ;
#10259=EDGE_CURVE ( 'NONE', #10253, #6369, #11624, .T. ) ;
#10261=CARTESIAN_POINT ( 'NONE',  ( 0.000000000000000000, -23.24434456306331143, 8.645255683528922930 ) ) ;
#10262=CARTESIAN_POINT ( 'NONE',  ( 0.000000000000000000, 21.97817939804039611, 11.48910920600691554 ) ) ;
#10263=ORIENTED_EDGE ( 'NONE', *, *, #5767, .T. ) ;
#10265=VERTEX_POINT ( 'NONE', #2319 ) ;
#10266=LINE ( 'NONE', #7508, #11212 ) ;
#10270=CARTESIAN_POINT ( 'NONE',  ( 0.000000000000000000, 9.589108953448178596, -20.41249101028201451 ) ) ;
#10273=CIRCLE ( 'NONE', #4613, 24.80000000000000071 ) ;
#10274=DIRECTION ( 'NONE',  ( -1.000000000000000000, 0.000000000000000000, 0.000000000000000000 ) ) ;
#10275=ORIENTED_EDGE ( 'NONE', *, *, #4216, .F. ) ;
#10276=ORIENTED_EDGE ( 'NONE', *, *, #11923, .F. ) ;
#10277=CYLINDRICAL_SURFACE ( 'NONE', #11165, 22.99899999999999878 ) ;
#10278=VERTEX_POINT ( 'NONE', #9785 ) ;
#10279=VERTEX_POINT ( 'NONE', #1406 ) ;
#10280=CARTESIAN_POINT ( 'NONE',  ( 0.000000000000000000, 17.71842311621530186, 17.35216073792446423 ) ) ;
#10281=EDGE_CURVE ( 'NONE', #9071, #4609, #5546, .T. ) ;
#10282=DIRECTION ( 'NONE',  ( -1.000000000000000000, 0.000000000000000000, 0.000000000000000000 ) ) ;
#10284=ORIENTED_EDGE ( 'NONE', *, *, #2854, .T. ) ;
#10285=DIRECTION ( 'NONE',  ( 0.000000000000000000, 1.000000000000000000, 3.614007241618348376E-15 ) ) ;
#10286=CARTESIAN_POINT ( 'NONE',  ( 3.000000000000000888, -2.745295967526151237, 22.83456483164687967 ) ) ;
#10288=CARTESIAN_POINT ( 'NONE',  ( 0.000000000000000000, -20.86861857134741172, 9.667200211209745930 ) ) ;
#10289=EDGE_CURVE ( 'NONE', #962, #6987, #656, .T. ) ;
#10290=DIRECTION ( 'NONE',  ( -1.000000000000000000, 0.000000000000000000, -0.000000000000000000 ) ) ;
#10292=AXIS2_PLACEMENT_3D ( 'NONE', #5136, #1283, #3186 ) ;
#10293=ORIENTED_EDGE ( 'NONE', *, *, #7322, .F. ) ;
#10294=CARTESIAN_POINT ( 'NONE',  ( 3.000000000000000888, 0.000000000000000000, 0.000000000000000000 ) ) ;
#10295=ORIENTED_EDGE ( 'NONE', *, *, #11615, .F. ) ;
#10297=DIRECTION ( 'NONE',  ( -1.000000000000000000, 0.000000000000000000, 0.000000000000000000 ) ) ;
#10299=DIRECTION ( 'NONE',  ( -1.000000000000000000, 0.000000000000000000, 0.000000000000000000 ) ) ;
#10300=CARTESIAN_POINT ( 'NONE',  ( 3.000000000000000888, 19.29833442572359559, 11.67026512804553562 ) ) ;
#10303=CARTESIAN_POINT ( 'NONE',  ( 3.000000000000000888, 0.000000000000000000, 0.000000000000000000 ) ) ;
#10306=ORIENTED_EDGE ( 'NONE', *, *, #3248, .F. ) ;
#10307=AXIS2_PLACEMENT_3D ( 'NONE', #6446, #6268, #2473 ) ;
#10308=CARTESIAN_POINT ( 'NONE',  ( 3.000000000000000888, 24.75110766671654261, -1.556492618230388425 ) ) ;
#10313=ADVANCED_FACE ( 'NONE', ( #10947, #2568 ), #8935, .F. ) ;
#10314=CIRCLE ( 'NONE', #4656, 24.80000000000000071 ) ;
#10315=LINE ( 'NONE', #8496, #9403 ) ;
#10316=VERTEX_POINT ( 'NONE', #3433 ) ;
#10318=EDGE_LOOP ( 'NONE', ( #7506, #4005, #3123, #8667 ) ) ;
#10319=EDGE_CURVE ( 'NONE', #11133, #6834, #3402, .T. ) ;
#10320=EDGE_LOOP ( 'NONE', ( #6344, #324, #4046, #11841 ) ) ;
#10321=DIRECTION ( 'NONE',  ( -1.000000000000000000, 0.000000000000000000, 0.000000000000000000 ) ) ;
#10323=CARTESIAN_POINT ( 'NONE',  ( 3.000000000000000888, -4.445336973060693531, -22.56530478845653676 ) ) ;
#10325=FACE_OUTER_BOUND ( 'NONE', #5419, .T. ) ;
#10327=CIRCLE ( 'NONE', #4665, 24.80000000000000071 ) ;
#10328=DIRECTION ( 'NONE',  ( -1.000000000000000000, -0.000000000000000000, -0.000000000000000000 ) ) ;
#10330=DIRECTION ( 'NONE',  ( -1.000000000000000000, 0.000000000000000000, 0.000000000000000000 ) ) ;
#10331=DIRECTION ( 'NONE',  ( 0.000000000000000000, -0.9135454576426046414, 0.4067366430757920481 ) ) ;
#10332=AXIS2_PLACEMENT_3D ( 'NONE', #11385, #6723, #5815 ) ;
#10333=VERTEX_POINT ( 'NONE', #5324 ) ;
#10334=ORIENTED_EDGE ( 'NONE', *, *, #8904, .T. ) ;
#10338=DIRECTION ( 'NONE',  ( -1.000000000000000000, -0.000000000000000000, -0.000000000000000000 ) ) ;
#10339=ORIENTED_EDGE ( 'NONE', *, *, #207, .T. ) ;
#10340=AXIS2_PLACEMENT_3D ( 'NONE', #2376, #9849, #10123 ) ;
#10341=LINE ( 'NONE', #7527, #9246 ) ;
#10342=ADVANCED_FACE ( 'NONE', ( #2381 ), #1523, .T. ) ;
#10343=DIRECTION ( 'NONE',  ( -1.000000000000000000, 0.000000000000000000, -0.000000000000000000 ) ) ;
#10346=EDGE_CURVE ( 'NONE', #9959, #5148, #8281, .T. ) ;
#10347=DIRECTION ( 'NONE',  ( 1.000000000000000000, 0.000000000000000000, 0.000000000000000000 ) ) ;
#10348=VERTEX_POINT ( 'NONE', #11803 ) ;
#10349=VERTEX_POINT ( 'NONE', #8133 ) ;
#10350=CYLINDRICAL_SURFACE ( 'NONE', #9396, 24.80000000000000071 ) ;
#10351=VERTEX_POINT ( 'NONE', #10833 ) ;
#10353=CARTESIAN_POINT ( 'NONE',  ( 0.000000000000000000, 0.000000000000000000, 0.000000000000000000 ) ) ;
#10356=DIRECTION ( 'NONE',  ( 1.000000000000000000, -0.000000000000000000, -0.000000000000000000 ) ) ;
#10357=DIRECTION ( 'NONE',  ( 0.000000000000000000, 0.000000000000000000, 1.000000000000000000 ) ) ;
#10358=CARTESIAN_POINT ( 'NONE',  ( 0.000000000000000000, 21.14796121233196402, 9.039786367038912474 ) ) ;
#10359=AXIS2_PLACEMENT_3D ( 'NONE', #6629, #11234, #1012 ) ;
#10360=CARTESIAN_POINT ( 'NONE',  ( 0.000000000000000000, 13.79477846460795831, 18.40266524480593802 ) ) ;
#10361=LINE ( 'NONE', #4560, #11977 ) ;
#10362=CIRCLE ( 'NONE', #4888, 24.80000000000000071 ) ;
#10363=CARTESIAN_POINT ( 'NONE',  ( 3.000000000000000888, 17.97274125076092233, -13.62355943574001671 ) ) ;
#10364=DIRECTION ( 'NONE',  ( -1.000000000000000000, -0.000000000000000000, 0.000000000000000000 ) ) ;
#10365=ORIENTED_EDGE ( 'NONE', *, *, #3856, .T. ) ;
#10366=CARTESIAN_POINT ( 'NONE',  ( -10.00000000000000000, 0.000000000000000000, 0.000000000000000000 ) ) ;
#10367=VERTEX_POINT ( 'NONE', #4277 ) ;
#10368=CIRCLE ( 'NONE', #8219, 22.99900000000000233 ) ;
#10369=CARTESIAN_POINT ( 'NONE',  ( 3.000000000000000888, 0.000000000000000000, 0.000000000000000000 ) ) ;
#10370=CIRCLE ( 'NONE', #10958, 24.80000000000000071 ) ;
#10372=CIRCLE ( 'NONE', #1382, 9.599999999999997868 ) ;
#10373=CARTESIAN_POINT ( 'NONE',  ( 0.000000000000000000, 24.45282072769601101, 4.135161237383664812 ) ) ;
#10376=AXIS2_PLACEMENT_3D ( 'NONE', #10166, #9183, #2704 ) ;
#10377=CARTESIAN_POINT ( 'NONE',  ( 3.000000000000000888, 6.668524164681944200, -23.88662356770108985 ) ) ;
#10378=CIRCLE ( 'NONE', #602, 22.99899999999999523 ) ;
#10379=ORIENTED_EDGE ( 'NONE', *, *, #10888, .T. ) ;
#10380=CIRCLE ( 'NONE', #4910, 9.599999999999997868 ) ;
#10381=ORIENTED_EDGE ( 'NONE', *, *, #6912, .T. ) ;
#10382=EDGE_LOOP ( 'NONE', ( #4941, #1417, #3290, #2999 ) ) ;
#10383=CARTESIAN_POINT ( 'NONE',  ( 1.499999999999999556, -6.168200451485919444, 24.02068490260611000 ) ) ;
#10384=CARTESIAN_POINT ( 'NONE',  ( 3.000000000000000000, 2.449293598294706119E-15, -19.99999999999999645 ) ) ;
#10385=VECTOR ( 'NONE', #8959, 1000.000000000000000 ) ;
#10387=CARTESIAN_POINT ( 'NONE',  ( 3.000000000000000888, -7.402892494506437160, 21.30300407174360444 ) ) ;
#10388=CYLINDRICAL_SURFACE ( 'NONE', #10516, 9.599999999999997868 ) ;
#10389=ORIENTED_EDGE ( 'NONE', *, *, #8239, .T. ) ;
#10390=CARTESIAN_POINT ( 'NONE',  ( 0.000000000000000000, 0.000000000000000000, 0.000000000000000000 ) ) ;
#10391=EDGE_CURVE ( 'NONE', #10167, #10826, #2223, .T. ) ;
#10393=EDGE_CURVE ( 'NONE', #7927, #10972, #2813, .T. ) ;
#10394=EDGE_CURVE ( 'NONE', #532, #3460, #9056, .T. ) ;
#10395=AXIS2_PLACEMENT_3D ( 'NONE', #7669, #2224, #4983 ) ;
#10397=VERTEX_POINT ( 'NONE', #6305 ) ;
#10398=AXIS2_PLACEMENT_3D ( 'NONE', #7949, #2204, #7766 ) ;
#10401=ORIENTED_EDGE ( 'NONE', *, *, #5873, .F. ) ;
#10403=CARTESIAN_POINT ( 'NONE',  ( 1.500000000000000444, -20.93895013827572171, -13.28910708463150492 ) ) ;
#10404=ORIENTED_EDGE ( 'NONE', *, *, #11783, .F. ) ;
#10405=ADVANCED_FACE ( 'NONE', ( #11743 ), #8073, .T. ) ;
#10406=CARTESIAN_POINT ( 'NONE',  ( 3.000000000000000888, 18.40266524480607657, -13.79477846460777357 ) ) ;
#10408=DIRECTION ( 'NONE',  ( 0.000000000000000000, 0.9510565162951521989, 0.3090169943749515036 ) ) ;
#10410=FACE_OUTER_BOUND ( 'NONE', #5749, .T. ) ;
#10411=FACE_OUTER_BOUND ( 'NONE', #2210, .T. ) ;
#10412=ORIENTED_EDGE ( 'NONE', *, *, #6395, .T. ) ;
#10413=ORIENTED_EDGE ( 'NONE', *, *, #1938, .T. ) ;
#10414=CARTESIAN_POINT ( 'NONE',  ( 3.000000000000000888, -2.811977935937933104, 22.37663021667342989 ) ) ;
#10415=ORIENTED_EDGE ( 'NONE', *, *, #4499, .T. ) ;
#10416=CIRCLE ( 'NONE', #56, 9.599999999999997868 ) ;
#10417=EDGE_CURVE ( 'NONE', #8297, #9994, #6708, .T. ) ;
#10419=CARTESIAN_POINT ( 'NONE',  ( 3.000000000000000888, 0.000000000000000000, 0.000000000000000000 ) ) ;
#10421=ADVANCED_FACE ( 'NONE', ( #9165 ), #6182, .T. ) ;
#10422=CARTESIAN_POINT ( 'NONE',  ( 3.000000000000000888, 0.3433949777334901476, -22.99643626497956461 ) ) ;
#10423=CARTESIAN_POINT ( 'NONE',  ( 3.000000000000000888, 0.000000000000000000, 0.000000000000000000 ) ) ;
#10425=CIRCLE ( 'NONE', #4370, 9.599999999999997868 ) ;
#10426=DIRECTION ( 'NONE',  ( 0.000000000000000000, -0.6691306063588494668, -0.7431448254774021267 ) ) ;
#10428=CARTESIAN_POINT ( 'NONE',  ( 3.000000000000000000, 0.000000000000000000, 0.000000000000000000 ) ) ;
#10430=CARTESIAN_POINT ( 'NONE',  ( 0.000000000000000000, 0.000000000000000000, 0.000000000000000000 ) ) ;
#10431=EDGE_LOOP ( 'NONE', ( #6683, #4539, #7189, #3275 ) ) ;
#10432=ORIENTED_EDGE ( 'NONE', *, *, #11513, .T. ) ;
#10433=CIRCLE ( 'NONE', #863, 9.599999999999996092 ) ;
#10434=CARTESIAN_POINT ( 'NONE',  ( 0.000000000000000000, 0.000000000000000000, 0.000000000000000000 ) ) ;
#10436=EDGE_CURVE ( 'NONE', #8511, #11900, #10425, .T. ) ;
#10437=LINE ( 'NONE', #11420, #6592 ) ;
#10441=CARTESIAN_POINT ( 'NONE',  ( 3.000000000000000888, 17.31945870441147406, 15.13242714128125499 ) ) ;
#10442=ORIENTED_EDGE ( 'NONE', *, *, #11685, .T. ) ;
#10443=EDGE_CURVE ( 'NONE', #2754, #3254, #1435, .T. ) ;
#10444=ORIENTED_EDGE ( 'NONE', *, *, #6624, .T. ) ;
#10445=DIRECTION ( 'NONE',  ( -1.000000000000000000, 0.000000000000000000, -0.000000000000000000 ) ) ;
#10447=ORIENTED_EDGE ( 'NONE', *, *, #3771, .F. ) ;
#10448=CIRCLE ( 'NONE', #11429, 22.99899999999999523 ) ;
#10449=CARTESIAN_POINT ( 'NONE',  ( 3.000000000000000888, 0.000000000000000000, 0.000000000000000000 ) ) ;
#10451=DIRECTION ( 'NONE',  ( 0.000000000000000000, -0.9945218953682744001, 0.1045284632676436593 ) ) ;
#10453=DIRECTION ( 'NONE',  ( 0.000000000000000000, 0.000000000000000000, 1.000000000000000000 ) ) ;
#10454=ORIENTED_EDGE ( 'NONE', *, *, #303, .F. ) ;
#10455=ORIENTED_EDGE ( 'NONE', *, *, #8682, .T. ) ;
#10457=DIRECTION ( 'NONE',  ( -1.000000000000000000, -0.000000000000000000, 0.000000000000000000 ) ) ;
#10458=VERTEX_POINT ( 'NONE', #5682 ) ;
#10459=DIRECTION ( 'NONE',  ( 0.000000000000000000, 0.000000000000000000, 1.000000000000000000 ) ) ;
#10461=DIRECTION ( 'NONE',  ( 0.000000000000000000, 0.7431448254773910245, 0.6691306063588619013 ) ) ;
#10462=ORIENTED_EDGE ( 'NONE', *, *, #1670, .T. ) ;
#10465=CYLINDRICAL_SURFACE ( 'NONE', #5518, 9.599999999999997868 ) ;
#10467=EDGE_CURVE ( 'NONE', #2284, #6367, #9415, .T. ) ;
#10469=ORIENTED_EDGE ( 'NONE', *, *, #6642, .F. ) ;
#10470=CARTESIAN_POINT ( 'NONE',  ( 8.000000000000000000, 0.000000000000000000, 0.000000000000000000 ) ) ;
#10471=VERTEX_POINT ( 'NONE', #9235 ) ;
#10472=ORIENTED_EDGE ( 'NONE', *, *, #7854, .F. ) ;
#10474=ORIENTED_EDGE ( 'NONE', *, *, #4409, .T. ) ;
#10475=EDGE_CURVE ( 'NONE', #1430, #10068, #3794, .T. ) ;
#10476=CIRCLE ( 'NONE', #5200, 22.99900000000000233 ) ;
#10478=EDGE_CURVE ( 'NONE', #9193, #1445, #3006, .T. ) ;
#10479=CYLINDRICAL_SURFACE ( 'NONE', #502, 9.599999999999997868 ) ;
#10480=ADVANCED_FACE ( 'NONE', ( #9295 ), #1829, .T. ) ;
#10481=CYLINDRICAL_SURFACE ( 'NONE', #11674, 22.99899999999999878 ) ;
#10482=CARTESIAN_POINT ( 'NONE',  ( 3.000000000000000888, 22.90635393027949007, -2.062268319295327057 ) ) ;
#10484=CIRCLE ( 'NONE', #5208, 24.80000000000000071 ) ;
#10485=CARTESIAN_POINT ( 'NONE',  ( 3.000000000000000888, -21.14796121233203152, 9.039786367038763260 ) ) ;
#10487=DIRECTION ( 'NONE',  ( -0.000000000000000000, 0.000000000000000000, 1.000000000000000000 ) ) ;
#10488=EDGE_LOOP ( 'NONE', ( #12080, #1085, #7147, #6659 ) ) ;
#10489=DIRECTION ( 'NONE',  ( 0.000000000000000000, 0.000000000000000000, -1.000000000000000000 ) ) ;
#10491=ORIENTED_EDGE ( 'NONE', *, *, #7139, .T. ) ;
#10492=VERTEX_POINT ( 'NONE', #6476 ) ;
#10493=CARTESIAN_POINT ( 'NONE',  ( 0.000000000000000000, 22.54798042742718067, -0.4575788569252652871 ) ) ;
#10495=DIRECTION ( 'NONE',  ( -1.000000000000000000, 0.000000000000000000, 0.000000000000000000 ) ) ;
#10498=CARTESIAN_POINT ( 'NONE',  ( 0.000000000000000000, 9.039786367039127413, -21.14796121233187520 ) ) ;
#10499=EDGE_LOOP ( 'NONE', ( #6045, #3867 ) ) ;
#10500=ADVANCED_FACE ( 'NONE', ( #11982 ), #6651, .T. ) ;
#10501=ORIENTED_EDGE ( 'NONE', *, *, #7199, .F. ) ;
#10502=LINE ( 'NONE', #11484, #1806 ) ;
#10503=DIRECTION ( 'NONE',  ( -1.000000000000000000, 0.000000000000000000, 0.000000000000000000 ) ) ;
#10505=CARTESIAN_POINT ( 'NONE',  ( 0.000000000000000000, 0.000000000000000000, 0.000000000000000000 ) ) ;
#10506=CARTESIAN_POINT ( 'NONE',  ( 0.000000000000000000, -2.062268319295407881, -22.90635393027948297 ) ) ;
#10507=EDGE_CURVE ( 'NONE', #9240, #2984, #10233, .T. ) ;
#10508=CIRCLE ( 'NONE', #1719, 22.99899999999999878 ) ;
#10510=DIRECTION ( 'NONE',  ( -1.000000000000000000, 0.000000000000000000, 0.000000000000000000 ) ) ;
#10511=ORIENTED_EDGE ( 'NONE', *, *, #7857, .T. ) ;
#10514=CARTESIAN_POINT ( 'NONE',  ( 3.000000000000000888, -23.05871956130128808, 9.128825345752948905 ) ) ;
#10515=ORIENTED_EDGE ( 'NONE', *, *, #7057, .F. ) ;
#10516=AXIS2_PLACEMENT_3D ( 'NONE', #5564, #9294, #4705 ) ;
#10517=VECTOR ( 'NONE', #3345, 1000.000000000000000 ) ;
#10518=DIRECTION ( 'NONE',  ( 0.000000000000000000, -0.8090169943749526693, 0.5877852522924660317 ) ) ;
#10520=DIRECTION ( 'NONE',  ( -1.000000000000000000, 0.000000000000000000, 0.000000000000000000 ) ) ;
#10521=ORIENTED_EDGE ( 'NONE', *, *, #4034, .F. ) ;
#10522=CYLINDRICAL_SURFACE ( 'NONE', #11209, 9.599999999999997868 ) ;
#10523=DIRECTION ( 'NONE',  ( -1.000000000000000000, 0.000000000000000000, -0.000000000000000000 ) ) ;
#10525=AXIS2_PLACEMENT_3D ( 'NONE', #10818, #3475, #11905 ) ;
#10526=AXIS2_PLACEMENT_3D ( 'NONE', #10998, #2730, #4571 ) ;
#10527=CARTESIAN_POINT ( 'NONE',  ( -10.00000000000000000, 0.000000000000000000, 0.000000000000000000 ) ) ;
#10528=ORIENTED_EDGE ( 'NONE', *, *, #5158, .T. ) ;
#10531=CARTESIAN_POINT ( 'NONE',  ( 0.000000000000000000, 20.78471918669860941, 8.753070780933226658 ) ) ;
#10532=ORIENTED_EDGE ( 'NONE', *, *, #7395, .T. ) ;
#10534=CIRCLE ( 'NONE', #2925, 9.599999999999997868 ) ;
#10537=CARTESIAN_POINT ( 'NONE',  ( 3.000000000000000888, -9.667200211209685534, -20.86861857134744014 ) ) ;
#10540=DIRECTION ( 'NONE',  ( -1.000000000000000000, -0.000000000000000000, -0.000000000000000000 ) ) ;
#10541=CARTESIAN_POINT ( 'NONE',  ( 3.000000000000000888, 15.13242714128143440, -17.31945870441131419 ) ) ;
#10542=ADVANCED_FACE ( 'NONE', ( #3610 ), #3661, .T. ) ;
#10544=DIRECTION ( 'NONE',  ( -1.000000000000000000, -0.000000000000000000, 0.000000000000000000 ) ) ;
#10545=ADVANCED_FACE ( 'NONE', ( #7319 ), #855, .T. ) ;
#10546=DIRECTION ( 'NONE',  ( -1.000000000000000000, -0.000000000000000000, -0.000000000000000000 ) ) ;
#10547=CIRCLE ( 'NONE', #9958, 9.599999999999996092 ) ;
#10548=ORIENTED_EDGE ( 'NONE', *, *, #6147, .T. ) ;
#10549=ORIENTED_EDGE ( 'NONE', *, *, #866, .T. ) ;
#10550=CARTESIAN_POINT ( 'NONE',  ( -10.00000000000000000, 0.000000000000000000, 0.000000000000000000 ) ) ;
#10552=CARTESIAN_POINT ( 'NONE',  ( 0.000000000000000000, -21.30300407174357957, -7.402892494506506438 ) ) ;
#10553=AXIS2_PLACEMENT_3D ( 'NONE', #5041, #11591, #10610 ) ;
#10555=EDGE_CURVE ( 'NONE', #2310, #348, #5941, .T. ) ;
#10557=CARTESIAN_POINT ( 'NONE',  ( 0.000000000000000000, -9.667200211209964422, 20.86861857134731579 ) ) ;
#10558=FACE_OUTER_BOUND ( 'NONE', #10057, .T. ) ;
#10559=ORIENTED_EDGE ( 'NONE', *, *, #4598, .T. ) ;
#10560=AXIS2_PLACEMENT_3D ( 'NONE', #10428, #3207, #10487 ) ;
#10562=ORIENTED_EDGE ( 'NONE', *, *, #4868, .F. ) ;
#10563=CYLINDRICAL_SURFACE ( 'NONE', #10210, 22.99899999999999878 ) ;
#10564=EDGE_CURVE ( 'NONE', #5933, #2253, #9841, .T. ) ;
#10568=CARTESIAN_POINT ( 'NONE',  ( -10.00000000000000000, 0.000000000000000000, 0.000000000000000000 ) ) ;
#10569=DIRECTION ( 'NONE',  ( 0.000000000000000000, 0.000000000000000000, -1.000000000000000000 ) ) ;
#10570=CIRCLE ( 'NONE', #3340, 9.599999999999997868 ) ;
#10571=EDGE_CURVE ( 'NONE', #3166, #4944, #1250, .T. ) ;
#10572=VECTOR ( 'NONE', #5311, 1000.000000000000000 ) ;
#10573=VECTOR ( 'NONE', #9794, 1000.000000000000000 ) ;
#10577=ORIENTED_EDGE ( 'NONE', *, *, #5481, .F. ) ;
#10581=EDGE_CURVE ( 'NONE', #3718, #7675, #10035, .T. ) ;
#10582=CIRCLE ( 'NONE', #7846, 9.599999999999999645 ) ;
#10583=ORIENTED_EDGE ( 'NONE', *, *, #11138, .T. ) ;
#10584=CARTESIAN_POINT ( 'NONE',  ( 0.000000000000000000, -17.35216073792428304, -17.71842311621547950 ) ) ;
#10585=DIRECTION ( 'NONE',  ( 0.000000000000000000, 0.000000000000000000, 1.000000000000000000 ) ) ;
#10587=CIRCLE ( 'NONE', #807, 24.80000000000000071 ) ;
#10588=LINE ( 'NONE', #2379, #3646 ) ;
#10589=ORIENTED_EDGE ( 'NONE', *, *, #11003, .F. ) ;
#10590=DIRECTION ( 'NONE',  ( 0.000000000000000000, -1.000000000000000000, -1.047444401652940007E-14 ) ) ;
#10591=DIRECTION ( 'NONE',  ( -1.000000000000000000, -0.000000000000000000, -0.000000000000000000 ) ) ;
#10593=VECTOR ( 'NONE', #627, 1000.000000000000000 ) ;
#10595=VECTOR ( 'NONE', #6186, 1000.000000000000000 ) ;
#10596=CARTESIAN_POINT ( 'NONE',  ( 3.000000000000000888, -21.76479567747236743, -7.432877647175426539 ) ) ;
#10597=CARTESIAN_POINT ( 'NONE',  ( 3.000000000000000888, 4.445336973061170482, -22.56530478845644794 ) ) ;
#10598=EDGE_CURVE ( 'NONE', #5600, #7059, #7451, .T. ) ;
#10599=ORIENTED_EDGE ( 'NONE', *, *, #3161, .F. ) ;
#10601=CIRCLE ( 'NONE', #631, 9.599999999999996092 ) ;
#10602=VECTOR ( 'NONE', #4662, 1000.000000000000000 ) ;
#10603=DIRECTION ( 'NONE',  ( -1.000000000000000000, -0.000000000000000000, -0.000000000000000000 ) ) ;
#10604=CARTESIAN_POINT ( 'NONE',  ( 0.000000000000000000, 6.668524164681944200, -23.88662356770108630 ) ) ;
#10607=DIRECTION ( 'NONE',  ( 1.000000000000000000, 0.000000000000000000, -0.000000000000000000 ) ) ;
#10608=CARTESIAN_POINT ( 'NONE',  ( 0.000000000000000000, -20.65684170206481696, -13.72351598154918406 ) ) ;
#10609=AXIS2_PLACEMENT_3D ( 'NONE', #7500, #92, #9284 ) ;
#10610=DIRECTION ( 'NONE',  ( 0.000000000000000000, 0.000000000000000000, 1.000000000000000000 ) ) ;
#10612=CIRCLE ( 'NONE', #9251, 9.599999999999997868 ) ;
#10613=EDGE_LOOP ( 'NONE', ( #7521, #9241, #9590, #9674 ) ) ;
#10614=ORIENTED_EDGE ( 'NONE', *, *, #12045, .T. ) ;
#10617=AXIS2_PLACEMENT_3D ( 'NONE', #9670, #241, #3239 ) ;
#10618=DIRECTION ( 'NONE',  ( -1.000000000000000000, -0.000000000000000000, -0.000000000000000000 ) ) ;
#10619=EDGE_CURVE ( 'NONE', #2975, #7896, #6336, .T. ) ;
#10620=DIRECTION ( 'NONE',  ( -1.000000000000000000, 0.000000000000000000, 0.000000000000000000 ) ) ;
#10622=CIRCLE ( 'NONE', #11976, 22.99899999999999878 ) ;
#10623=AXIS2_PLACEMENT_3D ( 'NONE', #1899, #2018, #55 ) ;
#10625=DIRECTION ( 'NONE',  ( 0.000000000000000000, 0.5877852522924690293, 0.8090169943749505599 ) ) ;
#10626=DIRECTION ( 'NONE',  ( 0.000000000000000000, -0.4067366430758070917, 0.9135454576425978690 ) ) ;
#10627=ORIENTED_EDGE ( 'NONE', *, *, #8507, .F. ) ;
#10628=ORIENTED_EDGE ( 'NONE', *, *, #5798, .F. ) ;
#10629=AXIS2_PLACEMENT_3D ( 'NONE', #7381, #11125, #104 ) ;
#10630=ORIENTED_EDGE ( 'NONE', *, *, #11892, .T. ) ;
#10632=DIRECTION ( 'NONE',  ( 0.000000000000000000, 0.6691306063588543518, 0.7431448254773976858 ) ) ;
#10634=ADVANCED_FACE ( 'NONE', ( #11652 ), #7919, .T. ) ;
#10635=DIRECTION ( 'NONE',  ( -1.000000000000000000, 0.000000000000000000, -0.000000000000000000 ) ) ;
#10636=DIRECTION ( 'NONE',  ( 1.000000000000000000, 0.000000000000000000, -0.000000000000000000 ) ) ;
#10637=CIRCLE ( 'NONE', #4776, 9.599999999999997868 ) ;
#10639=CARTESIAN_POINT ( 'NONE',  ( 3.000000000000000888, -22.99643626497957172, 0.3433949777330864706 ) ) ;
#10640=VERTEX_POINT ( 'NONE', #3404 ) ;
#10641=ORIENTED_EDGE ( 'NONE', *, *, #8582, .F. ) ;
#10644=EDGE_LOOP ( 'NONE', ( #4843, #9555, #9704, #11396 ) ) ;
#10645=AXIS2_PLACEMENT_3D ( 'NONE', #11029, #7097, #7338 ) ;
#10646=DIRECTION ( 'NONE',  ( -1.000000000000000000, 0.000000000000000000, 0.000000000000000000 ) ) ;
#10647=CYLINDRICAL_SURFACE ( 'NONE', #1242, 9.599999999999997868 ) ;
#10650=ORIENTED_EDGE ( 'NONE', *, *, #2406, .F. ) ;
#10651=DIRECTION ( 'NONE',  ( -1.000000000000000000, -0.000000000000000000, 0.000000000000000000 ) ) ;
#10652=DIRECTION ( 'NONE',  ( -1.000000000000000000, 0.000000000000000000, 0.000000000000000000 ) ) ;
#10655=DIRECTION ( 'NONE',  ( -1.000000000000000000, 0.000000000000000000, -0.000000000000000000 ) ) ;
#10656=VERTEX_POINT ( 'NONE', #3215 ) ;
#10657=CARTESIAN_POINT ( 'NONE',  ( -10.00000000000000000, 0.000000000000000000, 0.000000000000000000 ) ) ;
#10658=EDGE_LOOP ( 'NONE', ( #1019, #8488, #667, #947 ) ) ;
#10661=DIRECTION ( 'NONE',  ( 0.000000000000000000, 0.6691306063588544628, 0.7431448254773976858 ) ) ;
#10662=AXIS2_PLACEMENT_3D ( 'NONE', #7288, #5355, #6265 ) ;
#10666=DIRECTION ( 'NONE',  ( 0.000000000000000000, 0.000000000000000000, 1.000000000000000000 ) ) ;
#10668=CARTESIAN_POINT ( 'NONE',  ( 3.000000000000000888, 20.86861857134747922, -9.667200211209612704 ) ) ;
#10670=CARTESIAN_POINT ( 'NONE',  ( 0.000000000000000000, 15.40502424595170972, -19.43515443678387555 ) ) ;
#10671=CIRCLE ( 'NONE', #8915, 9.599999999999997868 ) ;
#10672=ORIENTED_EDGE ( 'NONE', *, *, #1791, .T. ) ;
#10673=FACE_OUTER_BOUND ( 'NONE', #4626, .T. ) ;
#10674=ORIENTED_EDGE ( 'NONE', *, *, #9546, .F. ) ;
#10675=CARTESIAN_POINT ( 'NONE',  ( 3.000000000000000888, 0.000000000000000000, 0.000000000000000000 ) ) ;
#10676=CARTESIAN_POINT ( 'NONE',  ( 8.000000000000000000, 2.449293598294706119E-15, -19.99999999999999645 ) ) ;
#10677=VECTOR ( 'NONE', #11622, 1000.000000000000000 ) ;
#10678=CARTESIAN_POINT ( 'NONE',  ( 3.000000000000000888, -15.13242714128131361, 17.31945870441142077 ) ) ;
#10681=CARTESIAN_POINT ( 'NONE',  ( 3.000000000000000888, -17.31945870441136748, -15.13242714128137401 ) ) ;
#10683=ORIENTED_EDGE ( 'NONE', *, *, #1124, .F. ) ;
#10684=VERTEX_POINT ( 'NONE', #3268 ) ;
#10687=CARTESIAN_POINT ( 'NONE',  ( 0.000000000000000000, 0.000000000000000000, 0.000000000000000000 ) ) ;
#10691=PRODUCT_DEFINITION ( 'UNKNOWN', '', #10756, #4521 ) ;
#10692=EDGE_CURVE ( 'NONE', #10684, #8706, #665, .T. ) ;
#10693=DIRECTION ( 'NONE',  ( 1.000000000000000000, 0.000000000000000000, 0.000000000000000000 ) ) ;
#10695=ORIENTED_EDGE ( 'NONE', *, *, #3454, .F. ) ;
#10698=EDGE_CURVE ( 'NONE', #8629, #6518, #6715, .T. ) ;
#10699=VERTEX_POINT ( 'NONE', #4824 ) ;
#10700=LINE ( 'NONE', #7707, #7978 ) ;
#10701=DIRECTION ( 'NONE',  ( 0.000000000000000000, -0.5877852522924630341, -0.8090169943749546677 ) ) ;
#10703=LINE ( 'NONE', #7015, #4627 ) ;
#10704=EDGE_LOOP ( 'NONE', ( #10882, #6098, #3571, #4218 ) ) ;
#10706=CARTESIAN_POINT ( 'NONE',  ( 3.000000000000000888, 0.000000000000000000, 0.000000000000000000 ) ) ;
#10708=ORIENTED_EDGE ( 'NONE', *, *, #11742, .F. ) ;
#10709=DIRECTION ( 'NONE',  ( -1.000000000000000000, -0.000000000000000000, -0.000000000000000000 ) ) ;
#10710=CIRCLE ( 'NONE', #1131, 22.99899999999999878 ) ;
#10711=ORIENTED_EDGE ( 'NONE', *, *, #7857, .F. ) ;
#10712=CARTESIAN_POINT ( 'NONE',  ( 1.500000000000000444, 11.48910920600683561, 21.97817939804043874 ) ) ;
#10713=VERTEX_POINT ( 'NONE', #10678 ) ;
#10715=EDGE_CURVE ( 'NONE', #5315, #5509, #3803, .T. ) ;
#10716=CARTESIAN_POINT ( 'NONE',  ( 3.000000000000000888, -22.90635393027947941, 2.062268319295487817 ) ) ;
#10719=LINE ( 'NONE', #3136, #2302 ) ;
#10723=ADVANCED_FACE ( 'NONE', ( #8960 ), #4307, .T. ) ;
#10724=LINE ( 'NONE', #8894, #10593 ) ;
#10726=DIRECTION ( 'NONE',  ( -1.000000000000000000, -0.000000000000000000, -0.000000000000000000 ) ) ;
#10727=ORIENTED_EDGE ( 'NONE', *, *, #9185, .T. ) ;
#10728=FACE_OUTER_BOUND ( 'NONE', #11426, .T. ) ;
#10729=VERTEX_POINT ( 'NONE', #6990 ) ;
#10730=AXIS2_PLACEMENT_3D ( 'NONE', #3184, #6955, #5014 ) ;
#10731=ADVANCED_FACE ( 'NONE', ( #6090 ), #5169, .T. ) ;
#10732=CYLINDRICAL_SURFACE ( 'NONE', #10662, 9.599999999999997868 ) ;
#10733=ORIENTED_EDGE ( 'NONE', *, *, #1429, .F. ) ;
#10734=DIRECTION ( 'NONE',  ( -1.000000000000000000, 0.000000000000000000, 0.000000000000000000 ) ) ;
#10735=DIRECTION ( 'NONE',  ( -1.000000000000000000, -0.000000000000000000, 0.000000000000000000 ) ) ;
#10737=AXIS2_PLACEMENT_3D ( 'NONE', #2625, #6358, #10080 ) ;
#10738=AXIS2_PLACEMENT_3D ( 'NONE', #2496, #7074, #7943 ) ;
#10740=DIRECTION ( 'NONE',  ( -1.000000000000000000, -0.000000000000000000, -0.000000000000000000 ) ) ;
#10741=CIRCLE ( 'NONE', #2928, 9.599999999999996092 ) ;
#10742=CARTESIAN_POINT ( 'NONE',  ( 3.000000000000000888, 0.000000000000000000, 0.000000000000000000 ) ) ;
#10743=ORIENTED_EDGE ( 'NONE', *, *, #9585, .T. ) ;
#10744=VERTEX_POINT ( 'NONE', #5105 ) ;
#10745=AXIS2_PLACEMENT_3D ( 'NONE', #4766, #8557, #2926 ) ;
#10746=CARTESIAN_POINT ( 'NONE',  ( 0.000000000000000000, 2.062268319295562424, 22.90635393027947231 ) ) ;
#10747=DIRECTION ( 'NONE',  ( 0.000000000000000000, 0.000000000000000000, 1.000000000000000000 ) ) ;
#10748=CARTESIAN_POINT ( 'NONE',  ( 3.000000000000000888, -14.74749645579999857, -17.06259499759959297 ) ) ;
#10750=AXIS2_PLACEMENT_3D ( 'NONE', #5785, #4803, #11411 ) ;
#10751=DIRECTION ( 'NONE',  ( -1.000000000000000000, -0.000000000000000000, -0.000000000000000000 ) ) ;
#10752=VECTOR ( 'NONE', #6854, 1000.000000000000000 ) ;
#10753=CARTESIAN_POINT ( 'NONE',  ( 3.000000000000000888, -6.779701584702581663, -21.97702544527764701 ) ) ;
#10754=EDGE_LOOP ( 'NONE', ( #616, #1837, #4763, #3806 ) ) ;
#10755=ORIENTED_EDGE ( 'NONE', *, *, #4345, .F. ) ;
#10756=PRODUCT_DEFINITION_FORMATION_WITH_SPECIFIED_SOURCE ( 'ANY', '', #8642, .NOT_KNOWN. ) ;
#10758=ORIENTED_EDGE ( 'NONE', *, *, #3689, .F. ) ;
#10759=DIRECTION ( 'NONE',  ( 0.000000000000000000, 0.000000000000000000, 1.000000000000000000 ) ) ;
#10761=DIRECTION ( 'NONE',  ( -1.000000000000000000, -0.000000000000000000, 0.000000000000000000 ) ) ;
#10762=EDGE_LOOP ( 'NONE', ( #1379, #10641, #8957, #5444 ) ) ;
#10763=EDGE_CURVE ( 'NONE', #9620, #11676, #11709, .T. ) ;
#10764=CIRCLE ( 'NONE', #3737, 9.599999999999997868 ) ;
#10765=AXIS2_PLACEMENT_3D ( 'NONE', #7509, #5618, #42 ) ;
#10766=DIRECTION ( 'NONE',  ( 0.000000000000000000, 0.000000000000000000, 1.000000000000000000 ) ) ;
#10767=EDGE_CURVE ( 'NONE', #5179, #6658, #268, .T. ) ;
#10768=EDGE_CURVE ( 'NONE', #7721, #9363, #8286, .T. ) ;
#10769=CARTESIAN_POINT ( 'NONE',  ( 3.000000000000000888, -22.56530478845645860, -4.445336973061090546 ) ) ;
#10771=ORIENTED_EDGE ( 'NONE', *, *, #596, .F. ) ;
#10772=DIRECTION ( 'NONE',  ( 0.000000000000000000, -0.2079116908177466583, -0.9781476007338082423 ) ) ;
#10773=CIRCLE ( 'NONE', #3734, 24.80000000000000071 ) ;
#10774=ORIENTED_EDGE ( 'NONE', *, *, #10785, .T. ) ;
#10775=LINE ( 'NONE', #3304, #11938 ) ;
#10776=CIRCLE ( 'NONE', #5895, 9.599999999999996092 ) ;
#10777=ORIENTED_EDGE ( 'NONE', *, *, #9833, .F. ) ;
#10778=VECTOR ( 'NONE', #1517, 1000.000000000000000 ) ;
#10780=EDGE_CURVE ( 'NONE', #5379, #8825, #9534, .T. ) ;
#10782=CARTESIAN_POINT ( 'NONE',  ( 3.000000000000000888, 22.90635393027946165, 2.062268319295641472 ) ) ;
#10784=ORIENTED_EDGE ( 'NONE', *, *, #2571, .F. ) ;
#10785=EDGE_CURVE ( 'NONE', #6248, #2893, #224, .T. ) ;
#10786=AXIS2_PLACEMENT_3D ( 'NONE', #6496, #1850, #931 ) ;
#10787=DIRECTION ( 'NONE',  ( 0.000000000000000000, 0.000000000000000000, 1.000000000000000000 ) ) ;
#10788=CYLINDRICAL_SURFACE ( 'NONE', #7511, 24.80000000000000071 ) ;
#10790=DIRECTION ( 'NONE',  ( 0.000000000000000000, -0.5000000000000072164, 0.8660254037844344888 ) ) ;
#10792=DIRECTION ( 'NONE',  ( -1.000000000000000000, -0.000000000000000000, 0.000000000000000000 ) ) ;
#10793=EDGE_CURVE ( 'NONE', #8912, #2073, #10433, .T. ) ;
#10794=VERTEX_POINT ( 'NONE', #4193 ) ;
#10795=CARTESIAN_POINT ( 'NONE',  ( 1.500000000000000444, 20.93895013827581408, 13.28910708463135215 ) ) ;
#10796=AXIS2_PLACEMENT_3D ( 'NONE', #5346, #3205, #6015 ) ;
#10797=VERTEX_POINT ( 'NONE', #3464 ) ;
#10798=AXIS2_PLACEMENT_3D ( 'NONE', #6552, #3808, #2084 ) ;
#10800=ORIENTED_EDGE ( 'NONE', *, *, #7005, .F. ) ;
#10801=CARTESIAN_POINT ( 'NONE',  ( 3.000000000000000888, 0.000000000000000000, 0.000000000000000000 ) ) ;
#10802=CARTESIAN_POINT ( 'NONE',  ( 0.000000000000000000, -17.97274125076083351, 13.62355943574013750 ) ) ;
#10803=DIRECTION ( 'NONE',  ( -1.000000000000000000, 0.000000000000000000, -0.000000000000000000 ) ) ;
#10805=CIRCLE ( 'NONE', #1416, 9.599999999999996092 ) ;
#10809=VERTEX_POINT ( 'NONE', #9088 ) ;
#10810=ORIENTED_EDGE ( 'NONE', *, *, #12105, .T. ) ;
#10811=ORIENTED_EDGE ( 'NONE', *, *, #6728, .T. ) ;
#10813=AXIS2_PLACEMENT_3D ( 'NONE', #2828, #8518, #3921 ) ;
#10816=CYLINDRICAL_SURFACE ( 'NONE', #3682, 24.80000000000000071 ) ;
#10817=CIRCLE ( 'NONE', #5542, 22.99899999999999523 ) ;
#10818=CARTESIAN_POINT ( 'NONE',  ( 8.000000000000000000, 0.000000000000000000, 0.000000000000000000 ) ) ;
#10819=EDGE_CURVE ( 'NONE', #5404, #10823, #3211, .T. ) ;
#10821=FACE_OUTER_BOUND ( 'NONE', #9300, .T. ) ;
#10822=CARTESIAN_POINT ( 'NONE',  ( 3.000000000000000888, -22.37663021667341923, -2.811977935938010376 ) ) ;
#10823=VERTEX_POINT ( 'NONE', #5413 ) ;
#10824=VERTEX_POINT ( 'NONE', #9199 ) ;
#10826=VERTEX_POINT ( 'NONE', #4557 ) ;
#10831=DIRECTION ( 'NONE',  ( 0.000000000000000000, 0.000000000000000000, 1.000000000000000000 ) ) ;
#10832=ORIENTED_EDGE ( 'NONE', *, *, #1917, .T. ) ;
#10833=CARTESIAN_POINT ( 'NONE',  ( 0.000000000000000000, 17.35216073792440739, 17.71842311621536226 ) ) ;
#10834=DIRECTION ( 'NONE',  ( 0.000000000000000000, 0.000000000000000000, 1.000000000000000000 ) ) ;
#10837=AXIS2_PLACEMENT_3D ( 'NONE', #8593, #190, #10 ) ;
#10838=CARTESIAN_POINT ( 'NONE',  ( 3.000000000000000888, -21.58580335785681115, 6.532525787310899723 ) ) ;
#10839=ORIENTED_EDGE ( 'NONE', *, *, #8948, .T. ) ;
#10840=EDGE_CURVE ( 'NONE', #7059, #1167, #7099, .T. ) ;
#10842=CARTESIAN_POINT ( 'NONE',  ( 0.000000000000000000, -8.645255683529166291, 23.24434456306322971 ) ) ;
#10843=DIRECTION ( 'NONE',  ( 0.000000000000000000, 0.1045284632676538872, -0.9945218953682732899 ) ) ;
#10844=EDGE_LOOP ( 'NONE', ( #8436, #5613, #4864, #1991 ) ) ;
#10845=AXIS2_PLACEMENT_3D ( 'NONE', #5637, #8396, #2829 ) ;
#10846=EDGE_CURVE ( 'NONE', #11972, #5818, #3017, .T. ) ;
#10847=DIRECTION ( 'NONE',  ( -1.000000000000000000, 0.000000000000000000, 0.000000000000000000 ) ) ;
#10848=FACE_OUTER_BOUND ( 'NONE', #1043, .T. ) ;
#10850=DIRECTION ( 'NONE',  ( -1.000000000000000000, 0.000000000000000000, 0.000000000000000000 ) ) ;
#10853=CARTESIAN_POINT ( 'NONE',  ( 0.000000000000000000, -0.4575788569250363036, -22.54798042742718778 ) ) ;
#10854=ORIENTED_EDGE ( 'NONE', *, *, #10619, .F. ) ;
#10855=DIRECTION ( 'NONE',  ( 0.000000000000000000, 0.000000000000000000, 1.000000000000000000 ) ) ;
#10856=EDGE_CURVE ( 'NONE', #4242, #9539, #1795, .T. ) ;
#10858=ADVANCED_FACE ( 'NONE', ( #1623 ), #11832, .T. ) ;
#10859=CARTESIAN_POINT ( 'NONE',  ( 3.000000000000000888, -18.40266524480597710, 13.79477846460790147 ) ) ;
#10860=CARTESIAN_POINT ( 'NONE',  ( 0.000000000000000000, 24.45282072769606430, -4.135161237383341515 ) ) ;
#10862=ORIENTED_EDGE ( 'NONE', *, *, #9914, .T. ) ;
#10863=DIRECTION ( 'NONE',  ( -1.000000000000000000, 0.000000000000000000, -0.000000000000000000 ) ) ;
#10864=CARTESIAN_POINT ( 'NONE',  ( 3.000000000000000888, -22.37663021667341923, 6.788022064061986605 ) ) ;
#10865=CARTESIAN_POINT ( 'NONE',  ( 0.000000000000000000, 15.13242714128143440, -17.31945870441131419 ) ) ;
#10866=CIRCLE ( 'NONE', #6934, 18.49999999999999645 ) ;
#10868=DIRECTION ( 'NONE',  ( 1.000000000000000000, 0.000000000000000000, 0.000000000000000000 ) ) ;
#10869=FACE_OUTER_BOUND ( 'NONE', #5302, .T. ) ;
#10870=EDGE_LOOP ( 'NONE', ( #6872, #1396, #3243, #9095 ) ) ;
#10871=VERTEX_POINT ( 'NONE', #5291 ) ;
#10872=VERTEX_POINT ( 'NONE', #5359 ) ;
#10873=CIRCLE ( 'NONE', #5005, 9.599999999999996092 ) ;
#10876=DIRECTION ( 'NONE',  ( -1.000000000000000000, -0.000000000000000000, -0.000000000000000000 ) ) ;
#10878=EDGE_CURVE ( 'NONE', #2308, #6849, #4576, .T. ) ;
#10881=CYLINDRICAL_SURFACE ( 'NONE', #1745, 9.599999999999997868 ) ;
#10882=ORIENTED_EDGE ( 'NONE', *, *, #4948, .F. ) ;
#10884=ORIENTED_EDGE ( 'NONE', *, *, #11256, .T. ) ;
#10886=FACE_OUTER_BOUND ( 'NONE', #9525, .T. ) ;
#10887=CARTESIAN_POINT ( 'NONE',  ( 3.000000000000000888, 18.40266524480588473, 13.79477846460802226 ) ) ;
#10888=EDGE_CURVE ( 'NONE', #6277, #6987, #2422, .T. ) ;
#10889=CARTESIAN_POINT ( 'NONE',  ( 3.000000000000000888, 11.20082935824075321, 20.08719549084868561 ) ) ;
#10890=ORIENTED_EDGE ( 'NONE', *, *, #9164, .F. ) ;
#10891=CARTESIAN_POINT ( 'NONE',  ( 3.000000000000000888, -0.4575788569250363036, -22.54798042742718778 ) ) ;
#10892=CARTESIAN_POINT ( 'NONE',  ( 0.000000000000000000, -22.37663021667346186, 2.811977935937707063 ) ) ;
#10894=FACE_OUTER_BOUND ( 'NONE', #9079, .T. ) ;
#10895=CARTESIAN_POINT ( 'NONE',  ( 8.000000000000000000, 2.265596578422603002E-15, -18.49999999999999645 ) ) ;
#10897=VECTOR ( 'NONE', #2289, 1000.000000000000000 ) ;
#10900=DIRECTION ( 'NONE',  ( 0.000000000000000000, 0.9135454576426018658, -0.4067366430757979323 ) ) ;
#10902=CARTESIAN_POINT ( 'NONE',  ( 3.000000000000000888, 0.000000000000000000, 0.000000000000000000 ) ) ;
#10904=CIRCLE ( 'NONE', #8169, 9.599999999999997868 ) ;
#10905=DIRECTION ( 'NONE',  ( -1.000000000000000000, 0.000000000000000000, -0.000000000000000000 ) ) ;
#10906=CYLINDRICAL_SURFACE ( 'NONE', #6074, 9.599999999999997868 ) ;
#10907=ORIENTED_EDGE ( 'NONE', *, *, #4570, .T. ) ;
#10908=CARTESIAN_POINT ( 'NONE',  ( 3.000000000000000888, -17.06259499759935139, -14.74749645580028101 ) ) ;
#10909=ORIENTED_EDGE ( 'NONE', *, *, #8689, .T. ) ;
#10911=AXIS2_PLACEMENT_3D ( 'NONE', #5792, #1929, #3889 ) ;
#10912=DIRECTION ( 'NONE',  ( 0.000000000000000000, 0.000000000000000000, 1.000000000000000000 ) ) ;
#10913=ORIENTED_EDGE ( 'NONE', *, *, #9683, .F. ) ;
#10914=FACE_OUTER_BOUND ( 'NONE', #3885, .T. ) ;
#10915=EDGE_CURVE ( 'NONE', #7882, #139, #75, .T. ) ;
#10916=DIRECTION ( 'NONE',  ( -1.000000000000000000, -0.000000000000000000, -0.000000000000000000 ) ) ;
#10919=EDGE_CURVE ( 'NONE', #4735, #5828, #8351, .T. ) ;
#10920=LINE ( 'NONE', #2537, #3555 ) ;
#10921=EDGE_CURVE ( 'NONE', #11050, #7635, #10046, .T. ) ;
#10922=VECTOR ( 'NONE', #9719, 1000.000000000000000 ) ;
#10923=DIRECTION ( 'NONE',  ( -1.000000000000000000, -0.000000000000000000, -0.000000000000000000 ) ) ;
#10924=EDGE_LOOP ( 'NONE', ( #6426, #5335, #11931, #11248 ) ) ;
#10925=ORIENTED_EDGE ( 'NONE', *, *, #4237, .T. ) ;
#10928=AXIS2_PLACEMENT_3D ( 'NONE', #8130, #8069, #7136 ) ;
#10929=ADVANCED_FACE ( 'NONE', ( #6338 ), #7292, .T. ) ;
#10930=AXIS2_PLACEMENT_3D ( 'NONE', #3312, #8375, #1885 ) ;
#10932=CARTESIAN_POINT ( 'NONE',  ( 0.000000000000000000, 1.039229259764835600, -24.77821629063820907 ) ) ;
#10934=DIRECTION ( 'NONE',  ( -1.000000000000000000, -0.000000000000000000, -0.000000000000000000 ) ) ;
#10935=CIRCLE ( 'NONE', #3318, 9.599999999999996092 ) ;
#10936=CARTESIAN_POINT ( 'NONE',  ( 0.000000000000000000, -13.62355943574006645, -17.97274125076088680 ) ) ;
#10937=ORIENTED_EDGE ( 'NONE', *, *, #7263, .T. ) ;
#10938=EDGE_LOOP ( 'NONE', ( #6422, #4927, #7505, #266 ) ) ;
#10939=EDGE_CURVE ( 'NONE', #6849, #6658, #639, .T. ) ;
#10941=ORIENTED_EDGE ( 'NONE', *, *, #7874, .T. ) ;
#10942=DIRECTION ( 'NONE',  ( -1.000000000000000000, -0.000000000000000000, 0.000000000000000000 ) ) ;
#10943=CARTESIAN_POINT ( 'NONE',  ( -10.00000000000000000, 0.000000000000000000, 0.000000000000000000 ) ) ;
#10944=ADVANCED_FACE ( 'NONE', ( #11950 ), #6447, .T. ) ;
#10946=ORIENTED_EDGE ( 'NONE', *, *, #2052, .F. ) ;
#10947=FACE_BOUND ( 'NONE', #10499, .T. ) ;
#10948=VECTOR ( 'NONE', #2049, 1000.000000000000000 ) ;
#10951=EDGE_CURVE ( 'NONE', #4817, #11323, #10637, .T. ) ;
#10952=CARTESIAN_POINT ( 'NONE',  ( 3.000000000000000888, 22.37663021667344054, -2.811977935937859385 ) ) ;
#10953=ORIENTED_EDGE ( 'NONE', *, *, #71, .T. ) ;
#10954=DIRECTION ( 'NONE',  ( 0.000000000000000000, -0.9945218953682744001, 0.1045284632676436593 ) ) ;
#10955=AXIS2_PLACEMENT_3D ( 'NONE', #1611, #3389, #11876 ) ;
#10956=ORIENTED_EDGE ( 'NONE', *, *, #299, .T. ) ;
#10957=ORIENTED_EDGE ( 'NONE', *, *, #9648, .F. ) ;
#10958=AXIS2_PLACEMENT_3D ( 'NONE', #6480, #4403, #5388 ) ;
#10960=AXIS2_PLACEMENT_3D ( 'NONE', #6616, #6558, #1722 ) ;
#10961=ORIENTED_EDGE ( 'NONE', *, *, #5184, .F. ) ;
#10962=CARTESIAN_POINT ( 'NONE',  ( 3.000000000000000888, -22.37663021667341923, -2.811977935938010376 ) ) ;
#10964=ORIENTED_EDGE ( 'NONE', *, *, #10248, .T. ) ;
#10965=DIRECTION ( 'NONE',  ( 0.000000000000000000, 0.000000000000000000, 1.000000000000000000 ) ) ;
#10966=DIRECTION ( 'NONE',  ( 1.000000000000000000, 0.000000000000000000, -0.000000000000000000 ) ) ;
#10968=CIRCLE ( 'NONE', #7239, 24.80000000000000071 ) ;
#10969=CARTESIAN_POINT ( 'NONE',  ( 3.000000000000000888, 11.67026512804547345, 19.29833442572363822 ) ) ;
#10970=EDGE_CURVE ( 'NONE', #9017, #2317, #2822, .T. ) ;
#10971=CARTESIAN_POINT ( 'NONE',  ( 3.000000000000000888, 19.75591328264886215, 10.87771529938168946 ) ) ;
#10972=VERTEX_POINT ( 'NONE', #1918 ) ;
#10973=ORIENTED_EDGE ( 'NONE', *, *, #7854, .T. ) ;
#10974=CARTESIAN_POINT ( 'NONE',  ( 3.000000000000000888, -21.58580335785672233, -6.532525787311189269 ) ) ;
#10975=VERTEX_POINT ( 'NONE', #11405 ) ;
#10977=AXIS2_PLACEMENT_3D ( 'NONE', #8537, #9629, #3945 ) ;
#10978=AXIS2_PLACEMENT_3D ( 'NONE', #1378, #5111, #8854 ) ;
#10979=DIRECTION ( 'NONE',  ( 0.000000000000000000, 0.000000000000000000, 1.000000000000000000 ) ) ;
#10981=ORIENTED_EDGE ( 'NONE', *, *, #9789, .F. ) ;
#10982=AXIS2_PLACEMENT_3D ( 'NONE', #1860, #7418, #5536 ) ;
#10983=CYLINDRICAL_SURFACE ( 'NONE', #930, 9.599999999999997868 ) ;
#10984=CARTESIAN_POINT ( 'NONE',  ( 3.000000000000000888, -19.74380051311532114, -11.79560690673893042 ) ) ;
#10987=DIRECTION ( 'NONE',  ( -1.000000000000000000, -0.000000000000000000, -0.000000000000000000 ) ) ;
#10988=CARTESIAN_POINT ( 'NONE',  ( 0.000000000000000000, 19.43515443678423793, -15.40502424595125852 ) ) ;
#10989=CIRCLE ( 'NONE', #3372, 22.99899999999999523 ) ;
#10991=AXIS2_PLACEMENT_3D ( 'NONE', #4650, #2631, #9239 ) ;
#10994=EDGE_LOOP ( 'NONE', ( #961, #340, #4893, #11926 ) ) ;
#10996=EDGE_CURVE ( 'NONE', #10809, #10316, #6914, .T. ) ;
#10997=CIRCLE ( 'NONE', #9823, 9.599999999999999645 ) ;
#10998=CARTESIAN_POINT ( 'NONE',  ( 0.000000000000000000, 0.000000000000000000, 0.000000000000000000 ) ) ;
#10999=DIRECTION ( 'NONE',  ( -1.000000000000000000, -0.000000000000000000, -0.000000000000000000 ) ) ;
#11000=ADVANCED_FACE ( 'NONE', ( #2966 ), #6625, .T. ) ;
#11002=CARTESIAN_POINT ( 'NONE',  ( 3.000000000000000888, 0.000000000000000000, 0.000000000000000000 ) ) ;
#11003=EDGE_CURVE ( 'NONE', #3932, #6844, #7898, .T. ) ;
#11004=CARTESIAN_POINT ( 'NONE',  ( 1.499999999999999556, 24.75110766671652129, 1.556492618230721492 ) ) ;
#11007=ORIENTED_EDGE ( 'NONE', *, *, #5841, .T. ) ;
#11009=ORIENTED_EDGE ( 'NONE', *, *, #875, .T. ) ;
#11011=VECTOR ( 'NONE', #1643, 1000.000000000000000 ) ;
#11012=AXIS2_PLACEMENT_3D ( 'NONE', #9268, #2845, #887 ) ;
#11013=CARTESIAN_POINT ( 'NONE',  ( 3.000000000000000888, -6.532525787311115550, 21.58580335785674365 ) ) ;
#11014=DIRECTION ( 'NONE',  ( -1.000000000000000000, 0.000000000000000000, -0.000000000000000000 ) ) ;
#11015=CIRCLE ( 'NONE', #6905, 24.80000000000000071 ) ;
#11016=DIRECTION ( 'NONE',  ( 0.000000000000000000, -0.9135454576425964257, -0.4067366430758104223 ) ) ;
#11017=DIRECTION ( 'NONE',  ( -1.000000000000000000, -0.000000000000000000, -0.000000000000000000 ) ) ;
#11019=DIRECTION ( 'NONE',  ( -1.000000000000000000, 0.000000000000000000, -0.000000000000000000 ) ) ;
#11020=ORIENTED_EDGE ( 'NONE', *, *, #9726, .F. ) ;
#11021=DIRECTION ( 'NONE',  ( 0.000000000000000000, -0.9510565162951504226, -0.3090169943749574433 ) ) ;
#11022=ORIENTED_EDGE ( 'NONE', *, *, #1982, .F. ) ;
#11023=AXIS2_PLACEMENT_3D ( 'NONE', #45, #1093, #12040 ) ;
#11025=ORIENTED_EDGE ( 'NONE', *, *, #7199, .T. ) ;
#11026=DIRECTION ( 'NONE',  ( -1.000000000000000000, 0.000000000000000000, 0.000000000000000000 ) ) ;
#11027=VERTEX_POINT ( 'NONE', #10482 ) ;
#11028=CARTESIAN_POINT ( 'NONE',  ( 3.000000000000000888, 9.039786367039127413, -21.14796121233187520 ) ) ;
#11029=CARTESIAN_POINT ( 'NONE',  ( 3.000000000000000888, 9.589108953447894379, 20.41249101028215307 ) ) ;
#11032=CARTESIAN_POINT ( 'NONE',  ( 3.000000000000000888, 20.86861857134734421, 9.667200211209893368 ) ) ;
#11033=EDGE_CURVE ( 'NONE', #3365, #4516, #9665, .T. ) ;
#11034=FACE_OUTER_BOUND ( 'NONE', #9047, .T. ) ;
#11035=EDGE_LOOP ( 'NONE', ( #3526, #4406, #459, #681 ) ) ;
#11036=ORIENTED_EDGE ( 'NONE', *, *, #11363, .F. ) ;
#11037=CARTESIAN_POINT ( 'NONE',  ( 3.000000000000000888, 22.56530478845654386, -4.445336973060635799 ) ) ;
#11038=ORIENTED_EDGE ( 'NONE', *, *, #6335, .T. ) ;
#11040=AXIS2_PLACEMENT_3D ( 'NONE', #4741, #7667, #258 ) ;
#11043=EDGE_CURVE ( 'NONE', #4836, #10397, #5562, .T. ) ;
#11044=CARTESIAN_POINT ( 'NONE',  ( 3.000000000000000888, -13.28910708463142498, 20.93895013827577145 ) ) ;
#11048=DIRECTION ( 'NONE',  ( 0.000000000000000000, 0.000000000000000000, -1.000000000000000000 ) ) ;
#11049=CARTESIAN_POINT ( 'NONE',  ( 3.000000000000000888, 11.67026512804572924, -19.29833442572348190 ) ) ;
#11050=VERTEX_POINT ( 'NONE', #8411 ) ;
#11051=ORIENTED_EDGE ( 'NONE', *, *, #6795, .T. ) ;
#11054=DIRECTION ( 'NONE',  ( -1.000000000000000000, 0.000000000000000000, -0.000000000000000000 ) ) ;
#11055=AXIS2_PLACEMENT_3D ( 'NONE', #1550, #6682, #9380 ) ;
#11057=DIRECTION ( 'NONE',  ( -1.000000000000000000, -0.000000000000000000, -0.000000000000000000 ) ) ;
#11058=ORIENTED_EDGE ( 'NONE', *, *, #11459, .T. ) ;
#11059=DIRECTION ( 'NONE',  ( 0.000000000000000000, -0.9781476007338034684, -0.2079116908177697509 ) ) ;
#11060=ORIENTED_EDGE ( 'NONE', *, *, #6432, .T. ) ;
#11061=VERTEX_POINT ( 'NONE', #7483 ) ;
#11062=DIRECTION ( 'NONE',  ( 0.000000000000000000, 0.000000000000000000, 1.000000000000000000 ) ) ;
#11063=EDGE_CURVE ( 'NONE', #862, #3166, #1859, .T. ) ;
#11064=DIRECTION ( 'NONE',  ( 0.000000000000000000, 0.3090169943749480064, -0.9510565162951533091 ) ) ;
#11065=LINE ( 'NONE', #8192, #9119 ) ;
#11067=DIRECTION ( 'NONE',  ( -1.000000000000000000, -0.000000000000000000, -0.000000000000000000 ) ) ;
#11068=AXIS2_PLACEMENT_3D ( 'NONE', #5577, #1161, #8460 ) ;
#11069=ADVANCED_FACE ( 'NONE', ( #5593 ), #9382, .T. ) ;
#11070=DIRECTION ( 'NONE',  ( 0.000000000000000000, -0.2079116908177466305, -0.9781476007338082423 ) ) ;
#11071=LINE ( 'NONE', #10681, #7449 ) ;
#11073=FACE_OUTER_BOUND ( 'NONE', #5558, .T. ) ;
#11074=EDGE_LOOP ( 'NONE', ( #11304, #7507, #1235, #8665 ) ) ;
#11075=ORIENTED_EDGE ( 'NONE', *, *, #2355, .F. ) ;
#11076=FACE_OUTER_BOUND ( 'NONE', #4832, .T. ) ;
#11078=ORIENTED_EDGE ( 'NONE', *, *, #101, .F. ) ;
#11080=EDGE_LOOP ( 'NONE', ( #10151, #935, #12051, #7326 ) ) ;
#11081=DIRECTION ( 'NONE',  ( 0.000000000000000000, -0.9135454576426046414, 0.4067366430757920481 ) ) ;
#11082=ORIENTED_EDGE ( 'NONE', *, *, #4345, .T. ) ;
#11083=ADVANCED_FACE ( 'NONE', ( #5723 ), #3762, .T. ) ;
#11084=DIRECTION ( 'NONE',  ( -1.000000000000000000, -0.000000000000000000, 0.000000000000000000 ) ) ;
#11085=CARTESIAN_POINT ( 'NONE',  ( 1.500000000000000444, -17.35216073792452107, 17.71842311621524146 ) ) ;
#11087=DIRECTION ( 'NONE',  ( -1.000000000000000000, 0.000000000000000000, 0.000000000000000000 ) ) ;
#11088=CARTESIAN_POINT ( 'NONE',  ( 0.000000000000000000, 22.83456483164689033, 2.745295967526073078 ) ) ;
#11089=ORIENTED_EDGE ( 'NONE', *, *, #5774, .F. ) ;
#11090=LINE ( 'NONE', #2706, #3725 ) ;
#11091=ORIENTED_EDGE ( 'NONE', *, *, #11991, .T. ) ;
#11092=ADVANCED_FACE ( 'NONE', ( #3943 ), #1007, .T. ) ;
#11095=CARTESIAN_POINT ( 'NONE',  ( 0.000000000000000000, 0.000000000000000000, 0.000000000000000000 ) ) ;
#11096=EDGE_CURVE ( 'NONE', #4186, #5315, #3810, .T. ) ;
#11097=FACE_OUTER_BOUND ( 'NONE', #3287, .T. ) ;
#11098=CYLINDRICAL_SURFACE ( 'NONE', #8242, 22.99899999999999878 ) ;
#11099=CARTESIAN_POINT ( 'NONE',  ( 3.000000000000000888, 20.41249101028211754, -9.589108953447965433 ) ) ;
#11100=CARTESIAN_POINT ( 'NONE',  ( 0.000000000000000000, 0.000000000000000000, 0.000000000000000000 ) ) ;
#11102=DIRECTION ( 'NONE',  ( 0.000000000000000000, 0.7431448254773909134, 0.6691306063588619013 ) ) ;
#11103=DIRECTION ( 'NONE',  ( -1.000000000000000000, -0.000000000000000000, 0.000000000000000000 ) ) ;
#11104=ORIENTED_EDGE ( 'NONE', *, *, #8498, .T. ) ;
#11105=EDGE_CURVE ( 'NONE', #10471, #6735, #3418, .T. ) ;
#11106=ORIENTED_EDGE ( 'NONE', *, *, #10919, .T. ) ;
#11107=EDGE_LOOP ( 'NONE', ( #675, #4637, #4566, #1776 ) ) ;
#11108=DIRECTION ( 'NONE',  ( 0.000000000000000000, 0.5877852522924742473, -0.8090169943749467851 ) ) ;
#11110=LINE ( 'NONE', #707, #1925 ) ;
#11113=CIRCLE ( 'NONE', #4872, 18.49999999999999645 ) ;
#11114=VECTOR ( 'NONE', #7693, 1000.000000000000000 ) ;
#11115=LINE ( 'NONE', #7370, #8062 ) ;
#11117=ORIENTED_EDGE ( 'NONE', *, *, #3784, .F. ) ;
#11118=ORIENTED_EDGE ( 'NONE', *, *, #6179, .F. ) ;
#11120=DIRECTION ( 'NONE',  ( -1.000000000000000000, -0.000000000000000000, 0.000000000000000000 ) ) ;
#11122=CARTESIAN_POINT ( 'NONE',  ( 3.000000000000000888, 15.40502424595145037, 19.43515443678408516 ) ) ;
#11123=DIRECTION ( 'NONE',  ( -1.000000000000000000, 0.000000000000000000, 0.000000000000000000 ) ) ;
#11125=DIRECTION ( 'NONE',  ( -1.000000000000000000, 0.000000000000000000, 0.000000000000000000 ) ) ;
#11128=CIRCLE ( 'NONE', #6041, 22.99899999999999878 ) ;
#11129=AXIS2_PLACEMENT_3D ( 'NONE', #4884, #8683, #156 ) ;
#11130=AXIS2_PLACEMENT_3D ( 'NONE', #530, #1453, #5187 ) ;
#11131=CARTESIAN_POINT ( 'NONE',  ( 3.000000000000000888, 22.37663021667340146, 2.811977935938166695 ) ) ;
#11132=VERTEX_POINT ( 'NONE', #11463 ) ;
#11133=VERTEX_POINT ( 'NONE', #941 ) ;
#11134=DIRECTION ( 'NONE',  ( 1.000000000000000000, 0.000000000000000000, 0.000000000000000000 ) ) ;
#11135=ORIENTED_EDGE ( 'NONE', *, *, #3182, .T. ) ;
#11136=EDGE_LOOP ( 'NONE', ( #4089, #1935, #11592, #8105 ) ) ;
#11138=EDGE_CURVE ( 'NONE', #1768, #1367, #6565, .T. ) ;
#11139=ORIENTED_EDGE ( 'NONE', *, *, #7879, .T. ) ;
#11140=CARTESIAN_POINT ( 'NONE',  ( 3.000000000000000888, -20.86861857134728027, -9.667200211210033700 ) ) ;
#11141=EDGE_CURVE ( 'NONE', #2390, #1419, #3607, .T. ) ;
#11142=EDGE_LOOP ( 'NONE', ( #435, #9066, #10041, #11995 ) ) ;
#11143=ADVANCED_FACE ( 'NONE', ( #4797 ), #8533, .T. ) ;
#11144=CIRCLE ( 'NONE', #6643, 9.599999999999997868 ) ;
#11147=DIRECTION ( 'NONE',  ( 0.000000000000000000, -0.9945218953682744001, 0.1045284632676437564 ) ) ;
#11149=DIRECTION ( 'NONE',  ( -1.000000000000000000, 0.000000000000000000, 0.000000000000000000 ) ) ;
#11150=AXIS2_PLACEMENT_3D ( 'NONE', #11346, #3032, #501 ) ;
#11152=ORIENTED_EDGE ( 'NONE', *, *, #2783, .T. ) ;
#11153=ORIENTED_EDGE ( 'NONE', *, *, #846, .T. ) ;
#11154=DIRECTION ( 'NONE',  ( -1.000000000000000000, -0.000000000000000000, -0.000000000000000000 ) ) ;
#11155=CIRCLE ( 'NONE', #7031, 9.599999999999996092 ) ;
#11156=ORIENTED_EDGE ( 'NONE', *, *, #3225, .F. ) ;
#11160=ADVANCED_FACE ( 'NONE', ( #316 ), #8892, .T. ) ;
#11163=ORIENTED_EDGE ( 'NONE', *, *, #8312, .T. ) ;
#11164=LINE ( 'NONE', #1004, #2108 ) ;
#11165=AXIS2_PLACEMENT_3D ( 'NONE', #727, #8264, #1895 ) ;
#11166=CARTESIAN_POINT ( 'NONE',  ( 3.000000000000000888, 0.000000000000000000, 0.000000000000000000 ) ) ;
#11169=DIRECTION ( 'NONE',  ( -1.000000000000000000, 0.000000000000000000, -0.000000000000000000 ) ) ;
#11170=CARTESIAN_POINT ( 'NONE',  ( 0.000000000000000000, 5.135568396240030253, 21.96011696265493285 ) ) ;
#11171=DIRECTION ( 'NONE',  ( 0.000000000000000000, -0.9945218953682721796, -0.1045284632676635739 ) ) ;
#11172=ORIENTED_EDGE ( 'NONE', *, *, #10846, .F. ) ;
#11173=CIRCLE ( 'NONE', #8451, 22.99899999999999523 ) ;
#11174=VERTEX_POINT ( 'NONE', #1358 ) ;
#11175=CIRCLE ( 'NONE', #3940, 22.99899999999999878 ) ;
#11176=AXIS2_PLACEMENT_3D ( 'NONE', #1682, #10987, #1627 ) ;
#11177=EDGE_LOOP ( 'NONE', ( #11414, #11118, #841, #8386 ) ) ;
#11178=CARTESIAN_POINT ( 'NONE',  ( 0.000000000000000000, 0.000000000000000000, 0.000000000000000000 ) ) ;
#11180=DIRECTION ( 'NONE',  ( -1.000000000000000000, -0.000000000000000000, 0.000000000000000000 ) ) ;
#11184=CIRCLE ( 'NONE', #4708, 24.80000000000000071 ) ;
#11186=CARTESIAN_POINT ( 'NONE',  ( 0.000000000000000000, -20.93895013827591001, 13.28910708463121360 ) ) ;
#11187=ADVANCED_FACE ( 'NONE', ( #2157 ), #10788, .T. ) ;
#11188=EDGE_LOOP ( 'NONE', ( #3401, #5210, #2463, #562 ) ) ;
#11189=ORIENTED_EDGE ( 'NONE', *, *, #8405, .F. ) ;
#11190=CIRCLE ( 'NONE', #2782, 9.599999999999997868 ) ;
#11191=VERTEX_POINT ( 'NONE', #8023 ) ;
#11192=DIRECTION ( 'NONE',  ( -1.000000000000000000, 0.000000000000000000, -0.000000000000000000 ) ) ;
#11193=CARTESIAN_POINT ( 'NONE',  ( 3.000000000000000888, -24.75110766671651064, -1.556492618230893132 ) ) ;
#11194=VECTOR ( 'NONE', #1320, 1000.000000000000000 ) ;
#11195=CARTESIAN_POINT ( 'NONE',  ( 3.000000000000000888, 0.000000000000000000, 0.000000000000000000 ) ) ;
#11196=DIRECTION ( 'NONE',  ( 0.000000000000000000, 0.000000000000000000, 1.000000000000000000 ) ) ;
#11197=EDGE_CURVE ( 'NONE', #11333, #992, #5164, .T. ) ;
#11198=CARTESIAN_POINT ( 'NONE',  ( 3.000000000000000888, 9.039786367038837867, 21.14796121233199599 ) ) ;
#11201=DIRECTION ( 'NONE',  ( 0.000000000000000000, -0.3090169943749349057, -0.9510565162951577500 ) ) ;
#11202=ORIENTED_EDGE ( 'NONE', *, *, #5991, .T. ) ;
#11203=EDGE_LOOP ( 'NONE', ( #7313, #495, #702, #9228 ) ) ;
#11205=DIRECTION ( 'NONE',  ( 1.000000000000000000, -0.000000000000000000, 0.000000000000000000 ) ) ;
#11206=ORIENTED_EDGE ( 'NONE', *, *, #1579, .T. ) ;
#11207=ORIENTED_EDGE ( 'NONE', *, *, #9082, .F. ) ;
#11209=AXIS2_PLACEMENT_3D ( 'NONE', #6729, #5073, #8639 ) ;
#11210=LINE ( 'NONE', #10403, #7148 ) ;
#11211=ORIENTED_EDGE ( 'NONE', *, *, #5471, .T. ) ;
#11212=VECTOR ( 'NONE', #6588, 1000.000000000000000 ) ;
#11213=FACE_OUTER_BOUND ( 'NONE', #9714, .T. ) ;
#11214=LINE ( 'NONE', #62, #7860 ) ;
#11216=CARTESIAN_POINT ( 'NONE',  ( 3.000000000000000888, 9.667200211209818761, 20.86861857134737264 ) ) ;
#11217=CARTESIAN_POINT ( 'NONE',  ( 3.000000000000000888, -20.41249101028205004, -9.589108953448107542 ) ) ;
#11218=VERTEX_POINT ( 'NONE', #438 ) ;
#11219=EDGE_LOOP ( 'NONE', ( #4477, #10672 ) ) ;
#11220=FACE_OUTER_BOUND ( 'NONE', #11107, .T. ) ;
#11221=ORIENTED_EDGE ( 'NONE', *, *, #11265, .T. ) ;
#11224=DIRECTION ( 'NONE',  ( 1.000000000000000000, -0.000000000000000000, -0.000000000000000000 ) ) ;
#11226=VECTOR ( 'NONE', #7696, 1000.000000000000000 ) ;
#11227=CARTESIAN_POINT ( 'NONE',  ( 1.500000000000000444, 1.039229259764490321, 24.77821629063822328 ) ) ;
#11228=DIRECTION ( 'NONE',  ( -1.000000000000000000, 0.000000000000000000, 0.000000000000000000 ) ) ;
#11230=EDGE_CURVE ( 'NONE', #8970, #3076, #85, .T. ) ;
#11232=DIRECTION ( 'NONE',  ( -1.000000000000000000, 0.000000000000000000, 0.000000000000000000 ) ) ;
#11233=EDGE_CURVE ( 'NONE', #3964, #11218, #2236, .T. ) ;
#11234=DIRECTION ( 'NONE',  ( -1.000000000000000000, 0.000000000000000000, 0.000000000000000000 ) ) ;
#11235=ORIENTED_EDGE ( 'NONE', *, *, #8174, .T. ) ;
#11236=EDGE_CURVE ( 'NONE', #1419, #6719, #6151, .T. ) ;
#11237=ORIENTED_EDGE ( 'NONE', *, *, #6325, .F. ) ;
#11238=AXIS2_PLACEMENT_3D ( 'NONE', #5781, #9565, #9447 ) ;
#11239=VERTEX_POINT ( 'NONE', #8715 ) ;
#11240=DIRECTION ( 'NONE',  ( 0.000000000000000000, 0.5000000000000011102, -0.8660254037844381525 ) ) ;
#11244=CARTESIAN_POINT ( 'NONE',  ( 1.499999999999999556, -1.039229259764661961, 24.77821629063821263 ) ) ;
#11245=CARTESIAN_POINT ( 'NONE',  ( 3.000000000000000888, 0.000000000000000000, 0.000000000000000000 ) ) ;
#11246=VERTEX_POINT ( 'NONE', #7908 ) ;
#11247=ORIENTED_EDGE ( 'NONE', *, *, #5232, .F. ) ;
#11248=ORIENTED_EDGE ( 'NONE', *, *, #3771, .T. ) ;
#11250=CARTESIAN_POINT ( 'NONE',  ( 0.000000000000000000, -19.74380051311532114, -11.79560690673893042 ) ) ;
#11251=ADVANCED_FACE ( 'NONE', ( #7961 ), #6922, .T. ) ;
#11252=CIRCLE ( 'NONE', #8519, 22.99899999999999523 ) ;
#11253=DIRECTION ( 'NONE',  ( -1.000000000000000000, 0.000000000000000000, 0.000000000000000000 ) ) ;
#11254=DIRECTION ( 'NONE',  ( 0.000000000000000000, 0.000000000000000000, 1.000000000000000000 ) ) ;
#11255=CARTESIAN_POINT ( 'NONE',  ( 3.000000000000000888, 12.88318129270205148, -18.51065745848364230 ) ) ;
#11256=EDGE_CURVE ( 'NONE', #5746, #10699, #3219, .T. ) ;
#11259=CARTESIAN_POINT ( 'NONE',  ( 0.000000000000000000, 5.117118920208799437, -22.42251312757874260 ) ) ;
#11260=DIRECTION ( 'NONE',  ( 0.000000000000000000, -0.9781476007338077983, 0.2079116908177493783 ) ) ;
#11261=CARTESIAN_POINT ( 'NONE',  ( 3.000000000000000888, 0.000000000000000000, 0.000000000000000000 ) ) ;
#11262=ORIENTED_EDGE ( 'NONE', *, *, #8539, .F. ) ;
#11263=ORIENTED_EDGE ( 'NONE', *, *, #823, .T. ) ;
#11264=LINE ( 'NONE', #2878, #795 ) ;
#11265=EDGE_CURVE ( 'NONE', #9763, #5965, #557, .T. ) ;
#11266=ORIENTED_EDGE ( 'NONE', *, *, #4192, .T. ) ;
#11267=DIRECTION ( 'NONE',  ( -1.000000000000000000, 0.000000000000000000, -0.000000000000000000 ) ) ;
#11268=DIRECTION ( 'NONE',  ( 0.000000000000000000, 0.7431448254773909134, 0.6691306063588619013 ) ) ;
#11269=VECTOR ( 'NONE', #5633, 1000.000000000000000 ) ;
#11270=ORIENTED_EDGE ( 'NONE', *, *, #7095, .F. ) ;
#11271=CYLINDRICAL_SURFACE ( 'NONE', #8482, 9.599999999999997868 ) ;
#11274=CARTESIAN_POINT ( 'NONE',  ( 3.000000000000000888, 5.117118920208799437, -22.42251312757874260 ) ) ;
#11275=DIRECTION ( 'NONE',  ( -1.000000000000000000, -0.000000000000000000, 0.000000000000000000 ) ) ;
#11276=CARTESIAN_POINT ( 'NONE',  ( 1.499999999999999556, -23.88662356770110762, -6.668524164681869593 ) ) ;
#11277=ORIENTED_EDGE ( 'NONE', *, *, #8626, .T. ) ;
#11278=AXIS2_PLACEMENT_3D ( 'NONE', #2080, #10520, #4217 ) ;
#11280=DIRECTION ( 'NONE',  ( 0.000000000000000000, -0.9135454576425964257, -0.4067366430758103668 ) ) ;
#11281=ORIENTED_EDGE ( 'NONE', *, *, #1124, .T. ) ;
#11283=DIRECTION ( 'NONE',  ( -1.000000000000000000, 0.000000000000000000, 0.000000000000000000 ) ) ;
#11285=CARTESIAN_POINT ( 'NONE',  ( 3.000000000000000888, 0.000000000000000000, 22.99899999999999878 ) ) ;
#11286=DIRECTION ( 'NONE',  ( 0.000000000000000000, -0.9510565162951565288, 0.3090169943749382364 ) ) ;
#11288=CARTESIAN_POINT ( 'NONE',  ( 3.000000000000000888, 0.000000000000000000, 0.000000000000000000 ) ) ;
#11289=DIRECTION ( 'NONE',  ( 0.000000000000000000, 0.000000000000000000, 1.000000000000000000 ) ) ;
#11290=CARTESIAN_POINT ( 'NONE',  ( 3.000000000000000888, 0.000000000000000000, 0.000000000000000000 ) ) ;
#11291=CARTESIAN_POINT ( 'NONE',  ( 3.000000000000000888, 0.000000000000000000, 0.000000000000000000 ) ) ;
#11292=ORIENTED_EDGE ( 'NONE', *, *, #7990, .T. ) ;
#11293=AXIS2_PLACEMENT_3D ( 'NONE', #9933, #4556, #3578 ) ;
#11294=LINE ( 'NONE', #9393, #8201 ) ;
#11296=EDGE_CURVE ( 'NONE', #1972, #2776, #9627, .T. ) ;
#11297=DIRECTION ( 'NONE',  ( 0.000000000000000000, 0.000000000000000000, 1.000000000000000000 ) ) ;
#11298=EDGE_CURVE ( 'NONE', #3516, #3003, #1847, .T. ) ;
#11300=AXIS2_PLACEMENT_3D ( 'NONE', #189, #10299, #3939 ) ;
#11301=LINE ( 'NONE', #2918, #1979 ) ;
#11302=ORIENTED_EDGE ( 'NONE', *, *, #7900, .F. ) ;
#11303=ORIENTED_EDGE ( 'NONE', *, *, #3214, .F. ) ;
#11304=ORIENTED_EDGE ( 'NONE', *, *, #7778, .T. ) ;
#11305=EDGE_CURVE ( 'NONE', #7198, #1881, #9473, .T. ) ;
#11306=CARTESIAN_POINT ( 'NONE',  ( 3.000000000000000888, -5.135568396240178579, 21.96011696265489377 ) ) ;
#11308=CIRCLE ( 'NONE', #6799, 22.99899999999999523 ) ;
#11309=CYLINDRICAL_SURFACE ( 'NONE', #11524, 9.599999999999997868 ) ;
#11310=CYLINDRICAL_SURFACE ( 'NONE', #11883, 9.599999999999997868 ) ;
#11311=AXIS2_PLACEMENT_3D ( 'NONE', #9949, #8301, #4385 ) ;
#11314=CARTESIAN_POINT ( 'NONE',  ( 3.000000000000000888, 23.88662356770115736, 6.668524164681708832 ) ) ;
#11315=EDGE_LOOP ( 'NONE', ( #458, #7702, #7705, #5890 ) ) ;
#11316=ORIENTED_EDGE ( 'NONE', *, *, #9569, .T. ) ;
#11317=AXIS2_PLACEMENT_3D ( 'NONE', #8041, #7291, #5465 ) ;
#11318=DIRECTION ( 'NONE',  ( 0.000000000000000000, -0.1045284632676401482, -0.9945218953682748442 ) ) ;
#11319=VERTEX_POINT ( 'NONE', #2277 ) ;
#11320=EDGE_CURVE ( 'NONE', #9990, #7212, #4585, .T. ) ;
#11321=DIRECTION ( 'NONE',  ( 0.000000000000000000, 0.000000000000000000, 1.000000000000000000 ) ) ;
#11323=VERTEX_POINT ( 'NONE', #11639 ) ;
#11324=CIRCLE ( 'NONE', #6043, 24.80000000000000071 ) ;
#11326=FACE_OUTER_BOUND ( 'NONE', #12064, .T. ) ;
#11328=DIRECTION ( 'NONE',  ( 0.000000000000000000, -0.3090169943749545012, 0.9510565162951513107 ) ) ;
#11329=DIRECTION ( 'NONE',  ( -1.000000000000000000, -0.000000000000000000, -0.000000000000000000 ) ) ;
#11330=ORIENTED_EDGE ( 'NONE', *, *, #3182, .F. ) ;
#11332=CARTESIAN_POINT ( 'NONE',  ( 3.000000000000000888, 13.62355943574044481, -17.97274125076060258 ) ) ;
#11333=VERTEX_POINT ( 'NONE', #3257 ) ;
#11334=EDGE_CURVE ( 'NONE', #9734, #35, #6976, .T. ) ;
#11336=CIRCLE ( 'NONE', #4110, 9.599999999999997868 ) ;
#11337=DIRECTION ( 'NONE',  ( 0.000000000000000000, -0.3090169943749543902, 0.9510565162951514218 ) ) ;
#11338=ORIENTED_EDGE ( 'NONE', *, *, #8268, .T. ) ;
#11339=CARTESIAN_POINT ( 'NONE',  ( 0.000000000000000000, -19.10918332567947076, -15.80756504416710229 ) ) ;
#11340=EDGE_CURVE ( 'NONE', #10253, #11877, #4198, .T. ) ;
#11341=DIRECTION ( 'NONE',  ( -1.000000000000000000, 0.000000000000000000, 0.000000000000000000 ) ) ;
#11343=CIRCLE ( 'NONE', #6064, 9.599999999999996092 ) ;
#11344=DIRECTION ( 'NONE',  ( 0.000000000000000000, 0.000000000000000000, 1.000000000000000000 ) ) ;
#11345=DIRECTION ( 'NONE',  ( -1.000000000000000000, -0.000000000000000000, -0.000000000000000000 ) ) ;
#11346=CARTESIAN_POINT ( 'NONE',  ( 3.000000000000000000, 0.000000000000000000, 0.000000000000000000 ) ) ;
#11347=ORIENTED_EDGE ( 'NONE', *, *, #5397, .T. ) ;
#11349=ORIENTED_EDGE ( 'NONE', *, *, #10200, .F. ) ;
#11350=AXIS2_PLACEMENT_3D ( 'NONE', #6514, #9329, #11171 ) ;
#11352=CIRCLE ( 'NONE', #3537, 9.599999999999996092 ) ;
#11354=CIRCLE ( 'NONE', #8029, 9.599999999999996092 ) ;
#11355=DIRECTION ( 'NONE',  ( -1.000000000000000000, 0.000000000000000000, -0.000000000000000000 ) ) ;
#11358=CIRCLE ( 'NONE', #3153, 24.80000000000000071 ) ;
#11359=CYLINDRICAL_SURFACE ( 'NONE', #5307, 9.599999999999997868 ) ;
#11361=EDGE_LOOP ( 'NONE', ( #11211, #1405, #6709, #4683 ) ) ;
#11363=EDGE_CURVE ( 'NONE', #730, #3959, #6722, .T. ) ;
#11364=VERTEX_POINT ( 'NONE', #1607 ) ;
#11366=DIRECTION ( 'NONE',  ( -1.000000000000000000, 0.000000000000000000, 0.000000000000000000 ) ) ;
#11368=VERTEX_POINT ( 'NONE', #9008 ) ;
#11369=EDGE_CURVE ( 'NONE', #9620, #8125, #873, .T. ) ;
#11370=DIRECTION ( 'NONE',  ( -1.000000000000000000, 0.000000000000000000, 0.000000000000000000 ) ) ;
#11371=DIRECTION ( 'NONE',  ( 1.000000000000000000, 0.000000000000000000, 0.000000000000000000 ) ) ;
#11372=VECTOR ( 'NONE', #3612, 1000.000000000000000 ) ;
#11373=DIRECTION ( 'NONE',  ( -1.000000000000000000, -0.000000000000000000, -0.000000000000000000 ) ) ;
#11375=EDGE_CURVE ( 'NONE', #6837, #679, #10100, .T. ) ;
#11376=EDGE_CURVE ( 'NONE', #11900, #5379, #8504, .T. ) ;
#11377=VECTOR ( 'NONE', #440, 1000.000000000000000 ) ;
#11378=CARTESIAN_POINT ( 'NONE',  ( 3.000000000000000888, -7.432877647175354596, 21.76479567747239230 ) ) ;
#11379=VERTEX_POINT ( 'NONE', #4416 ) ;
#11380=CIRCLE ( 'NONE', #6102, 24.80000000000000071 ) ;
#11381=EDGE_LOOP ( 'NONE', ( #7267, #869, #1893, #6601 ) ) ;
#11382=EDGE_CURVE ( 'NONE', #8357, #4987, #3998, .T. ) ;
#11384=ORIENTED_EDGE ( 'NONE', *, *, #1451, .T. ) ;
#11385=CARTESIAN_POINT ( 'NONE',  ( 0.000000000000000000, 0.000000000000000000, 0.000000000000000000 ) ) ;
#11386=DIRECTION ( 'NONE',  ( 0.000000000000000000, 0.000000000000000000, 1.000000000000000000 ) ) ;
#11387=DIRECTION ( 'NONE',  ( 0.000000000000000000, 0.000000000000000000, 1.000000000000000000 ) ) ;
#11388=ORIENTED_EDGE ( 'NONE', *, *, #11629, .T. ) ;
#11390=CARTESIAN_POINT ( 'NONE',  ( 0.000000000000000000, 9.589108953447894379, 20.41249101028215307 ) ) ;
#11391=DIRECTION ( 'NONE',  ( 0.000000000000000000, -0.9945218953682721796, -0.1045284632676635878 ) ) ;
#11394=ORIENTED_EDGE ( 'NONE', *, *, #10698, .T. ) ;
#11395=DIRECTION ( 'NONE',  ( -1.000000000000000000, -0.000000000000000000, 0.000000000000000000 ) ) ;
#11396=ORIENTED_EDGE ( 'NONE', *, *, #1432, .T. ) ;
#11397=ORIENTED_EDGE ( 'NONE', *, *, #4942, .F. ) ;
#11398=CARTESIAN_POINT ( 'NONE',  ( 1.500000000000000444, -15.40502424595132247, -19.43515443678418464 ) ) ;
#11399=ORIENTED_EDGE ( 'NONE', *, *, #4639, .F. ) ;
#11402=CARTESIAN_POINT ( 'NONE',  ( 3.000000000000000888, 22.21333432029563681, 11.02759168516752730 ) ) ;
#11403=ORIENTED_EDGE ( 'NONE', *, *, #11773, .T. ) ;
#11404=FACE_OUTER_BOUND ( 'NONE', #2819, .T. ) ;
#11405=CARTESIAN_POINT ( 'NONE',  ( 3.000000000000000888, 24.45282072769600745, 4.135161237383664812 ) ) ;
#11407=EDGE_CURVE ( 'NONE', #1145, #8746, #5373, .T. ) ;
#11408=AXIS2_PLACEMENT_3D ( 'NONE', #5752, #10143, #4645 ) ;
#11409=CARTESIAN_POINT ( 'NONE',  ( 3.000000000000000888, -16.85990652506910692, 15.64281154287591669 ) ) ;
#11411=DIRECTION ( 'NONE',  ( 0.000000000000000000, 0.9510565162951521989, 0.3090169943749515036 ) ) ;
#11412=ORIENTED_EDGE ( 'NONE', *, *, #11783, .T. ) ;
#11413=DIRECTION ( 'NONE',  ( 1.000000000000000000, 0.000000000000000000, 0.000000000000000000 ) ) ;
#11414=ORIENTED_EDGE ( 'NONE', *, *, #1195, .T. ) ;
#11415=EDGE_CURVE ( 'NONE', #8186, #4467, #7716, .T. ) ;
#11416=ORIENTED_EDGE ( 'NONE', *, *, #2052, .T. ) ;
#11418=DIRECTION ( 'NONE',  ( 0.000000000000000000, 0.4999999999999948375, 0.8660254037844415942 ) ) ;
#11420=CARTESIAN_POINT ( 'NONE',  ( 1.500000000000000444, 23.24434456306325103, 8.645255683529084578 ) ) ;
#11424=DIRECTION ( 'NONE',  ( 0.000000000000000000, 0.000000000000000000, 1.000000000000000000 ) ) ;
#11425=ORIENTED_EDGE ( 'NONE', *, *, #6455, .F. ) ;
#11426=EDGE_LOOP ( 'NONE', ( #9133, #11025, #7360, #291 ) ) ;
#11427=CARTESIAN_POINT ( 'NONE',  ( -10.00000000000000000, 0.000000000000000000, 0.000000000000000000 ) ) ;
#11428=DIRECTION ( 'NONE',  ( 0.000000000000000000, 0.000000000000000000, 1.000000000000000000 ) ) ;
#11429=AXIS2_PLACEMENT_3D ( 'NONE', #7278, #3623, #9921 ) ;
#11430=LINE ( 'NONE', #6770, #7586 ) ;
#11431=DIRECTION ( 'NONE',  ( 1.000000000000000000, -0.000000000000000000, 0.000000000000000000 ) ) ;
#11432=CARTESIAN_POINT ( 'NONE',  ( 3.000000000000000888, 7.402892494506579268, -21.30300407174355115 ) ) ;
#11434=CARTESIAN_POINT ( 'NONE',  ( 0.000000000000000000, 19.43515443678402832, 15.40502424595151609 ) ) ;
#11435=EDGE_CURVE ( 'NONE', #6456, #8246, #5569, .T. ) ;
#11436=ORIENTED_EDGE ( 'NONE', *, *, #3662, .F. ) ;
#11437=ORIENTED_EDGE ( 'NONE', *, *, #8843, .F. ) ;
#11438=CARTESIAN_POINT ( 'NONE',  ( 3.000000000000000888, -11.48910920600668462, -21.97817939804051335 ) ) ;
#11439=ORIENTED_EDGE ( 'NONE', *, *, #9652, .T. ) ;
#11440=CARTESIAN_POINT ( 'NONE',  ( 3.000000000000000888, 19.43515443678423793, -15.40502424595125497 ) ) ;
#11441=DIRECTION ( 'NONE',  ( 1.000000000000000000, 0.000000000000000000, 0.000000000000000000 ) ) ;
#11442=EDGE_CURVE ( 'NONE', #2229, #5263, #6733, .T. ) ;
#11443=DIRECTION ( 'NONE',  ( 0.000000000000000000, -0.8660254037844328234, -0.5000000000000101030 ) ) ;
#11444=ORIENTED_EDGE ( 'NONE', *, *, #587, .F. ) ;
#11445=ADVANCED_FACE ( 'NONE', ( #6435 ), #11873, .T. ) ;
#11446=DIRECTION ( 'NONE',  ( -1.000000000000000000, 0.000000000000000000, 0.000000000000000000 ) ) ;
#11447=AXIS2_PLACEMENT_3D ( 'NONE', #3399, #3155, #2471 ) ;
#11448=EDGE_CURVE ( 'NONE', #8331, #8912, #8209, .T. ) ;
#11449=CARTESIAN_POINT ( 'NONE',  ( 3.000000000000000888, -21.97817939804031440, -11.48910920600707186 ) ) ;
#11451=CARTESIAN_POINT ( 'NONE',  ( 3.000000000000000888, -22.56530478845651544, 4.445336973060782348 ) ) ;
#11452=ORIENTED_EDGE ( 'NONE', *, *, #4977, .T. ) ;
#11453=DIRECTION ( 'NONE',  ( 0.000000000000000000, 0.000000000000000000, 1.000000000000000000 ) ) ;
#11455=DIRECTION ( 'NONE',  ( -1.000000000000000000, 0.000000000000000000, 0.000000000000000000 ) ) ;
#11456=ORIENTED_EDGE ( 'NONE', *, *, #523, .T. ) ;
#11457=CIRCLE ( 'NONE', #903, 24.80000000000000071 ) ;
#11459=EDGE_CURVE ( 'NONE', #4610, #6260, #282, .T. ) ;
#11460=CARTESIAN_POINT ( 'NONE',  ( 0.000000000000000000, -22.54798042742717357, -0.4575788569254196636 ) ) ;
#11462=DIRECTION ( 'NONE',  ( -1.000000000000000000, 0.000000000000000000, -0.000000000000000000 ) ) ;
#11463=CARTESIAN_POINT ( 'NONE',  ( 3.000000000000002665, 4.898587196589412829E-16, -4.000000000000000000 ) ) ;
#11465=AXIS2_PLACEMENT_3D ( 'NONE', #171, #6549, #3859 ) ;
#11467=DIRECTION ( 'NONE',  ( 0.000000000000000000, 0.000000000000000000, -1.000000000000000000 ) ) ;
#11468=ADVANCED_FACE ( 'NONE', ( #10848 ), #6323, .T. ) ;
#11469=CARTESIAN_POINT ( 'NONE',  ( 0.000000000000000000, 0.000000000000000000, 0.000000000000000000 ) ) ;
#11471=VERTEX_POINT ( 'NONE', #6377 ) ;
#11472=ADVANCED_FACE ( 'NONE', ( #802 ), #5399, .T. ) ;
#11473=DIRECTION ( 'NONE',  ( -1.000000000000000000, 0.000000000000000000, 0.000000000000000000 ) ) ;
#11475=CYLINDRICAL_SURFACE ( 'NONE', #5426, 24.80000000000000071 ) ;
#11476=EDGE_CURVE ( 'NONE', #10278, #1752, #11933, .T. ) ;
#11479=DIRECTION ( 'NONE',  ( 0.000000000000000000, 0.000000000000000000, 1.000000000000000000 ) ) ;
#11480=EDGE_CURVE ( 'NONE', #7835, #6502, #10448, .T. ) ;
#11481=CARTESIAN_POINT ( 'NONE',  ( 3.000000000000000888, 0.000000000000000000, 0.000000000000000000 ) ) ;
#11482=ORIENTED_EDGE ( 'NONE', *, *, #10598, .T. ) ;
#11483=ORIENTED_EDGE ( 'NONE', *, *, #11415, .T. ) ;
#11484=CARTESIAN_POINT ( 'NONE',  ( 1.499999999999999556, -13.28910708463113544, -20.93895013827595619 ) ) ;
#11486=CARTESIAN_POINT ( 'NONE',  ( 1.500000000000000444, -13.72351598154911478, 20.65684170206487025 ) ) ;
#11487=CARTESIAN_POINT ( 'NONE',  ( 0.000000000000000000, 0.000000000000000000, 0.000000000000000000 ) ) ;
#11488=CARTESIAN_POINT ( 'NONE',  ( 3.000000000000000888, 0.000000000000000000, 0.000000000000000000 ) ) ;
#11489=AXIS2_PLACEMENT_3D ( 'NONE', #1420, #3255, #10787 ) ;
#11491=DIRECTION ( 'NONE',  ( -1.000000000000000000, 0.000000000000000000, 0.000000000000000000 ) ) ;
#11492=ORIENTED_EDGE ( 'NONE', *, *, #6741, .T. ) ;
#11493=EDGE_LOOP ( 'NONE', ( #1642, #6247, #22, #9636 ) ) ;
#11495=FACE_OUTER_BOUND ( 'NONE', #11909, .T. ) ;
#11496=ORIENTED_EDGE ( 'NONE', *, *, #8102, .F. ) ;
#11498=AXIS2_PLACEMENT_3D ( 'NONE', #6891, #10635, #9709 ) ;
#11499=DIRECTION ( 'NONE',  ( -1.000000000000000000, -0.000000000000000000, 0.000000000000000000 ) ) ;
#11501=DIRECTION ( 'NONE',  ( -1.000000000000000000, 0.000000000000000000, 0.000000000000000000 ) ) ;
#11502=EDGE_LOOP ( 'NONE', ( #8470, #7351, #3231, #6810 ) ) ;
#11503=CARTESIAN_POINT ( 'NONE',  ( 3.000000000000000888, 22.42251312757879234, 5.117118920208566735 ) ) ;
#11504=DIRECTION ( 'NONE',  ( -1.000000000000000000, -0.000000000000000000, -0.000000000000000000 ) ) ;
#11506=CIRCLE ( 'NONE', #10525, 18.49999999999999645 ) ;
#11507=AXIS2_PLACEMENT_3D ( 'NONE', #5225, #10734, #8903 ) ;
#11508=ORIENTED_EDGE ( 'NONE', *, *, #11846, .F. ) ;
#11509=CARTESIAN_POINT ( 'NONE',  ( 3.000000000000000888, 0.000000000000000000, 0.000000000000000000 ) ) ;
#11510=ORIENTED_EDGE ( 'NONE', *, *, #2578, .T. ) ;
#11511=DIRECTION ( 'NONE',  ( 0.000000000000000000, 0.000000000000000000, 1.000000000000000000 ) ) ;
#11512=EDGE_LOOP ( 'NONE', ( #10295, #11189, #11292, #1033 ) ) ;
#11513=EDGE_CURVE ( 'NONE', #4392, #10744, #9283, .T. ) ;
#11515=CIRCLE ( 'NONE', #1153, 24.80000000000000071 ) ;
#11517=DIRECTION ( 'NONE',  ( -1.000000000000000000, -0.000000000000000000, 0.000000000000000000 ) ) ;
#11518=CARTESIAN_POINT ( 'NONE',  ( -10.00000000000000000, 0.000000000000000000, 0.000000000000000000 ) ) ;
#11520=DIRECTION ( 'NONE',  ( -1.000000000000000000, -0.000000000000000000, 0.000000000000000000 ) ) ;
#11521=CARTESIAN_POINT ( 'NONE',  ( 0.000000000000000000, -22.83456483164687256, -2.745295967526231173 ) ) ;
#11522=CIRCLE ( 'NONE', #7203, 9.599999999999999645 ) ;
#11523=EDGE_CURVE ( 'NONE', #9363, #1910, #6159, .T. ) ;
#11524=AXIS2_PLACEMENT_3D ( 'NONE', #10387, #4822, #6826 ) ;
#11526=CARTESIAN_POINT ( 'NONE',  ( 3.000000000000000888, 12.88318129270205148, -18.51065745848364230 ) ) ;
#11527=EDGE_CURVE ( 'NONE', #7105, #9539, #5175, .T. ) ;
#11529=ORIENTED_EDGE ( 'NONE', *, *, #3559, .F. ) ;
#11531=VERTEX_POINT ( 'NONE', #10286 ) ;
#11532=DIRECTION ( 'NONE',  ( 0.000000000000000000, 0.000000000000000000, 1.000000000000000000 ) ) ;
#11534=VECTOR ( 'NONE', #5363, 1000.000000000000000 ) ;
#11535=DIRECTION ( 'NONE',  ( -1.000000000000000000, -0.000000000000000000, 0.000000000000000000 ) ) ;
#11536=VECTOR ( 'NONE', #7605, 1000.000000000000000 ) ;
#11539=DIRECTION ( 'NONE',  ( 0.000000000000000000, -0.5000000000000072164, 0.8660254037844344888 ) ) ;
#11540=CARTESIAN_POINT ( 'NONE',  ( 3.000000000000000888, 0.000000000000000000, 0.000000000000000000 ) ) ;
#11541=ORIENTED_EDGE ( 'NONE', *, *, #9829, .F. ) ;
#11542=AXIS2_PLACEMENT_3D ( 'NONE', #2523, #8030, #11764 ) ;
#11543=AXIS2_PLACEMENT_3D ( 'NONE', #12046, #7454, #6310 ) ;
#11544=AXIS2_PLACEMENT_3D ( 'NONE', #5221, #8098, #689 ) ;
#11545=VERTEX_POINT ( 'NONE', #3862 ) ;
#11546=CARTESIAN_POINT ( 'NONE',  ( 3.000000000000000888, 17.35216073792464542, -17.71842311621511712 ) ) ;
#11548=CARTESIAN_POINT ( 'NONE',  ( 3.000000000000000888, 2.062268319295562424, 22.90635393027947231 ) ) ;
#11549=PLANE ( 'NONE',  #11498 ) ;
#11551=AXIS2_PLACEMENT_3D ( 'NONE', #6406, #899, #3839 ) ;
#11552=AXIS2_PLACEMENT_3D ( 'NONE', #6483, #7328, #5442 ) ;
#11555=CARTESIAN_POINT ( 'NONE',  ( 3.000000000000000888, 4.445336973061170482, -22.56530478845644794 ) ) ;
#11556=VERTEX_POINT ( 'NONE', #9550 ) ;
#11557=ORIENTED_EDGE ( 'NONE', *, *, #4970, .T. ) ;
#11560=VECTOR ( 'NONE', #27, 1000.000000000000000 ) ;
#11561=ORIENTED_EDGE ( 'NONE', *, *, #8542, .T. ) ;
#11562=CIRCLE ( 'NONE', #5672, 9.599999999999999645 ) ;
#11563=DIRECTION ( 'NONE',  ( -1.000000000000000000, 0.000000000000000000, -0.000000000000000000 ) ) ;
#11564=CARTESIAN_POINT ( 'NONE',  ( 8.000000000000000000, 0.000000000000000000, 0.000000000000000000 ) ) ;
#11565=ADVANCED_FACE ( 'NONE', ( #11326 ), #6669, .T. ) ;
#11566=AXIS2_PLACEMENT_3D ( 'NONE', #3059, #3913, #2016 ) ;
#11567=LINE ( 'NONE', #3295, #10083 ) ;
#11568=EDGE_LOOP ( 'NONE', ( #8792, #10234, #11851, #5178 ) ) ;
#11570=FACE_OUTER_BOUND ( 'NONE', #11177, .T. ) ;
#11572=AXIS2_PLACEMENT_3D ( 'NONE', #559, #7964, #5093 ) ;
#11574=ORIENTED_EDGE ( 'NONE', *, *, #2115, .T. ) ;
#11576=CARTESIAN_POINT ( 'NONE',  ( 3.000000000000000888, 9.039786367038837867, 21.14796121233199599 ) ) ;
#11577=VERTEX_POINT ( 'NONE', #1106 ) ;
#11578=DIRECTION ( 'NONE',  ( -1.000000000000000000, -0.000000000000000000, -0.000000000000000000 ) ) ;
#11579=ORIENTED_EDGE ( 'NONE', *, *, #4443, .F. ) ;
#11581=AXIS2_PLACEMENT_3D ( 'NONE', #2321, #10591, #9787 ) ;
#11582=CARTESIAN_POINT ( 'NONE',  ( 3.000000000000000888, -5.117118920208326038, -22.42251312757885273 ) ) ;
#11584=AXIS2_PLACEMENT_3D ( 'NONE', #9470, #3719, #9408 ) ;
#11585=CARTESIAN_POINT ( 'NONE',  ( 3.000000000000000888, -19.29833442572351743, -11.67026512804567062 ) ) ;
#11586=DIRECTION ( 'NONE',  ( -1.000000000000000000, -0.000000000000000000, -0.000000000000000000 ) ) ;
#11588=FACE_OUTER_BOUND ( 'NONE', #10318, .T. ) ;
#11589=CARTESIAN_POINT ( 'NONE',  ( 3.000000000000000888, 0.000000000000000000, 0.000000000000000000 ) ) ;
#11591=DIRECTION ( 'NONE',  ( -1.000000000000000000, 0.000000000000000000, 0.000000000000000000 ) ) ;
#11592=ORIENTED_EDGE ( 'NONE', *, *, #2881, .F. ) ;
#11595=DIRECTION ( 'NONE',  ( 0.000000000000000000, 0.000000000000000000, -1.000000000000000000 ) ) ;
#11596=EDGE_CURVE ( 'NONE', #7251, #2827, #6308, .T. ) ;
#11597=CARTESIAN_POINT ( 'NONE',  ( 0.000000000000000000, -24.45282072769597903, -4.135161237383833566 ) ) ;
#11598=ADVANCED_FACE ( 'NONE', ( #988 ), #4729, .T. ) ;
#11600=VECTOR ( 'NONE', #8635, 1000.000000000000000 ) ;
#11602=CARTESIAN_POINT ( 'NONE',  ( 3.000000000000000888, -12.88318129270165890, -18.51065745848391586 ) ) ;
#11603=DIRECTION ( 'NONE',  ( -1.000000000000000000, 0.000000000000000000, -0.000000000000000000 ) ) ;
#11604=ORIENTED_EDGE ( 'NONE', *, *, #9499, .F. ) ;
#11605=ORIENTED_EDGE ( 'NONE', *, *, #1882, .F. ) ;
#11606=AXIS2_PLACEMENT_3D ( 'NONE', #7019, #606, #11677 ) ;
#11607=VERTEX_POINT ( 'NONE', #2026 ) ;
#11608=CARTESIAN_POINT ( 'NONE',  ( 3.000000000000000888, -14.74749645579999857, -17.06259499759959297 ) ) ;
#11609=CARTESIAN_POINT ( 'NONE',  ( 0.000000000000000000, -5.117118920208326038, -22.42251312757885273 ) ) ;
#11610=DIRECTION ( 'NONE',  ( 0.000000000000000000, 0.000000000000000000, 1.000000000000000000 ) ) ;
#11612=DIRECTION ( 'NONE',  ( 0.000000000000000000, 0.5877852522924690293, 0.8090169943749504489 ) ) ;
#11613=ORIENTED_EDGE ( 'NONE', *, *, #5583, .T. ) ;
#11614=ORIENTED_EDGE ( 'NONE', *, *, #7018, .F. ) ;
#11615=EDGE_CURVE ( 'NONE', #8841, #1098, #9039, .T. ) ;
#11617=ORIENTED_EDGE ( 'NONE', *, *, #481, .F. ) ;
#11618=VECTOR ( 'NONE', #1980, 1000.000000000000000 ) ;
#11619=CARTESIAN_POINT ( 'NONE',  ( 3.000000000000000888, 11.79560690673899970, -19.74380051311527495 ) ) ;
#11620=FACE_OUTER_BOUND ( 'NONE', #6181, .T. ) ;
#11621=EDGE_CURVE ( 'NONE', #7393, #962, #8466, .T. ) ;
#11622=DIRECTION ( 'NONE',  ( -1.000000000000000000, 0.000000000000000000, -0.000000000000000000 ) ) ;
#11623=ORIENTED_EDGE ( 'NONE', *, *, #9218, .T. ) ;
#11624=LINE ( 'NONE', #9612, #1637 ) ;
#11625=EDGE_CURVE ( 'NONE', #1851, #9423, #3743, .T. ) ;
#11626=CARTESIAN_POINT ( 'NONE',  ( 3.000000000000000888, -24.77821629063822328, 1.039229259764401947 ) ) ;
#11628=ORIENTED_EDGE ( 'NONE', *, *, #444, .F. ) ;
#11629=EDGE_CURVE ( 'NONE', #10824, #6719, #11214, .T. ) ;
#11630=CARTESIAN_POINT ( 'NONE',  ( 3.000000000000000888, 15.13242714128119459, 17.31945870441152380 ) ) ;
#11631=CARTESIAN_POINT ( 'NONE',  ( 3.000000000000000888, -23.05871956130116374, -9.128825345753257992 ) ) ;
#11632=VERTEX_POINT ( 'NONE', #5704 ) ;
#11635=DIRECTION ( 'NONE',  ( -1.000000000000000000, 0.000000000000000000, 0.000000000000000000 ) ) ;
#11636=CIRCLE ( 'NONE', #7732, 24.80000000000000071 ) ;
#11637=ORIENTED_EDGE ( 'NONE', *, *, #8931, .T. ) ;
#11639=CARTESIAN_POINT ( 'NONE',  ( 3.000000000000000888, -20.65684170206481696, -13.72351598154918406 ) ) ;
#11641=CARTESIAN_POINT ( 'NONE',  ( 0.000000000000000000, -21.30300407174367905, 7.402892494506218668 ) ) ;
#11643=CARTESIAN_POINT ( 'NONE',  ( 3.000000000000000888, 20.41249101028211754, 9.589108953447965433 ) ) ;
#11644=CIRCLE ( 'NONE', #4420, 9.599999999999997868 ) ;
#11645=ORIENTED_EDGE ( 'NONE', *, *, #11320, .F. ) ;
#11646=LINE ( 'NONE', #10795, #8015 ) ;
#11647=ORIENTED_EDGE ( 'NONE', *, *, #1791, .F. ) ;
#11648=DIRECTION ( 'NONE',  ( -1.000000000000000000, -0.000000000000000000, -0.000000000000000000 ) ) ;
#11649=CARTESIAN_POINT ( 'NONE',  ( 0.000000000000000000, -24.77821629063822328, 1.039229259764401947 ) ) ;
#11650=AXIS2_PLACEMENT_3D ( 'NONE', #3805, #7397, #3918 ) ;
#11651=CYLINDRICAL_SURFACE ( 'NONE', #1399, 9.599999999999997868 ) ;
#11652=FACE_OUTER_BOUND ( 'NONE', #2705, .T. ) ;
#11655=DIRECTION ( 'NONE',  ( -1.000000000000000000, 0.000000000000000000, 0.000000000000000000 ) ) ;
#11656=ORIENTED_EDGE ( 'NONE', *, *, #2783, .F. ) ;
#11657=ADVANCED_FACE ( 'NONE', ( #3679 ), #10465, .T. ) ;
#11658=ORIENTED_EDGE ( 'NONE', *, *, #1579, .F. ) ;
#11659=EDGE_CURVE ( 'NONE', #11531, #1833, #9817, .T. ) ;
#11661=EDGE_CURVE ( 'NONE', #8512, #8970, #6609, .T. ) ;
#11662=DIRECTION ( 'NONE',  ( -1.000000000000000000, -0.000000000000000000, -0.000000000000000000 ) ) ;
#11663=CARTESIAN_POINT ( 'NONE',  ( 3.000000000000000888, 24.53384959170462665, -3.623565124516855640 ) ) ;
#11665=DIRECTION ( 'NONE',  ( 1.000000000000000000, -0.000000000000000000, -0.000000000000000000 ) ) ;
#11666=ADVANCED_FACE ( 'NONE', ( #1962 ), #9433, .T. ) ;
#11667=DIRECTION ( 'NONE',  ( -1.000000000000000000, 0.000000000000000000, 0.000000000000000000 ) ) ;
#11668=ORIENTED_EDGE ( 'NONE', *, *, #81, .T. ) ;
#11671=ORIENTED_EDGE ( 'NONE', *, *, #11923, .T. ) ;
#11672=CARTESIAN_POINT ( 'NONE',  ( 3.000000000000000888, 0.000000000000000000, 0.000000000000000000 ) ) ;
#11674=AXIS2_PLACEMENT_3D ( 'NONE', #7666, #3026, #9564 ) ;
#11675=DIRECTION ( 'NONE',  ( -1.000000000000000000, 0.000000000000000000, 0.000000000000000000 ) ) ;
#11676=VERTEX_POINT ( 'NONE', #5764 ) ;
#11677=DIRECTION ( 'NONE',  ( 0.000000000000000000, 0.000000000000000000, -1.000000000000000000 ) ) ;
#11678=EDGE_CURVE ( 'NONE', #5404, #7624, #2382, .T. ) ;
#11679=CARTESIAN_POINT ( 'NONE',  ( 0.000000000000000000, 17.31945870441167301, -15.13242714128102406 ) ) ;
#11681=ORIENTED_EDGE ( 'NONE', *, *, #6580, .T. ) ;
#11682=EDGE_CURVE ( 'NONE', #7675, #9669, #9230, .T. ) ;
#11683=DIRECTION ( 'NONE',  ( 0.000000000000000000, 0.000000000000000000, 1.000000000000000000 ) ) ;
#11684=AXIS2_PLACEMENT_3D ( 'NONE', #4644, #9350, #11196 ) ;
#11685=EDGE_CURVE ( 'NONE', #5818, #8458, #11768, .T. ) ;
#11686=CARTESIAN_POINT ( 'NONE',  ( 3.000000000000000888, 21.97702544527767188, -6.779701584702504391 ) ) ;
#11687=ORIENTED_EDGE ( 'NONE', *, *, #2766, .F. ) ;
#11689=CARTESIAN_POINT ( 'NONE',  ( 0.000000000000000000, 0.000000000000000000, 22.99899999999999878 ) ) ;
#11690=DIRECTION ( 'NONE',  ( 0.000000000000000000, 0.000000000000000000, -1.000000000000000000 ) ) ;
#11691=ORIENTED_EDGE ( 'NONE', *, *, #442, .T. ) ;
#11692=CIRCLE ( 'NONE', #2915, 9.599999999999997868 ) ;
#11693=DIRECTION ( 'NONE',  ( 0.000000000000000000, -0.6691306063588494668, -0.7431448254774020157 ) ) ;
#11694=AXIS2_PLACEMENT_3D ( 'NONE', #525, #11662, #10747 ) ;
#11695=CARTESIAN_POINT ( 'NONE',  ( 3.000000000000000888, -21.58580335785672233, -6.532525787311189269 ) ) ;
#11697=CARTESIAN_POINT ( 'NONE',  ( 3.000000000000000888, 0.000000000000000000, 0.000000000000000000 ) ) ;
#11700=CARTESIAN_POINT ( 'NONE',  ( 0.000000000000000000, -13.28910708463142498, 20.93895013827577145 ) ) ;
#11701=ORIENTED_EDGE ( 'NONE', *, *, #2125, .T. ) ;
#11702=FACE_OUTER_BOUND ( 'NONE', #95, .T. ) ;
#11703=ORIENTED_EDGE ( 'NONE', *, *, #10846, .T. ) ;
#11705=DIRECTION ( 'NONE',  ( 1.000000000000000000, 0.000000000000000000, 0.000000000000000000 ) ) ;
#11707=EDGE_CURVE ( 'NONE', #2848, #6354, #8054, .T. ) ;
#11708=DIRECTION ( 'NONE',  ( -1.000000000000000000, -0.000000000000000000, 0.000000000000000000 ) ) ;
#11709=LINE ( 'NONE', #8042, #1444 ) ;
#11711=AXIS2_PLACEMENT_3D ( 'NONE', #3292, #8929, #891 ) ;
#11713=FACE_OUTER_BOUND ( 'NONE', #4595, .T. ) ;
#11714=AXIS2_PLACEMENT_3D ( 'NONE', #5754, #8565, #3973 ) ;
#11716=ORIENTED_EDGE ( 'NONE', *, *, #1950, .T. ) ;
#11717=ORIENTED_EDGE ( 'NONE', *, *, #11817, .T. ) ;
#11719=ORIENTED_EDGE ( 'NONE', *, *, #7012, .T. ) ;
#11721=AXIS2_PLACEMENT_3D ( 'NONE', #5099, #5963, #10489 ) ;
#11722=DIRECTION ( 'NONE',  ( 0.000000000000000000, 0.000000000000000000, -1.000000000000000000 ) ) ;
#11724=CIRCLE ( 'NONE', #9972, 24.80000000000000071 ) ;
#11725=DIRECTION ( 'NONE',  ( -1.000000000000000000, -0.000000000000000000, -0.000000000000000000 ) ) ;
#11726=EDGE_CURVE ( 'NONE', #11784, #2212, #8653, .T. ) ;
#11727=CIRCLE ( 'NONE', #4504, 24.80000000000000071 ) ;
#11728=DIRECTION ( 'NONE',  ( -1.000000000000000000, 0.000000000000000000, -0.000000000000000000 ) ) ;
#11729=VERTEX_POINT ( 'NONE', #11679 ) ;
#11730=ORIENTED_EDGE ( 'NONE', *, *, #8616, .T. ) ;
#11734=EDGE_LOOP ( 'NONE', ( #5599, #8454, #1772, #1032 ) ) ;
#11735=CARTESIAN_POINT ( 'NONE',  ( 0.000000000000000000, 0.000000000000000000, 0.000000000000000000 ) ) ;
#11736=ADVANCED_FACE ( 'NONE', ( #1343 ), #6058, .T. ) ;
#11738=DIRECTION ( 'NONE',  ( 0.000000000000000000, 0.000000000000000000, 1.000000000000000000 ) ) ;
#11739=VECTOR ( 'NONE', #7281, 1000.000000000000000 ) ;
#11741=EDGE_LOOP ( 'NONE', ( #4312, #1306, #11756, #3686 ) ) ;
#11742=EDGE_CURVE ( 'NONE', #8458, #10699, #7022, .T. ) ;
#11743=FACE_OUTER_BOUND ( 'NONE', #10320, .T. ) ;
#11744=EDGE_CURVE ( 'NONE', #3286, #8186, #1466, .T. ) ;
#11745=DIRECTION ( 'NONE',  ( 0.000000000000000000, 0.000000000000000000, 1.000000000000000000 ) ) ;
#11747=EDGE_CURVE ( 'NONE', #4581, #9467, #8464, .T. ) ;
#11748=DIRECTION ( 'NONE',  ( -1.000000000000000000, 0.000000000000000000, -0.000000000000000000 ) ) ;
#11749=CARTESIAN_POINT ( 'NONE',  ( -10.00000000000000000, 0.000000000000000000, 0.000000000000000000 ) ) ;
#11750=VECTOR ( 'NONE', #8853, 1000.000000000000000 ) ;
#11751=ORIENTED_EDGE ( 'NONE', *, *, #1873, .T. ) ;
#11752=AXIS2_PLACEMENT_3D ( 'NONE', #9848, #1699, #7192 ) ;
#11754=DIRECTION ( 'NONE',  ( -1.000000000000000000, -0.000000000000000000, 0.000000000000000000 ) ) ;
#11755=DIRECTION ( 'NONE',  ( 0.000000000000000000, 0.000000000000000000, 1.000000000000000000 ) ) ;
#11756=ORIENTED_EDGE ( 'NONE', *, *, #5471, .F. ) ;
#11758=CARTESIAN_POINT ( 'NONE',  ( 0.000000000000000000, 23.24434456306324748, 8.645255683529086355 ) ) ;
#11759=CIRCLE ( 'NONE', #2777, 9.599999999999996092 ) ;
#11760=DIRECTION ( 'NONE',  ( 0.000000000000000000, -0.2079116908177664480, 0.9781476007338040235 ) ) ;
#11764=DIRECTION ( 'NONE',  ( 0.000000000000000000, -0.5877852522924631451, -0.8090169943749546677 ) ) ;
#11765=CARTESIAN_POINT ( 'NONE',  ( 3.000000000000000888, 0.000000000000000000, 0.000000000000000000 ) ) ;
#11767=VERTEX_POINT ( 'NONE', #7714 ) ;
#11768=CIRCLE ( 'NONE', #6491, 22.99900000000000233 ) ;
#11769=CARTESIAN_POINT ( 'NONE',  ( 0.000000000000000000, -15.13242714128131361, 17.31945870441142077 ) ) ;
#11770=AXIS2_PLACEMENT_3D ( 'NONE', #5801, #9527, #10632 ) ;
#11771=CARTESIAN_POINT ( 'NONE',  ( -10.00000000000000000, 0.000000000000000000, 0.000000000000000000 ) ) ;
#11772=ORIENTED_EDGE ( 'NONE', *, *, #2920, .T. ) ;
#11773=EDGE_CURVE ( 'NONE', #7424, #2472, #10989, .T. ) ;
#11774=DIRECTION ( 'NONE',  ( 0.000000000000000000, 0.4999999999999948375, 0.8660254037844415942 ) ) ;
#11775=DIRECTION ( 'NONE',  ( -1.000000000000000000, 0.000000000000000000, 0.000000000000000000 ) ) ;
#11777=AXIS2_PLACEMENT_3D ( 'NONE', #8194, #7320, #11070 ) ;
#11780=CARTESIAN_POINT ( 'NONE',  ( 3.000000000000000888, 18.40266524480607657, -13.79477846460777357 ) ) ;
#11781=VECTOR ( 'NONE', #6628, 1000.000000000000000 ) ;
#11782=ORIENTED_EDGE ( 'NONE', *, *, #3978, .T. ) ;
#11783=EDGE_CURVE ( 'NONE', #11174, #5068, #5329, .T. ) ;
#11784=VERTEX_POINT ( 'NONE', #4967 ) ;
#11785=ORIENTED_EDGE ( 'NONE', *, *, #6875, .T. ) ;
#11786=CIRCLE ( 'NONE', #1427, 19.99999999999999645 ) ;
#11788=DIRECTION ( 'NONE',  ( 0.000000000000000000, 0.000000000000000000, 1.000000000000000000 ) ) ;
#11791=AXIS2_PLACEMENT_3D ( 'NONE', #2744, #7570, #5565 ) ;
#11792=CARTESIAN_POINT ( 'NONE',  ( 3.000000000000000888, -11.48910920600699193, 21.97817939804035348 ) ) ;
#11793=CARTESIAN_POINT ( 'NONE',  ( 0.000000000000000000, 24.53384959170462665, -3.623565124516855640 ) ) ;
#11794=VERTEX_POINT ( 'NONE', #11449 ) ;
#11795=ORIENTED_EDGE ( 'NONE', *, *, #7356, .F. ) ;
#11796=ORIENTED_EDGE ( 'NONE', *, *, #4424, .T. ) ;
#11797=DIRECTION ( 'NONE',  ( 0.000000000000000000, 0.1045284632676536929, -0.9945218953682732899 ) ) ;
#11799=CARTESIAN_POINT ( 'NONE',  ( 0.000000000000000000, -13.79477846460808799, 18.40266524480583854 ) ) ;
#11800=AXIS2_PLACEMENT_3D ( 'NONE', #269, #4807, #6696 ) ;
#11801=DIRECTION ( 'NONE',  ( -1.000000000000000000, 0.000000000000000000, 0.000000000000000000 ) ) ;
#11802=VERTEX_POINT ( 'NONE', #11626 ) ;
#11803=CARTESIAN_POINT ( 'NONE',  ( 0.000000000000000000, 11.79560690673872436, 19.74380051311544193 ) ) ;
#11804=DIRECTION ( 'NONE',  ( 0.000000000000000000, 0.8660254037844363761, 0.5000000000000039968 ) ) ;
#11806=DIRECTION ( 'NONE',  ( 0.000000000000000000, 0.000000000000000000, 1.000000000000000000 ) ) ;
#11807=DIRECTION ( 'NONE',  ( 0.000000000000000000, 0.8660254037844397068, -0.4999999999999980016 ) ) ;
#11808=VERTEX_POINT ( 'NONE', #5022 ) ;
#11809=EDGE_CURVE ( 'NONE', #1972, #1329, #4344, .T. ) ;
#11810=ORIENTED_EDGE ( 'NONE', *, *, #3694, .F. ) ;
#11812=EDGE_CURVE ( 'NONE', #4077, #384, #5999, .T. ) ;
#11813=ORIENTED_EDGE ( 'NONE', *, *, #11985, .F. ) ;
#11814=DIRECTION ( 'NONE',  ( -1.000000000000000000, -0.000000000000000000, 0.000000000000000000 ) ) ;
#11815=EDGE_CURVE ( 'NONE', #4516, #7393, #425, .T. ) ;
#11816=ORIENTED_EDGE ( 'NONE', *, *, #2058, .F. ) ;
#11817=EDGE_CURVE ( 'NONE', #429, #9019, #828, .T. ) ;
#11818=CARTESIAN_POINT ( 'NONE',  ( 3.000000000000000888, -6.779701584702886308, 21.97702544527755109 ) ) ;
#11819=DIRECTION ( 'NONE',  ( 0.000000000000000000, 0.9945218953682736229, -0.1045284632676503622 ) ) ;
#11821=DIRECTION ( 'NONE',  ( -1.000000000000000000, -0.000000000000000000, 0.000000000000000000 ) ) ;
#11823=FACE_OUTER_BOUND ( 'NONE', #8441, .T. ) ;
#11825=DIRECTION ( 'NONE',  ( 0.000000000000000000, 0.000000000000000000, 1.000000000000000000 ) ) ;
#11826=ORIENTED_EDGE ( 'NONE', *, *, #5702, .F. ) ;
#11827=ADVANCED_FACE ( 'NONE', ( #11570 ), #3190, .T. ) ;
#11829=CARTESIAN_POINT ( 'NONE',  ( -10.00000000000000000, 0.000000000000000000, 0.000000000000000000 ) ) ;
#11830=VERTEX_POINT ( 'NONE', #9727 ) ;
#11832=CYLINDRICAL_SURFACE ( 'NONE', #7502, 9.599999999999997868 ) ;
#11834=ADVANCED_FACE ( 'NONE', ( #8818 ), #423, .T. ) ;
#11837=CARTESIAN_POINT ( 'NONE',  ( 0.000000000000000000, 21.76479567747241717, 7.432877647175279101 ) ) ;
#11838=CARTESIAN_POINT ( 'NONE',  ( 3.000000000000000888, 13.79477846460795831, 18.40266524480593802 ) ) ;
#11839=ORIENTED_EDGE ( 'NONE', *, *, #1685, .T. ) ;
#11841=ORIENTED_EDGE ( 'NONE', *, *, #8380, .T. ) ;
#11842=EDGE_LOOP ( 'NONE', ( #2271, #9604, #7289, #432 ) ) ;
#11844=CARTESIAN_POINT ( 'NONE',  ( 3.000000000000000888, 2.811977935938088535, -22.37663021667340857 ) ) ;
#11845=CYLINDRICAL_SURFACE ( 'NONE', #9358, 19.99999999999999645 ) ;
#11846=EDGE_CURVE ( 'NONE', #6939, #2895, #4341, .T. ) ;
#11848=DIRECTION ( 'NONE',  ( -1.000000000000000000, 0.000000000000000000, -0.000000000000000000 ) ) ;
#11849=CARTESIAN_POINT ( 'NONE',  ( 0.000000000000000000, 0.3433949777334901476, -22.99643626497956461 ) ) ;
#11850=ORIENTED_EDGE ( 'NONE', *, *, #6168, .F. ) ;
#11851=ORIENTED_EDGE ( 'NONE', *, *, #3569, .F. ) ;
#11853=CARTESIAN_POINT ( 'NONE',  ( 3.000000000000000888, -15.42759117534374447, -16.45023496161680754 ) ) ;
#11856=FACE_OUTER_BOUND ( 'NONE', #11741, .T. ) ;
#11857=ORIENTED_EDGE ( 'NONE', *, *, #9886, .T. ) ;
#11858=ADVANCED_FACE ( 'NONE', ( #6306 ), #5201, .T. ) ;
#11859=DIRECTION ( 'NONE',  ( 1.000000000000000000, 0.000000000000000000, -0.000000000000000000 ) ) ;
#11860=DIRECTION ( 'NONE',  ( -1.000000000000000000, -0.000000000000000000, -0.000000000000000000 ) ) ;
#11862=DIRECTION ( 'NONE',  ( -1.000000000000000000, 0.000000000000000000, -0.000000000000000000 ) ) ;
#11863=ORIENTED_EDGE ( 'NONE', *, *, #2288, .T. ) ;
#11864=CARTESIAN_POINT ( 'NONE',  ( 3.000000000000000888, 0.000000000000000000, 0.000000000000000000 ) ) ;
#11865=ORIENTED_EDGE ( 'NONE', *, *, #5328, .F. ) ;
#11869=ORIENTED_EDGE ( 'NONE', *, *, #2022, .T. ) ;
#11870=FACE_OUTER_BOUND ( 'NONE', #11203, .T. ) ;
#11871=ORIENTED_EDGE ( 'NONE', *, *, #5457, .F. ) ;
#11872=CARTESIAN_POINT ( 'NONE',  ( 3.000000000000000888, 4.240409074144393387, -22.15038895030644639 ) ) ;
#11873=CYLINDRICAL_SURFACE ( 'NONE', #3614, 24.80000000000000071 ) ;
#11875=CARTESIAN_POINT ( 'NONE',  ( 3.000000000000000888, -9.039786367038983528, 21.14796121233193560 ) ) ;
#11876=DIRECTION ( 'NONE',  ( 0.000000000000000000, 0.000000000000000000, 1.000000000000000000 ) ) ;
#11877=VERTEX_POINT ( 'NONE', #8936 ) ;
#11878=EDGE_LOOP ( 'NONE', ( #581, #7345, #5770, #2621 ) ) ;
#11879=EDGE_CURVE ( 'NONE', #9193, #11632, #2193, .T. ) ;
#11880=DIRECTION ( 'NONE',  ( 0.000000000000000000, -0.9135454576426046414, 0.4067366430757920481 ) ) ;
#11881=ORIENTED_EDGE ( 'NONE', *, *, #11096, .F. ) ;
#11883=AXIS2_PLACEMENT_3D ( 'NONE', #11255, #7380, #157 ) ;
#11884=EDGE_CURVE ( 'NONE', #2253, #1256, #2503, .T. ) ;
#11886=CARTESIAN_POINT ( 'NONE',  ( 0.000000000000000000, 20.65684170206491999, 13.72351598154904195 ) ) ;
#11888=DIRECTION ( 'NONE',  ( -1.000000000000000000, 0.000000000000000000, 0.000000000000000000 ) ) ;
#11889=DIRECTION ( 'NONE',  ( -1.000000000000000000, -0.000000000000000000, 0.000000000000000000 ) ) ;
#11890=DIRECTION ( 'NONE',  ( -1.000000000000000000, -0.000000000000000000, 0.000000000000000000 ) ) ;
#11892=EDGE_CURVE ( 'NONE', #8778, #2132, #2981, .T. ) ;
#11894=DIRECTION ( 'NONE',  ( 0.000000000000000000, 0.000000000000000000, 1.000000000000000000 ) ) ;
#11895=EDGE_CURVE ( 'NONE', #8200, #35, #11380, .T. ) ;
#11896=CIRCLE ( 'NONE', #6620, 9.599999999999997868 ) ;
#11897=CARTESIAN_POINT ( 'NONE',  ( 0.000000000000000000, 13.23915371906980631, -18.80635025205156907 ) ) ;
#11898=VERTEX_POINT ( 'NONE', #4459 ) ;
#11899=AXIS2_PLACEMENT_3D ( 'NONE', #10552, #5909, #2171 ) ;
#11900=VERTEX_POINT ( 'NONE', #784 ) ;
#11902=CIRCLE ( 'NONE', #764, 22.99900000000000233 ) ;
#11903=AXIS2_PLACEMENT_3D ( 'NONE', #6535, #10211, #11254 ) ;
#11904=DIRECTION ( 'NONE',  ( 0.000000000000000000, -0.9510565162951566398, 0.3090169943749381254 ) ) ;
#11905=DIRECTION ( 'NONE',  ( 0.000000000000000000, 0.000000000000000000, -1.000000000000000000 ) ) ;
#11907=CARTESIAN_POINT ( 'NONE',  ( 3.000000000000000888, -19.29833442572367375, 11.67026512804540950 ) ) ;
#11908=DIRECTION ( 'NONE',  ( -1.000000000000000000, -0.000000000000000000, -0.000000000000000000 ) ) ;
#11909=EDGE_LOOP ( 'NONE', ( #3759, #5797, #3057, #5830 ) ) ;
#11910=ORIENTED_EDGE ( 'NONE', *, *, #3540, .T. ) ;
#11911=FACE_OUTER_BOUND ( 'NONE', #10613, .T. ) ;
#11912=DIRECTION ( 'NONE',  ( -1.000000000000000000, -0.000000000000000000, 0.000000000000000000 ) ) ;
#11913=CARTESIAN_POINT ( 'NONE',  ( 3.000000000000000888, 11.20082935824075321, 20.08719549084868561 ) ) ;
#11914=CIRCLE ( 'NONE', #8413, 22.99899999999999878 ) ;
#11915=EDGE_CURVE ( 'NONE', #9819, #9915, #9238, .T. ) ;
#11916=DIRECTION ( 'NONE',  ( -1.000000000000000000, -0.000000000000000000, -0.000000000000000000 ) ) ;
#11917=VECTOR ( 'NONE', #3034, 1000.000000000000000 ) ;
#11918=CARTESIAN_POINT ( 'NONE',  ( 0.000000000000000000, 0.000000000000000000, 0.000000000000000000 ) ) ;
#11920=CARTESIAN_POINT ( 'NONE',  ( 3.000000000000000888, 13.72351598154897268, 20.65684170206495907 ) ) ;
#11921=VERTEX_POINT ( 'NONE', #9966 ) ;
#11922=DIRECTION ( 'NONE',  ( 0.000000000000000000, -0.9945218953682744001, 0.1045284632676437564 ) ) ;
#11923=EDGE_CURVE ( 'NONE', #3460, #4090, #10805, .T. ) ;
#11924=CIRCLE ( 'NONE', #10750, 9.599999999999997868 ) ;
#11925=EDGE_LOOP ( 'NONE', ( #4988, #11384, #3102, #39 ) ) ;
#11926=ORIENTED_EDGE ( 'NONE', *, *, #4074, .T. ) ;
#11927=CIRCLE ( 'NONE', #5683, 9.599999999999996092 ) ;
#11929=EDGE_LOOP ( 'NONE', ( #10733, #4157, #5513, #6639 ) ) ;
#11930=CARTESIAN_POINT ( 'NONE',  ( 1.499999999999999556, -3.623565124517271752, 24.53384959170456270 ) ) ;
#11931=ORIENTED_EDGE ( 'NONE', *, *, #1649, .T. ) ;
#11932=DIRECTION ( 'NONE',  ( -1.000000000000000000, 0.000000000000000000, 0.000000000000000000 ) ) ;
#11933=LINE ( 'NONE', #8336, #4593 ) ;
#11935=AXIS2_PLACEMENT_3D ( 'NONE', #8399, #7343, #5454 ) ;
#11936=VECTOR ( 'NONE', #5244, 1000.000000000000000 ) ;
#11937=DIRECTION ( 'NONE',  ( 0.000000000000000000, 0.9135454576425990902, 0.4067366430758041496 ) ) ;
#11938=VECTOR ( 'NONE', #7027, 1000.000000000000000 ) ;
#11939=DIRECTION ( 'NONE',  ( -1.000000000000000000, 0.000000000000000000, 0.000000000000000000 ) ) ;
#11940=ORIENTED_EDGE ( 'NONE', *, *, #1003, .F. ) ;
#11941=FACE_OUTER_BOUND ( 'NONE', #1684, .T. ) ;
#11942=ORIENTED_EDGE ( 'NONE', *, *, #3454, .T. ) ;
#11944=CIRCLE ( 'NONE', #5081, 22.99899999999999878 ) ;
#11945=CYLINDRICAL_SURFACE ( 'NONE', #1087, 24.80000000000000071 ) ;
#11946=ORIENTED_EDGE ( 'NONE', *, *, #11726, .T. ) ;
#11947=AXIS2_PLACEMENT_3D ( 'NONE', #7295, #2479, #11894 ) ;
#11949=CARTESIAN_POINT ( 'NONE',  ( 3.000000000000000888, -5.117118920208643118, 22.42251312757878168 ) ) ;
#11950=FACE_OUTER_BOUND ( 'NONE', #11734, .T. ) ;
#11951=DIRECTION ( 'NONE',  ( 0.000000000000000000, 0.000000000000000000, 1.000000000000000000 ) ) ;
#11953=CARTESIAN_POINT ( 'NONE',  ( 0.000000000000000000, -16.85990652506889376, -15.64281154287614584 ) ) ;
#11954=AXIS2_PLACEMENT_3D ( 'NONE', #5839, #261, #7543 ) ;
#11955=DIRECTION ( 'NONE',  ( -1.000000000000000000, -0.000000000000000000, 0.000000000000000000 ) ) ;
#11956=EDGE_CURVE ( 'NONE', #7635, #10066, #10217, .T. ) ;
#11958=ORIENTED_EDGE ( 'NONE', *, *, #227, .F. ) ;
#11960=ORIENTED_EDGE ( 'NONE', *, *, #3011, .T. ) ;
#11961=EDGE_CURVE ( 'NONE', #7191, #5600, #2987, .T. ) ;
#11963=EDGE_CURVE ( 'NONE', #9081, #862, #7262, .T. ) ;
#11964=DIRECTION ( 'NONE',  ( -1.000000000000000000, 0.000000000000000000, 0.000000000000000000 ) ) ;
#11965=FACE_OUTER_BOUND ( 'NONE', #715, .T. ) ;
#11966=EDGE_CURVE ( 'NONE', #6502, #6248, #2793, .T. ) ;
#11969=ORIENTED_EDGE ( 'NONE', *, *, #3703, .T. ) ;
#11970=DIRECTION ( 'NONE',  ( -1.000000000000000000, -0.000000000000000000, 0.000000000000000000 ) ) ;
#11971=ORIENTED_EDGE ( 'NONE', *, *, #7333, .F. ) ;
#11972=VERTEX_POINT ( 'NONE', #607 ) ;
#11973=ORIENTED_EDGE ( 'NONE', *, *, #9617, .F. ) ;
#11974=EDGE_CURVE ( 'NONE', #5828, #12032, #2003, .T. ) ;
#11975=DIRECTION ( 'NONE',  ( 0.000000000000000000, 0.9781476007338049117, 0.2079116908177629230 ) ) ;
#11976=AXIS2_PLACEMENT_3D ( 'NONE', #11735, #7073, #11797 ) ;
#11977=VECTOR ( 'NONE', #3642, 1000.000000000000000 ) ;
#11979=CARTESIAN_POINT ( 'NONE',  ( 3.000000000000000888, -24.75110766671653195, 1.556492618230561842 ) ) ;
#11980=CARTESIAN_POINT ( 'NONE',  ( 3.000000000000000888, -11.20082935824061110, -20.08719549084876732 ) ) ;
#11981=AXIS2_PLACEMENT_3D ( 'NONE', #3490, #7200, #8193 ) ;
#11982=FACE_OUTER_BOUND ( 'NONE', #11493, .T. ) ;
#11983=DIRECTION ( 'NONE',  ( -1.000000000000000000, -0.000000000000000000, 0.000000000000000000 ) ) ;
#11985=EDGE_CURVE ( 'NONE', #11830, #10120, #2596, .T. ) ;
#11986=CARTESIAN_POINT ( 'NONE',  ( 0.000000000000000000, 6.168200451486084646, -24.02068490260606026 ) ) ;
#11987=EDGE_LOOP ( 'NONE', ( #8585, #3814, #997, #9301 ) ) ;
#11989=DIRECTION ( 'NONE',  ( -1.000000000000000000, 0.000000000000000000, 0.000000000000000000 ) ) ;
#11990=ORIENTED_EDGE ( 'NONE', *, *, #11963, .T. ) ;
#11991=EDGE_CURVE ( 'NONE', #10351, #4929, #6503, .T. ) ;
#11992=VECTOR ( 'NONE', #697, 1000.000000000000000 ) ;
#11993=VERTEX_POINT ( 'NONE', #8135 ) ;
#11995=ORIENTED_EDGE ( 'NONE', *, *, #12079, .T. ) ;
#11996=DIRECTION ( 'NONE',  ( -1.000000000000000000, -0.000000000000000000, -0.000000000000000000 ) ) ;
#11997=ORIENTED_EDGE ( 'NONE', *, *, #2622, .F. ) ;
#11998=CYLINDRICAL_SURFACE ( 'NONE', #4952, 9.599999999999997868 ) ;
#11999=EDGE_CURVE ( 'NONE', #1084, #5065, #4754, .T. ) ;
#12001=DIRECTION ( 'NONE',  ( 0.000000000000000000, 0.000000000000000000, 1.000000000000000000 ) ) ;
#12003=AXIS2_PLACEMENT_3D ( 'NONE', #2643, #3566, #6255 ) ;
#12004=CARTESIAN_POINT ( 'NONE',  ( 3.000000000000000888, -6.532525787311115550, 21.58580335785674365 ) ) ;
#12005=DIRECTION ( 'NONE',  ( -1.000000000000000000, 0.000000000000000000, 0.000000000000000000 ) ) ;
#12006=ORIENTED_EDGE ( 'NONE', *, *, #1414, .F. ) ;
#12007=CARTESIAN_POINT ( 'NONE',  ( 3.000000000000000888, -7.402892494506437160, 21.30300407174360444 ) ) ;
#12010=AXIS2_PLACEMENT_3D ( 'NONE', #10043, #1664, #12001 ) ;
#12011=CYLINDRICAL_SURFACE ( 'NONE', #7323, 9.599999999999997868 ) ;
#12014=DIRECTION ( 'NONE',  ( -1.000000000000000000, -0.000000000000000000, 0.000000000000000000 ) ) ;
#12015=DIRECTION ( 'NONE',  ( -1.000000000000000000, -0.000000000000000000, 0.000000000000000000 ) ) ;
#12016=CARTESIAN_POINT ( 'NONE',  ( 3.000000000000000888, 20.93895013827581764, 13.28910708463135570 ) ) ;
#12019=VERTEX_POINT ( 'NONE', #6582 ) ;
#12020=ORIENTED_EDGE ( 'NONE', *, *, #556, .F. ) ;
#12021=ORIENTED_EDGE ( 'NONE', *, *, #11233, .T. ) ;
#12022=CARTESIAN_POINT ( 'NONE',  ( 0.000000000000000000, 21.14796121233209192, -9.039786367038628256 ) ) ;
#12024=DIRECTION ( 'NONE',  ( -1.000000000000000000, -0.000000000000000000, -0.000000000000000000 ) ) ;
#12025=CYLINDRICAL_SURFACE ( 'NONE', #10730, 9.599999999999997868 ) ;
#12026=CIRCLE ( 'NONE', #6173, 9.599999999999997868 ) ;
#12029=DIRECTION ( 'NONE',  ( -1.000000000000000000, 0.000000000000000000, 0.000000000000000000 ) ) ;
#12030=EDGE_LOOP ( 'NONE', ( #4883, #10964, #9107, #11156 ) ) ;
#12031=EDGE_CURVE ( 'NONE', #8566, #5393, #10997, .T. ) ;
#12032=VERTEX_POINT ( 'NONE', #8432 ) ;
#12033=VECTOR ( 'NONE', #1418, 1000.000000000000000 ) ;
#12034=EDGE_CURVE ( 'NONE', #11531, #9193, #11115, .T. ) ;
#12035=ORIENTED_EDGE ( 'NONE', *, *, #5161, .F. ) ;
#12038=DIRECTION ( 'NONE',  ( 1.000000000000000000, 0.000000000000000000, 0.000000000000000000 ) ) ;
#12039=CARTESIAN_POINT ( 'NONE',  ( 3.000000000000000888, -15.80756504416678432, -19.10918332567973721 ) ) ;
#12040=DIRECTION ( 'NONE',  ( 0.000000000000000000, 0.000000000000000000, 1.000000000000000000 ) ) ;
#12041=AXIS2_PLACEMENT_3D ( 'NONE', #420, #3063, #11443 ) ;
#12045=EDGE_CURVE ( 'NONE', #2082, #5009, #9431, .T. ) ;
#12046=CARTESIAN_POINT ( 'NONE',  ( 3.000000000000000888, 0.000000000000000000, 0.000000000000000000 ) ) ;
#12047=EDGE_LOOP ( 'NONE', ( #1819, #5810, #10800, #172 ) ) ;
#12048=ORIENTED_EDGE ( 'NONE', *, *, #10093, .T. ) ;
#12049=DIRECTION ( 'NONE',  ( -1.000000000000000000, 0.000000000000000000, 0.000000000000000000 ) ) ;
#12050=VERTEX_POINT ( 'NONE', #7304 ) ;
#12051=ORIENTED_EDGE ( 'NONE', *, *, #1836, .F. ) ;
#12053=ORIENTED_EDGE ( 'NONE', *, *, #7677, .F. ) ;
#12054=CARTESIAN_POINT ( 'NONE',  ( 0.000000000000000000, -17.31945870441136748, -15.13242714128137401 ) ) ;
#12055=VERTEX_POINT ( 'NONE', #3714 ) ;
#12057=CARTESIAN_POINT ( 'NONE',  ( 3.000000000000000888, 20.78471918669872665, -8.753070780932940664 ) ) ;
#12059=CARTESIAN_POINT ( 'NONE',  ( 3.000000000000000888, 16.45023496161665122, 15.42759117534391322 ) ) ;
#12060=CARTESIAN_POINT ( 'NONE',  ( 0.000000000000000000, 0.000000000000000000, 0.000000000000000000 ) ) ;
#12061=ORIENTED_EDGE ( 'NONE', *, *, #1157, .T. ) ;
#12062=ORIENTED_EDGE ( 'NONE', *, *, #7018, .T. ) ;
#12063=DIRECTION ( 'NONE',  ( -1.000000000000000000, 0.000000000000000000, 0.000000000000000000 ) ) ;
#12064=EDGE_LOOP ( 'NONE', ( #1319, #10511, #1662, #2707 ) ) ;
#12066=CARTESIAN_POINT ( 'NONE',  ( 3.000000000000000888, 22.42251312757886339, -5.117118920208268307 ) ) ;
#12068=CIRCLE ( 'NONE', #1915, 22.99900000000000233 ) ;
#12069=CARTESIAN_POINT ( 'NONE',  ( 0.000000000000000000, -21.58580335785681115, 6.532525787310899723 ) ) ;
#12070=DIRECTION ( 'NONE',  ( 0.000000000000000000, 0.9781476007338048007, 0.2079116908177630618 ) ) ;
#12071=FACE_OUTER_BOUND ( 'NONE', #10658, .T. ) ;
#12074=FACE_OUTER_BOUND ( 'NONE', #5197, .T. ) ;
#12075=DIRECTION ( 'NONE',  ( 0.000000000000000000, 0.000000000000000000, 1.000000000000000000 ) ) ;
#12076=ORIENTED_EDGE ( 'NONE', *, *, #8191, .T. ) ;
#12077=VECTOR ( 'NONE', #6591, 1000.000000000000000 ) ;
#12079=EDGE_CURVE ( 'NONE', #8706, #3600, #898, .T. ) ;
#12080=ORIENTED_EDGE ( 'NONE', *, *, #4810, .F. ) ;
#12081=DIRECTION ( 'NONE',  ( -1.000000000000000000, -0.000000000000000000, -0.000000000000000000 ) ) ;
#12083=LINE ( 'NONE', #1869, #11560 ) ;
#12084=CARTESIAN_POINT ( 'NONE',  ( 3.000000000000000888, 0.000000000000000000, 0.000000000000000000 ) ) ;
#12085=CARTESIAN_POINT ( 'NONE',  ( 1.499999999999999556, -9.128825345753185161, 23.05871956130119571 ) ) ;
#12087=VECTOR ( 'NONE', #3235, 1000.000000000000000 ) ;
#12088=AXIS2_PLACEMENT_3D ( 'NONE', #4013, #7738, #2794 ) ;
#12090=DIRECTION ( 'NONE',  ( 0.000000000000000000, 0.000000000000000000, 1.000000000000000000 ) ) ;
#12091=VERTEX_POINT ( 'NONE', #10261 ) ;
#12092=ORIENTED_EDGE ( 'NONE', *, *, #7934, .T. ) ;
#12093=CARTESIAN_POINT ( 'NONE',  ( 3.000000000000000888, -22.42251312757876036, -5.117118920208720390 ) ) ;
#12094=VECTOR ( 'NONE', #4568, 1000.000000000000000 ) ;
#12095=LINE ( 'NONE', #2741, #8237 ) ;
#12096=CARTESIAN_POINT ( 'NONE',  ( 0.000000000000000000, -5.135568396240178579, 21.96011696265489377 ) ) ;
#12097=LINE ( 'NONE', #2007, #12077 ) ;
#12098=DIRECTION ( 'NONE',  ( 0.000000000000000000, -0.4067366430757887730, -0.9135454576426059736 ) ) ;
#12101=VECTOR ( 'NONE', #3430, 1000.000000000000000 ) ;
#12102=AXIS2_PLACEMENT_3D ( 'NONE', #5925, #9474, #1090 ) ;
#12105=EDGE_CURVE ( 'NONE', #2327, #730, #1747, .T. ) ;
#12106=ORIENTED_EDGE ( 'NONE', *, *, #9518, .T. ) ;
#12108=DIRECTION ( 'NONE',  ( -1.000000000000000000, 0.000000000000000000, 0.000000000000000000 ) ) ;
#12109=ORIENTED_EDGE ( 'NONE', *, *, #1063, .F. ) ;
#12110=ORIENTED_EDGE ( 'NONE', *, *, #5107, .F. ) ;
#12112=EDGE_CURVE ( 'NONE', #2984, #8511, #2799, .T. ) ;
#12113=FACE_OUTER_BOUND ( 'NONE', #8048, .T. ) ;
#12114=ORIENTED_EDGE ( 'NONE', *, *, #3856, .F. ) ;
#12115=ADVANCED_FACE ( 'NONE', ( #5554 ), #4575, .T. ) ;
#12116=CIRCLE ( 'NONE', #4700, 24.80000000000000071 ) ;
#12117=ORIENTED_EDGE ( 'NONE', *, *, #4525, .F. ) ;
ENDSEC;
END-ISO-10303-21;
